ISO-10303-21;
HEADER;
FILE_DESCRIPTION (('STEP AP203'),
    '1' );
FILE_NAME ('Part2_handle2.step',
    '2026-10-06T15:07:10',
    ( '' ),
    ( '' ),
    'SwSTEP 2.0',
    'SolidWorks 2024',
    '' );
FILE_SCHEMA (( 'AUTOMOTIVE_DESIGN' ));
ENDSEC;

DATA;
#4=ORIENTED_EDGE ( 'NONE', *, *, #27611, .T. ) ;
#16=CARTESIAN_POINT ( 'NONE',  ( -21.76338877130672245, 18.20021209127403239, 1.779283699008895159 ) ) ;
#26=FACE_OUTER_BOUND ( 'NONE', #27997, .T. ) ;
#29=CARTESIAN_POINT ( 'NONE',  ( 26.04699060503310193, 19.53185396608588320, 1.500000000000000000 ) ) ;
#34=DIRECTION ( 'NONE',  ( -0.000000000000000000, -0.000000000000000000, 1.000000000000000000 ) ) ;
#46=EDGE_LOOP ( 'NONE', ( #17358, #23961, #2698, #31842 ) ) ;
#60=CARTESIAN_POINT ( 'NONE',  ( -40.65244704454411107, -12.44919619934167088, 5.499999999999999112 ) ) ;
#67=ADVANCED_FACE ( 'NONE', ( #1394 ), #31658, .F. ) ;
#80=FACE_OUTER_BOUND ( 'NONE', #3087, .T. ) ;
#87=DIRECTION ( 'NONE',  ( 4.458171167563049465E-29, -1.000000000000000000, -5.782411586589359611E-15 ) ) ;
#89=CIRCLE ( 'NONE', #23575, 2.099999999999997868 ) ;
#100=ORIENTED_EDGE ( 'NONE', *, *, #5872, .F. ) ;
#106=AXIS2_PLACEMENT_3D ( 'NONE', #14206, #26936, #32117 ) ;
#108=ORIENTED_EDGE ( 'NONE', *, *, #26018, .T. ) ;
#123=ADVANCED_FACE ( 'NONE', ( #13736 ), #14864, .T. ) ;
#126=CARTESIAN_POINT ( 'NONE',  ( 107.7308922075239082, 16.67966155151041363, -1.408250966677084381 ) ) ;
#128=DIRECTION ( 'NONE',  ( 0.000000000000000000, 0.000000000000000000, 1.000000000000000000 ) ) ;
#138=VECTOR ( 'NONE', #31382, 1000.000000000000114 ) ;
#145=CARTESIAN_POINT ( 'NONE',  ( 108.0191169540316167, 18.28461066811921754, 4.532506712702909724 ) ) ;
#148=AXIS2_PLACEMENT_3D ( 'NONE', #28905, #8200, #6010 ) ;
#167=VECTOR ( 'NONE', #10719, 1000.000000000000114 ) ;
#169=CIRCLE ( 'NONE', #6539, 2.099999999999997868 ) ;
#186=CARTESIAN_POINT ( 'NONE',  ( 107.7222261516258612, 19.48138685844068974, -4.344084370466780420 ) ) ;
#190=LINE ( 'NONE', #18394, #23629 ) ;
#229=EDGE_CURVE ( 'NONE', #7402, #25225, #10396, .T. ) ;
#230=LINE ( 'NONE', #2912, #2926 ) ;
#244=EDGE_CURVE ( 'NONE', #31304, #5929, #3201, .T. ) ;
#245=( BOUNDED_CURVE ( )  B_SPLINE_CURVE ( 3, ( #13031, #23237, #341, #27192 ),
 .UNSPECIFIED., .F., .F. ) 
 B_SPLINE_CURVE_WITH_KNOTS ( ( 4, 4 ),
 ( 0.000000000000000000, 1.570796326794914100 ),
 .UNSPECIFIED. ) 
 CURVE ( )  GEOMETRIC_REPRESENTATION_ITEM ( )  RATIONAL_B_SPLINE_CURVE ( ( 1.000000000000000000, 0.8047378541243608296, 0.8047378541243608296, 1.000000000000000000 ) ) 
 REPRESENTATION_ITEM ( '' )  );
#250=DIRECTION ( 'NONE',  ( 0.000000000000000000, 0.000000000000000000, 1.000000000000000000 ) ) ;
#267=EDGE_CURVE ( 'NONE', #17721, #28345, #13209, .T. ) ;
#269=FACE_OUTER_BOUND ( 'NONE', #21675, .T. ) ;
#282=ADVANCED_FACE ( 'NONE', ( #5372, #20917 ), #12718, .T. ) ;
#288=ORIENTED_EDGE ( 'NONE', *, *, #372, .T. ) ;
#293=VERTEX_POINT ( 'NONE', #28613 ) ;
#295=ADVANCED_FACE ( 'NONE', ( #25777 ), #18309, .T. ) ;
#301=DIRECTION ( 'NONE',  ( 0.4999999999999981681, 0.8660254037844397068, 0.000000000000000000 ) ) ;
#318=CARTESIAN_POINT ( 'NONE',  ( 108.0671932761865861, 18.55231859988835552, 4.648224005204301790 ) ) ;
#337=CARTESIAN_POINT ( 'NONE',  ( 108.3527736681033531, 20.14254290672267800, -1.579327705512915569 ) ) ;
#338=ORIENTED_EDGE ( 'NONE', *, *, #20871, .F. ) ;
#341=CARTESIAN_POINT ( 'NONE',  ( -31.68982948510041808, 0.2071067811865522357, 1.500000000000005329 ) ) ;
#346=EDGE_CURVE ( 'NONE', #14768, #27103, #14556, .T. ) ;
#351=ORIENTED_EDGE ( 'NONE', *, *, #13040, .F. ) ;
#359=CARTESIAN_POINT ( 'NONE',  ( -18.90990005423338971, 16.40670164838886791, 1.822708526801201767 ) ) ;
#371=CARTESIAN_POINT ( 'NONE',  ( 23.81497248397844402, 17.93793532042042571, 1.500000000000414557 ) ) ;
#372=EDGE_CURVE ( 'NONE', #17843, #32661, #6158, .T. ) ;
#378=CARTESIAN_POINT ( 'NONE',  ( 107.6235316907398811, 18.91057310341854603, 4.414476567109417715 ) ) ;
#383=DIRECTION ( 'NONE',  ( -0.000000000000000000, -0.000000000000000000, -1.000000000000000000 ) ) ;
#384=DIRECTION ( 'NONE',  ( -1.000000000000000000, -0.000000000000000000, -0.000000000000000000 ) ) ;
#388=DIRECTION ( 'NONE',  ( 0.000000000000000000, -1.000000000000000000, 0.000000000000000000 ) ) ;
#398=CARTESIAN_POINT ( 'NONE',  ( -40.27879340802675756, -12.50360960397076582, 5.500000000000000000 ) ) ;
#399=EDGE_LOOP ( 'NONE', ( #18098, #32679, #22647, #21722 ) ) ;
#405=DIRECTION ( 'NONE',  ( -1.000000000000000000, 0.000000000000000000, -0.000000000000000000 ) ) ;
#410=CARTESIAN_POINT ( 'NONE',  ( -23.54713438637982748, 14.02568012664692532, 10.48023388603047579 ) ) ;
#420=( BOUNDED_CURVE ( )  B_SPLINE_CURVE ( 3, ( #13886, #28791, #15780, #3092 ),
 .UNSPECIFIED., .F., .F. ) 
 B_SPLINE_CURVE_WITH_KNOTS ( ( 4, 4 ),
 ( 4.530379766455337354, 4.712388980384688786 ),
 .UNSPECIFIED. ) 
 CURVE ( )  GEOMETRIC_REPRESENTATION_ITEM ( )  RATIONAL_B_SPLINE_CURVE ( ( 1.000000000000000000, 0.9972412918903135193, 0.9972412918903135193, 1.000000000000000000 ) ) 
 REPRESENTATION_ITEM ( '' )  );
#429=VERTEX_POINT ( 'NONE', #6803 ) ;
#436=VERTEX_POINT ( 'NONE', #29725 ) ;
#437=ORIENTED_EDGE ( 'NONE', *, *, #9373, .F. ) ;
#439=ORIENTED_EDGE ( 'NONE', *, *, #22087, .T. ) ;
#446=DIRECTION ( 'NONE',  ( 0.000000000000000000, -1.000000000000000000, 0.000000000000000000 ) ) ;
#450=DIRECTION ( 'NONE',  ( 0.000000000000000000, -0.000000000000000000, 1.000000000000000000 ) ) ;
#464=CARTESIAN_POINT ( 'NONE',  ( 107.9275968081481238, 17.77499038371485440, 4.627610784060872895 ) ) ;
#467=ORIENTED_EDGE ( 'NONE', *, *, #26078, .F. ) ;
#470=CARTESIAN_POINT ( 'NONE',  ( 8.911384905465473238, 0.4717275430040298034, -1.041239158277187160 ) ) ;
#473=CARTESIAN_POINT ( 'NONE',  ( -56.32770133515839461, 0.5000000000000000000, -1.500000000000000000 ) ) ;
#490=DIRECTION ( 'NONE',  ( 0.000000000000000000, 0.000000000000000000, -1.000000000000000000 ) ) ;
#494=ADVANCED_FACE ( 'NONE', ( #32059 ), #21714, .T. ) ;
#509=EDGE_LOOP ( 'NONE', ( #5695, #23872, #18382, #2587 ) ) ;
#522=CARTESIAN_POINT ( 'NONE',  ( 9.282537329959881234, 0.2172754300398732352, 1.050000000000000044 ) ) ;
#523=CARTESIAN_POINT ( 'NONE',  ( 12.40148790557316794, 21.49000000000003041, 1.500000000000000000 ) ) ;
#527=CARTESIAN_POINT ( 'NONE',  ( -30.13173294563779692, 12.12011656760094347, 1.929752697766440095 ) ) ;
#534=LINE ( 'NONE', #15760, #25821 ) ;
#536=VERTEX_POINT ( 'NONE', #30638 ) ;
#544=FACE_OUTER_BOUND ( 'NONE', #17814, .T. ) ;
#547=CARTESIAN_POINT ( 'NONE',  ( 0.000000000000000000, 0.5000000000000000000, 1.500000000000000000 ) ) ;
#575=AXIS2_PLACEMENT_3D ( 'NONE', #12635, #6949, #22840 ) ;
#578=CARTESIAN_POINT ( 'NONE',  ( 13.28835132608794467, 21.83091171094871541, -1.350227401154549201 ) ) ;
#582=CIRCLE ( 'NONE', #14406, 8.025310301077755781 ) ;
#584=CYLINDRICAL_SURFACE ( 'NONE', #24225, 0.5000000000000000000 ) ;
#601=DIRECTION ( 'NONE',  ( -0.000000000000000000, -0.3746065934159164001, 0.9271838545667856479 ) ) ;
#617=DIRECTION ( 'NONE',  ( 1.000000000000000000, 5.361488761196503499E-16, 0.000000000000000000 ) ) ;
#618=EDGE_CURVE ( 'NONE', #28100, #32600, #18353, .T. ) ;
#628=LINE ( 'NONE', #13792, #10850 ) ;
#630=AXIS2_PLACEMENT_3D ( 'NONE', #19998, #29844, #32868 ) ;
#646=CARTESIAN_POINT ( 'NONE',  ( 26.08945412691625165, 19.05746434167071612, -1.104107218669578838 ) ) ;
#671=DIRECTION ( 'NONE',  ( 0.4999999999999981126, 0.8660254037844395958, -0.000000000000000000 ) ) ;
#685=VERTEX_POINT ( 'NONE', #6019 ) ;
#696=DIRECTION ( 'NONE',  ( 0.000000000000000000, -0.9271838545667856479, -0.3746065934159165667 ) ) ;
#699=CARTESIAN_POINT ( 'NONE',  ( 10.13822877939487199, 2.318259723584965570, 1.500000000000000000 ) ) ;
#707=CIRCLE ( 'NONE', #23645, 12.49867430706168570 ) ;
#708=CIRCLE ( 'NONE', #24193, 10.97000000000000064 ) ;
#712=AXIS2_PLACEMENT_3D ( 'NONE', #24711, #32423, #22364 ) ;
#713=CARTESIAN_POINT ( 'NONE',  ( -22.68133094298037378, 3.998227953278250535, 2.146185852361514268 ) ) ;
#717=DIRECTION ( 'NONE',  ( 0.09975574163943258521, -0.1727820128662111709, 0.9798954883250903247 ) ) ;
#739=AXIS2_PLACEMENT_3D ( 'NONE', #29345, #19505, #16967 ) ;
#742=VECTOR ( 'NONE', #14344, 1000.000000000000114 ) ;
#745=CARTESIAN_POINT ( 'NONE',  ( 107.7872093323711340, 16.99325752433615122, 1.795912459692029950 ) ) ;
#760=ORIENTED_EDGE ( 'NONE', *, *, #21404, .F. ) ;
#764=CARTESIAN_POINT ( 'NONE',  ( 107.8403069886983161, 17.28892622638833032, 3.587457385742634841 ) ) ;
#765=CARTESIAN_POINT ( 'NONE',  ( 13.62547635268498780, 21.94000000000002970, -1.050000000000000044 ) ) ;
#769=CARTESIAN_POINT ( 'NONE',  ( 15.28872660057386845, 20.76088595412476678, -4.612695725900422872 ) ) ;
#774=EDGE_CURVE ( 'NONE', #4552, #3662, #6328, .T. ) ;
#788=DIRECTION ( 'NONE',  ( 0.4999999999999978906, 0.8660254037844398178, 0.000000000000000000 ) ) ;
#796=LINE ( 'NONE', #23831, #12832 ) ;
#797=DIRECTION ( 'NONE',  ( -8.326672684688674053E-17, -0.3746065934159164001, 0.9271838545667857590 ) ) ;
#812=CARTESIAN_POINT ( 'NONE',  ( 107.6454270328456602, 19.04591414929136306, 5.010299225411025681 ) ) ;
#818=DIRECTION ( 'NONE',  ( 1.000000000000000000, 1.369475477426763776E-16, -4.370874484540404848E-33 ) ) ;
#822=EDGE_CURVE ( 'NONE', #24398, #8881, #4333, .T. ) ;
#844=CARTESIAN_POINT ( 'NONE',  ( -58.24607230066835228, -3.627201876406635606, 5.444121653535032301 ) ) ;
#845=( BOUNDED_CURVE ( )  B_SPLINE_CURVE ( 3, ( #15367, #15720, #25573, #27743 ),
 .UNSPECIFIED., .F., .T. ) 
 B_SPLINE_CURVE_WITH_KNOTS ( ( 4, 4 ),
 ( 0.6009777071441372298, 1.570796326794896558 ),
 .UNSPECIFIED. ) 
 CURVE ( )  GEOMETRIC_REPRESENTATION_ITEM ( )  RATIONAL_B_SPLINE_CURVE ( ( 1.000000000000000000, 0.9231448173252677636, 0.9231448173252677636, 1.000000000000000000 ) ) 
 REPRESENTATION_ITEM ( '' )  );
#847=CARTESIAN_POINT ( 'NONE',  ( -61.24371088333262492, -10.96999999999998643, 1.500000000000000000 ) ) ;
#865=CARTESIAN_POINT ( 'NONE',  ( 24.72695737054825926, 18.91229966141139229, -1.500000000000000000 ) ) ;
#868=CARTESIAN_POINT ( 'NONE',  ( 13.86820176991295739, 7.731990000458505818, 1.500000000000000000 ) ) ;
#872=EDGE_LOOP ( 'NONE', ( #15387, #30686 ) ) ;
#877=CARTESIAN_POINT ( 'NONE',  ( -17.10362080823519904, 9.298459344128380266, 1.499999999999894529 ) ) ;
#878=CARTESIAN_POINT ( 'NONE',  ( 16.36487458112949511, 19.37645981759117575, 4.629213727441584325 ) ) ;
#893=ORIENTED_EDGE ( 'NONE', *, *, #25791, .T. ) ;
#896=EDGE_LOOP ( 'NONE', ( #4625, #17001, #16391, #439, #13609, #23483, #12341 ) ) ;
#902=CARTESIAN_POINT ( 'NONE',  ( 14.62799800222094326, 9.826424398192026288, -1.500000000000000000 ) ) ;
#903=CARTESIAN_POINT ( 'NONE',  ( -2.926117933286927375, 0.000000000000000000, -1.252246291852652682 ) ) ;
#934=ORIENTED_EDGE ( 'NONE', *, *, #229, .F. ) ;
#948=FACE_OUTER_BOUND ( 'NONE', #24455, .T. ) ;
#952=CARTESIAN_POINT ( 'NONE',  ( 108.0191169609971524, 18.28461070690599399, 4.532506661183012042 ) ) ;
#980=ORIENTED_EDGE ( 'NONE', *, *, #20628, .T. ) ;
#987=DIRECTION ( 'NONE',  ( 1.000000000000000000, 0.000000000000000000, -0.000000000000000000 ) ) ;
#989=CARTESIAN_POINT ( 'NONE',  ( -57.64511383230080810, -3.319689624912403048, 5.564001359196002916 ) ) ;
#995=EDGE_CURVE ( 'NONE', #6245, #17057, #9237, .T. ) ;
#1012=CARTESIAN_POINT ( 'NONE',  ( 9.547359219815096054, 1.400520851204822392, 1.500000000000000000 ) ) ;
#1017=ORIENTED_EDGE ( 'NONE', *, *, #11179, .F. ) ;
#1019=CARTESIAN_POINT ( 'NONE',  ( -29.35928501929439705, 7.719156497800170769, 2.044692901794244122 ) ) ;
#1023=CARTESIAN_POINT ( 'NONE',  ( -23.54713438637982748, 3.998227953278294944, 2.146185852361370383 ) ) ;
#1025=PLANE ( 'NONE',  #30600 ) ;
#1037=CARTESIAN_POINT ( 'NONE',  ( -57.40374817251313999, -2.616512360834426509, 5.949999999999999289 ) ) ;
#1038=ORIENTED_EDGE ( 'NONE', *, *, #29832, .T. ) ;
#1040=DIRECTION ( 'NONE',  ( 0.000000000000000000, 0.000000000000000000, -1.000000000000000000 ) ) ;
#1048=DIRECTION ( 'NONE',  ( 0.07581065956227724112, 0.4221436659004729197, 0.9033534575330094407 ) ) ;
#1053=ADVANCED_FACE ( 'NONE', ( #20714 ), #9096, .T. ) ;
#1069=CARTESIAN_POINT ( 'NONE',  ( 2.382865613620175349, 0.000000000000000000, 1.508259000770581615 ) ) ;
#1079=VERTEX_POINT ( 'NONE', #18857 ) ;
#1083=CARTESIAN_POINT ( 'NONE',  ( 11.04311965146447427, 15.00000000000002132, 1.508259000770581615 ) ) ;
#1086=DIRECTION ( 'NONE',  ( -0.4999999999999978906, -0.8660254037844399289, 0.000000000000000000 ) ) ;
#1097=CARTESIAN_POINT ( 'NONE',  ( -23.54713438637982748, 8.443947424854778561, 8.182767265444946148 ) ) ;
#1104=CARTESIAN_POINT ( 'NONE',  ( 108.1960732670207079, 19.26997324246909926, -4.614321361849296643 ) ) ;
#1112=AXIS2_PLACEMENT_3D ( 'NONE', #18340, #28543, #26030 ) ;
#1113=CARTESIAN_POINT ( 'NONE',  ( 108.1401284731860528, 18.95845055555492564, 5.012270609766838803 ) ) ;
#1150=ORIENTED_EDGE ( 'NONE', *, *, #13653, .F. ) ;
#1151=VECTOR ( 'NONE', #9511, 1000.000000000000000 ) ;
#1172=EDGE_CURVE ( 'NONE', #10298, #5929, #13617, .T. ) ;
#1181=AXIS2_PLACEMENT_3D ( 'NONE', #22571, #24901, #7342 ) ;
#1182=CARTESIAN_POINT ( 'NONE',  ( 14.99916604752485583, 9.584522669699346409, 1.050000000000000044 ) ) ;
#1185=CARTESIAN_POINT ( 'NONE',  ( -23.54713438637982748, 6.487496165429137207, 7.419273015635701185 ) ) ;
#1206=CIRCLE ( 'NONE', #5996, 0.4500000000000000111 ) ;
#1215=ORIENTED_EDGE ( 'NONE', *, *, #29793, .F. ) ;
#1216=DIRECTION ( 'NONE',  ( -0.000000000000000000, 0.000000000000000000, 1.000000000000000000 ) ) ;
#1224=CARTESIAN_POINT ( 'NONE',  ( 107.7536796087345294, 16.80655079293032017, 1.395761063491601783 ) ) ;
#1225=VERTEX_POINT ( 'NONE', #27681 ) ;
#1227=CARTESIAN_POINT ( 'NONE',  ( 15.90893862159966865, 10.93205754344057645, -1.500000000000296208 ) ) ;
#1233=ADVANCED_FACE ( 'NONE', ( #7292 ), #2295, .T. ) ;
#1237=AXIS2_PLACEMENT_3D ( 'NONE', #23594, #717, #31311 ) ;
#1243=DIRECTION ( 'NONE',  ( -0.000000000000000000, 0.000000000000000000, 1.000000000000000000 ) ) ;
#1254=CARTESIAN_POINT ( 'NONE',  ( 46.69789307159569347, 25.15383447853596621, -4.612695725900423760 ) ) ;
#1267=ORIENTED_EDGE ( 'NONE', *, *, #12098, .T. ) ;
#1269=CARTESIAN_POINT ( 'NONE',  ( -38.14293509397969473, 10.97000000000000419, -1.500000000000000000 ) ) ;
#1299=CARTESIAN_POINT ( 'NONE',  ( 9.149098621172166546, 18.06225657836807841, -4.612695725900421984 ) ) ;
#1301=CARTESIAN_POINT ( 'NONE',  ( -41.58734146630091999, -15.56207840271351728, 5.312698343317051375 ) ) ;
#1311=ORIENTED_EDGE ( 'NONE', *, *, #30645, .F. ) ;
#1326=DIRECTION ( 'NONE',  ( 1.000000000000000000, 0.000000000000000000, 0.000000000000000000 ) ) ;
#1331=CARTESIAN_POINT ( 'NONE',  ( -9.288857950784214168, 18.90773822806172433, 1.500000000000000222 ) ) ;
#1336=ORIENTED_EDGE ( 'NONE', *, *, #31481, .F. ) ;
#1344=CARTESIAN_POINT ( 'NONE',  ( 107.4385791398478602, 17.85938043952733878, -4.612695725900422872 ) ) ;
#1345=EDGE_CURVE ( 'NONE', #25797, #24410, #6056, .T. ) ;
#1350=ORIENTED_EDGE ( 'NONE', *, *, #10220, .T. ) ;
#1361=CARTESIAN_POINT ( 'NONE',  ( 107.7872089731491485, 16.99325552404635076, -1.779390171460584646 ) ) ;
#1370=CARTESIAN_POINT ( 'NONE',  ( -29.77647832281567020, 15.08866638674292027, 1.500000000000000000 ) ) ;
#1373=CARTESIAN_POINT ( 'NONE',  ( -54.10469650629801919, 5.263418255572274163, 1.500000000000000000 ) ) ;
#1374=CARTESIAN_POINT ( 'NONE',  ( 9.286398372032465431, 0.2229077781794372437, 1.044673861545039051 ) ) ;
#1389=EDGE_CURVE ( 'NONE', #29167, #30955, #26209, .T. ) ;
#1390=ORIENTED_EDGE ( 'NONE', *, *, #4252, .F. ) ;
#1394=FACE_OUTER_BOUND ( 'NONE', #1540, .T. ) ;
#1395=CARTESIAN_POINT ( 'NONE',  ( 9.031711214211194161, 0.01997115109544311817, -1.016156546702293051 ) ) ;
#1405=CARTESIAN_POINT ( 'NONE',  ( 56.97280603064898941, -277.2763395528616002, 1.500000000000000000 ) ) ;
#1409=EDGE_CURVE ( 'NONE', #21301, #32600, #13383, .T. ) ;
#1410=CARTESIAN_POINT ( 'NONE',  ( 107.4385791398478744, 17.85938043952739918, 4.629213727441585213 ) ) ;
#1418=VERTEX_POINT ( 'NONE', #10622 ) ;
#1427=ORIENTED_EDGE ( 'NONE', *, *, #13616, .T. ) ;
#1431=ORIENTED_EDGE ( 'NONE', *, *, #24002, .F. ) ;
#1453=ORIENTED_EDGE ( 'NONE', *, *, #16885, .F. ) ;
#1463=CARTESIAN_POINT ( 'NONE',  ( 19.67866930034583817, 15.15590071967975305, -1.050000000000000044 ) ) ;
#1483=ORIENTED_EDGE ( 'NONE', *, *, #21699, .T. ) ;
#1488=CARTESIAN_POINT ( 'NONE',  ( -59.75626822162179508, -5.804869634004071521, 5.128141679950119602 ) ) ;
#1493=CARTESIAN_POINT ( 'NONE',  ( 107.7530755790500621, 16.80318731729051152, -2.530619919563210640 ) ) ;
#1519=EDGE_CURVE ( 'NONE', #26215, #10113, #11605, .T. ) ;
#1522=CARTESIAN_POINT ( 'NONE',  ( -23.54713438637982748, 18.90773822806172433, 1.500000000000000000 ) ) ;
#1529=ORIENTED_EDGE ( 'NONE', *, *, #3176, .F. ) ;
#1535=CARTESIAN_POINT ( 'NONE',  ( -50.81000000000000227, -10.96999999999998643, 5.700000000000000178 ) ) ;
#1539=ORIENTED_EDGE ( 'NONE', *, *, #23640, .F. ) ;
#1540=EDGE_LOOP ( 'NONE', ( #14662, #16932, #13034, #23553 ) ) ;
#1577=LINE ( 'NONE', #29322, #27820 ) ;
#1589=FACE_OUTER_BOUND ( 'NONE', #23217, .T. ) ;
#1590=ADVANCED_FACE ( 'NONE', ( #21650 ), #24460, .T. ) ;
#1591=DIRECTION ( 'NONE',  ( -1.000000000000000000, 0.000000000000000000, 0.000000000000000000 ) ) ;
#1597=EDGE_CURVE ( 'NONE', #10281, #29127, #1577, .T. ) ;
#1599=CIRCLE ( 'NONE', #19206, 297.9387600756452912 ) ;
#1601=CYLINDRICAL_SURFACE ( 'NONE', #739, 0.4500000000000004552 ) ;
#1633=CARTESIAN_POINT ( 'NONE',  ( 26.08945412691628007, 19.05746434167072678, 1.082350151677544448 ) ) ;
#1641=ORIENTED_EDGE ( 'NONE', *, *, #15129, .F. ) ;
#1642=DIRECTION ( 'NONE',  ( -0.000000000000000000, -0.000000000000000000, -1.000000000000000000 ) ) ;
#1644=ADVANCED_FACE ( 'NONE', ( #19486 ), #23970, .T. ) ;
#1658=CIRCLE ( 'NONE', #32090, 9.425032312242976218 ) ;
#1661=ORIENTED_EDGE ( 'NONE', *, *, #372, .F. ) ;
#1677=CARTESIAN_POINT ( 'NONE',  ( 13.62547635268499135, 21.94000000000002970, 1.081074820185998320 ) ) ;
#1704=AXIS2_PLACEMENT_3D ( 'NONE', #2013, #27580, #19721 ) ;
#1717=CARTESIAN_POINT ( 'NONE',  ( 19.81525666554439269, 15.27091977432025338, -1.499999999999881428 ) ) ;
#1719=CARTESIAN_POINT ( 'NONE',  ( -3.064492245890347188, 0.000000000000000000, -1.000000000000000222 ) ) ;
#1723=CARTESIAN_POINT ( 'NONE',  ( 2.671540748214986660, 0.5000000000000006661, 1.500000000000000000 ) ) ;
#1724=CIRCLE ( 'NONE', #13519, 0.4499999999999999001 ) ;
#1726=LINE ( 'NONE', #4403, #8633 ) ;
#1741=CARTESIAN_POINT ( 'NONE',  ( -53.47134659355816666, 5.052751005448547161, 3.951405864347744323 ) ) ;
#1751=VECTOR ( 'NONE', #28095, 1000.000000000000000 ) ;
#1757=AXIS2_PLACEMENT_3D ( 'NONE', #15577, #25796, #24255 ) ;
#1759=ORIENTED_EDGE ( 'NONE', *, *, #29459, .T. ) ;
#1772=CARTESIAN_POINT ( 'NONE',  ( 10.43095328441111924, 21.14375246189590030, -1.491740999229418385 ) ) ;
#1782=VERTEX_POINT ( 'NONE', #5366 ) ;
#1783=CIRCLE ( 'NONE', #12992, 0.4500000000000017875 ) ;
#1788=FACE_OUTER_BOUND ( 'NONE', #20620, .T. ) ;
#1799=EDGE_CURVE ( 'NONE', #15924, #27103, #20883, .T. ) ;
#1800=EDGE_LOOP ( 'NONE', ( #30781, #31477, #20672, #13523 ) ) ;
#1802=CARTESIAN_POINT ( 'NONE',  ( 10.49234587624072290, 2.036894776009066987, -1.050000000000000044 ) ) ;
#1806=LINE ( 'NONE', #32733, #32147 ) ;
#1813=AXIS2_PLACEMENT_3D ( 'NONE', #13429, #5274, #23649 ) ;
#1828=CARTESIAN_POINT ( 'NONE',  ( -24.00194742982113638, 3.998227953278373992, 2.146185852361368607 ) ) ;
#1832=ORIENTED_EDGE ( 'NONE', *, *, #14959, .F. ) ;
#1844=ORIENTED_EDGE ( 'NONE', *, *, #26197, .F. ) ;
#1870=CARTESIAN_POINT ( 'NONE',  ( 107.3934790618724406, 17.60822615140890335, 4.091707453491133961 ) ) ;
#1877=EDGE_CURVE ( 'NONE', #5412, #4370, #16219, .T. ) ;
#1894=ORIENTED_EDGE ( 'NONE', *, *, #31040, .F. ) ;
#1910=DIRECTION ( 'NONE',  ( 1.000000000000000000, 0.000000000000000000, 0.000000000000000000 ) ) ;
#1921=( BOUNDED_CURVE ( )  B_SPLINE_CURVE ( 3, ( #9458, #9808, #2117, #12297 ),
 .UNSPECIFIED., .F., .F. ) 
 B_SPLINE_CURVE_WITH_KNOTS ( ( 4, 4 ),
 ( 3.141592653589800221, 3.761815862121093090 ),
 .UNSPECIFIED. ) 
 CURVE ( )  GEOMETRIC_REPRESENTATION_ITEM ( )  RATIONAL_B_SPLINE_CURVE ( ( 1.000000000000000000, 0.9681996787398556847, 0.9681996787398556847, 1.000000000000000000 ) ) 
 REPRESENTATION_ITEM ( '' )  );
#1935=CARTESIAN_POINT ( 'NONE',  ( -83.35439080561378944, -0.0003384977252891612984, 1.500000000000000000 ) ) ;
#1938=CARTESIAN_POINT ( 'NONE',  ( -56.35387370928786765, 0.005482903227124292372, -1.004960936152643702 ) ) ;
#1949=CARTESIAN_POINT ( 'NONE',  ( -23.54713438637982748, 10.71031731502107576, 2.573304945315896042 ) ) ;
#1956=CARTESIAN_POINT ( 'NONE',  ( 107.1769020805352142, 16.40214705320008903, -1.491740999229418829 ) ) ;
#1957=CYLINDRICAL_SURFACE ( 'NONE', #17789, 0.5000000000000000000 ) ;
#1981=DIRECTION ( 'NONE',  ( 0.000000000000000000, 0.000000000000000000, -1.000000000000000000 ) ) ;
#1982=DIRECTION ( 'NONE',  ( 0.000000000000000000, 0.000000000000000000, 1.000000000000000000 ) ) ;
#2000=CARTESIAN_POINT ( 'NONE',  ( -56.29198263848482497, 0.01337210975256776860, -1.132057944610920686 ) ) ;
#2009=CARTESIAN_POINT ( 'NONE',  ( 107.5415233712214871, 18.44887242198213073, 5.148260821734984560 ) ) ;
#2013=CARTESIAN_POINT ( 'NONE',  ( 56.97280603064898941, -277.2763395528616002, -4.612695725900422872 ) ) ;
#2037=FACE_OUTER_BOUND ( 'NONE', #13424, .T. ) ;
#2044=CARTESIAN_POINT ( 'NONE',  ( -2.794738735352966685, 0.000000000000000000, -1.491740999229417941 ) ) ;
#2057=CARTESIAN_POINT ( 'NONE',  ( -42.85764933975779201, 24.74387538314362800, -1.050000000000000044 ) ) ;
#2059=CARTESIAN_POINT ( 'NONE',  ( 107.6876980308802985, 19.28759250760272437, -4.757993698474195732 ) ) ;
#2067=ADVANCED_FACE ( 'NONE', ( #27903 ), #30598, .T. ) ;
#2068=PRODUCT_DEFINITION ( 'UNKNOWN', '', #3447, #11579 ) ;
#2069=DIRECTION ( 'NONE',  ( 0.000000000000000000, 0.000000000000000000, -1.000000000000000000 ) ) ;
#2072=DIRECTION ( 'NONE',  ( -1.000000000000000000, 0.000000000000000000, -0.000000000000000000 ) ) ;
#2089=DIRECTION ( 'NONE',  ( 1.000000000000000000, 0.000000000000000000, 0.000000000000000000 ) ) ;
#2092=DIRECTION ( 'NONE',  ( 0.000000000000000000, 0.000000000000000000, 1.000000000000000000 ) ) ;
#2095=( BOUNDED_SURFACE ( )  B_SPLINE_SURFACE ( 3, 2, ( 
 ( #24591, #9721, #4394 ),
 ( #14739, #19262, #19947 ),
 ( #22271, #6874, #32642 ),
 ( #1395, #9224, #27462 ),
 ( #27617, #12076, #12222 ),
 ( #14232, #22426, #30155 ) ),
 .UNSPECIFIED., .F., .F., .F. ) 
 B_SPLINE_SURFACE_WITH_KNOTS ( ( 4, 2, 4 ),
 ( 3, 3 ),
 ( 6.884163014324140129, 7.369072324149311015, 7.853981633974482790 ),
 ( 0.000000000000000000, 1.000000000000000000 ),
 .UNSPECIFIED. ) 
 GEOMETRIC_REPRESENTATION_ITEM ( )  RATIONAL_B_SPLINE_SURFACE ( (
 ( 1.000000000000000000, 0.8123215895924605912, 1.000000000000000000),
 ( 1.000000000000000000, 0.8591172521900167780, 1.000000000000000000),
 ( 1.000000000000000000, 0.9088222585364039707, 1.000000000000000000),
 ( 1.000000000000000000, 0.9794174349135039703, 1.000000000000000000),
 ( 1.000000000000000000, 1.000375673120272202, 1.000000000000000000),
 ( 1.000000000000000000, 1.000000000000000000, 1.000000000000000000) ) ) 
 REPRESENTATION_ITEM ( '' )  SURFACE ( )  );
#2096=CARTESIAN_POINT ( 'NONE',  ( -38.14293509397969473, 10.97000000000000419, -1.050000000000000044 ) ) ;
#2104=DIRECTION ( 'NONE',  ( 1.000000000000000000, 0.000000000000000000, 0.000000000000000000 ) ) ;
#2110=ORIENTED_EDGE ( 'NONE', *, *, #22872, .T. ) ;
#2116=CARTESIAN_POINT ( 'NONE',  ( 9.288464280921653327, 0.2259206803923255180, -1.047120714225419524 ) ) ;
#2117=CARTESIAN_POINT ( 'NONE',  ( -56.78550605763575732, 0.5559970271814609344, 1.681829461946841908 ) ) ;
#2129=VECTOR ( 'NONE', #29857, 1000.000000000000000 ) ;
#2132=CARTESIAN_POINT ( 'NONE',  ( -56.30179757781805705, 0.05506136597571936742, -1.235259460217722483 ) ) ;
#2133=DIRECTION ( 'NONE',  ( -1.000000000000000000, -5.361488761196502513E-16, 0.000000000000000000 ) ) ;
#2135=ORIENTED_EDGE ( 'NONE', *, *, #2417, .T. ) ;
#2157=VERTEX_POINT ( 'NONE', #23373 ) ;
#2170=VERTEX_POINT ( 'NONE', #25905 ) ;
#2175=DIRECTION ( 'NONE',  ( 1.000000000000000000, 0.000000000000000000, 0.000000000000000000 ) ) ;
#2176=CARTESIAN_POINT ( 'NONE',  ( -22.61376412419456727, 18.90773822806010429, 1.500000000000000000 ) ) ;
#2178=CARTESIAN_POINT ( 'NONE',  ( -29.27706164892578045, 7.575660699118165198, 1.500000000003544498 ) ) ;
#2192=CARTESIAN_POINT ( 'NONE',  ( 107.9275968081481523, 17.77499038371486151, -4.611092782519706113 ) ) ;
#2200=AXIS2_PLACEMENT_3D ( 'NONE', #31856, #21490, #19303 ) ;
#2201=DIRECTION ( 'NONE',  ( -1.000000000000000000, 0.000000000000000000, 0.000000000000000000 ) ) ;
#2206=CARTESIAN_POINT ( 'NONE',  ( 21.09752163284169768, 16.24116300003629121, -1.500000000000059508 ) ) ;
#2210=CARTESIAN_POINT ( 'NONE',  ( 9.187365643239731483, 0.07845480144325879535, 1.031721989605144829 ) ) ;
#2213=ORIENTED_EDGE ( 'NONE', *, *, #4011, .F. ) ;
#2215=CIRCLE ( 'NONE', #9128, 10.52000000000000135 ) ;
#2216=CARTESIAN_POINT ( 'NONE',  ( -60.31029867951531998, -5.485000000000008313, 1.500000000000000222 ) ) ;
#2222=ORIENTED_EDGE ( 'NONE', *, *, #29350, .T. ) ;
#2233=CARTESIAN_POINT ( 'NONE',  ( -41.30970132048468457, -16.45499999999997343, 0.000000000000000000 ) ) ;
#2234=APPLICATION_CONTEXT ( 'configuration controlled 3d designs of mechanical parts and assemblies' ) ;
#2240=EDGE_CURVE ( 'NONE', #4740, #32685, #18913, .T. ) ;
#2241=ORIENTED_EDGE ( 'NONE', *, *, #2988, .T. ) ;
#2242=VECTOR ( 'NONE', #818, 1000.000000000000000 ) ;
#2243=VECTOR ( 'NONE', #23041, 1000.000000000000000 ) ;
#2244=CARTESIAN_POINT ( 'NONE',  ( -41.54586029198078023, -15.55146752323317116, 5.221982333014083544 ) ) ;
#2247=DIRECTION ( 'NONE',  ( 0.000000000000000000, 0.000000000000000000, -1.000000000000000000 ) ) ;
#2256=CARTESIAN_POINT ( 'NONE',  ( -56.56234538287964142, 0.08413247787389122045, -1.028003236817250698 ) ) ;
#2266=AXIS2_PLACEMENT_3D ( 'NONE', #30921, #28399, #7685 ) ;
#2279=ADVANCED_FACE ( 'NONE', ( #17156 ), #23675, .T. ) ;
#2280=DIRECTION ( 'NONE',  ( 1.000000000000000000, 0.000000000000000000, 0.000000000000000000 ) ) ;
#2287=ORIENTED_EDGE ( 'NONE', *, *, #5697, .T. ) ;
#2289=VECTOR ( 'NONE', #15237, 1000.000000000000000 ) ;
#2294=ORIENTED_EDGE ( 'NONE', *, *, #12893, .T. ) ;
#2295=CYLINDRICAL_SURFACE ( 'NONE', #575, 0.4500000000000025646 ) ;
#2304=VECTOR ( 'NONE', #24685, 1000.000000000000000 ) ;
#2308=CARTESIAN_POINT ( 'NONE',  ( -31.06438740200783855, 3.643637926576053676, 8.172925694146080389 ) ) ;
#2315=CIRCLE ( 'NONE', #22061, 297.9387600756452912 ) ;
#2318=CARTESIAN_POINT ( 'NONE',  ( -56.76591339919558976, 0.3588337185217547742, -1.487708500135610290 ) ) ;
#2361=VERTEX_POINT ( 'NONE', #6798 ) ;
#2362=CIRCLE ( 'NONE', #9272, 0.4500000000000033418 ) ;
#2364=CARTESIAN_POINT ( 'NONE',  ( 13.23555367686087259, 7.539807145823324674, 1.500000000000000222 ) ) ;
#2372=CARTESIAN_POINT ( 'NONE',  ( -56.28351068137280322, 0.4500000000000000111, -1.000000000000000000 ) ) ;
#2382=CARTESIAN_POINT ( 'NONE',  ( 107.4617478720205099, 17.99143216401991197, -4.844664824704018713 ) ) ;
#2387=ORIENTED_EDGE ( 'NONE', *, *, #14627, .T. ) ;
#2393=ORIENTED_EDGE ( 'NONE', *, *, #13040, .T. ) ;
#2394=CARTESIAN_POINT ( 'NONE',  ( 19.81525666539894459, 15.27091977451247828, -1.050000000000000044 ) ) ;
#2410=FACE_OUTER_BOUND ( 'NONE', #22658, .T. ) ;
#2417=EDGE_CURVE ( 'NONE', #15974, #4298, #4790, .T. ) ;
#2427=ORIENTED_EDGE ( 'NONE', *, *, #267, .F. ) ;
#2445=CARTESIAN_POINT ( 'NONE',  ( 8.930755659325141593, 0.5000000000000008882, 1.500000000000000000 ) ) ;
#2455=EDGE_LOOP ( 'NONE', ( #980, #31284, #17475, #11594, #15851, #9299 ) ) ;
#2475=ORIENTED_EDGE ( 'NONE', *, *, #21718, .F. ) ;
#2478=CARTESIAN_POINT ( 'NONE',  ( 48.53640747082131668, 22.19355195243385026, -1.491740999229419273 ) ) ;
#2481=ADVANCED_FACE ( 'NONE', ( #15470 ), #25304, .T. ) ;
#2484=CARTESIAN_POINT ( 'NONE',  ( -56.69688924229027549, 0.2251703961848605107, -1.041696575785743484 ) ) ;
#2536=CARTESIAN_POINT ( 'NONE',  ( 108.1401923855166842, 18.95880644471085574, -4.995517669168206609 ) ) ;
#2538=CARTESIAN_POINT ( 'NONE',  ( -23.54713438637982748, 18.46223496596754288, 1.773004750130224627 ) ) ;
#2550=CARTESIAN_POINT ( 'NONE',  ( -50.81000000000000227, -10.96999999999998643, 5.700000000000000178 ) ) ;
#2561=CARTESIAN_POINT ( 'NONE',  ( -29.02642725384296440, 4.820254766716771222, 1.500000000000000000 ) ) ;
#2567=ORIENTED_EDGE ( 'NONE', *, *, #4723, .F. ) ;
#2587=ORIENTED_EDGE ( 'NONE', *, *, #29459, .F. ) ;
#2588=CARTESIAN_POINT ( 'NONE',  ( -56.33578448492038859, 0.003046479527604620090, -1.000000000000000000 ) ) ;
#2606=EDGE_LOOP ( 'NONE', ( #7983, #20682, #100 ) ) ;
#2610=VERTEX_POINT ( 'NONE', #20831 ) ;
#2623=DIRECTION ( 'NONE',  ( 0.000000000000000000, -0.9271838545667854259, -0.3746065934159166777 ) ) ;
#2640=ORIENTED_EDGE ( 'NONE', *, *, #15320, .T. ) ;
#2645=ORIENTED_EDGE ( 'NONE', *, *, #22972, .T. ) ;
#2648=LINE ( 'NONE', #15985, #2242 ) ;
#2655=CARTESIAN_POINT ( 'NONE',  ( -1.176310634206514104E-14, 21.94000000000002260, 1.050000000000000044 ) ) ;
#2673=EDGE_CURVE ( 'NONE', #22357, #17959, #30504, .T. ) ;
#2679=CARTESIAN_POINT ( 'NONE',  ( -23.54713438637982748, 3.998227953278294944, 2.146185852361370383 ) ) ;
#2687=CIRCLE ( 'NONE', #12280, 9.425032312242976218 ) ;
#2693=CARTESIAN_POINT ( 'NONE',  ( 108.0068349480237657, 18.21621961241920218, -4.398253369385427547 ) ) ;
#2694=ORIENTED_EDGE ( 'NONE', *, *, #26513, .F. ) ;
#2698=ORIENTED_EDGE ( 'NONE', *, *, #18975, .F. ) ;
#2705=CARTESIAN_POINT ( 'NONE',  ( 26.08945412691624099, 19.05746434167065928, 1.500000000000000000 ) ) ;
#2706=DIRECTION ( 'NONE',  ( -1.000000000000000000, 0.000000000000000000, 0.000000000000000000 ) ) ;
#2717=DIRECTION ( 'NONE',  ( -0.000000000000000000, -0.000000000000000000, -1.000000000000000000 ) ) ;
#2722=CARTESIAN_POINT ( 'NONE',  ( -56.49561586466536056, 0.04964621674521208644, 1.500000000000000000 ) ) ;
#2733=VECTOR ( 'NONE', #6259, 1000.000000000000000 ) ;
#2755=CARTESIAN_POINT ( 'NONE',  ( -0.6528202993443400493, 0.000000000000000000, -5.396302277755718357 ) ) ;
#2759=CARTESIAN_POINT ( 'NONE',  ( 107.9622325421415212, 20.81773585569407459, 1.508259000770582059 ) ) ;
#2766=( BOUNDED_SURFACE ( )  B_SPLINE_SURFACE ( 3, 2, ( 
 ( #23356, #464, #28374 ),
 ( #9988, #17862, #5490 ),
 ( #145, #28060, #25702 ),
 ( #17670, #5156, #15331 ),
 ( #7318, #12808, #17509 ),
 ( #10643, #25383, #12660 ),
 ( #25536, #18020, #22863 ),
 ( #318, #23023, #10331 ),
 ( #13156, #20546, #30754 ),
 ( #7827, #15488, #20704 ),
 ( #30904, #1113, #812 ),
 ( #16157, #13954, #15833 ),
 ( #3630, #31388, #10988 ),
 ( #3308, #26531, #6138 ) ),
 .UNSPECIFIED., .F., .F., .T. ) 
 B_SPLINE_SURFACE_WITH_KNOTS ( ( 4, 2, 2, 2, 2, 2, 4 ),
 ( 3, 3 ),
 ( 2.385244779468109755E-18, 0.0002022272781459603930, 0.0003033409172189393968, 0.0004044545562919184007, 0.0005055681953648974046, 0.0006066818344378764084, 0.0008089091125838344162 ),
 ( 0.000000000000000000, 1.000000000000000000 ),
 .UNSPECIFIED. ) 
 GEOMETRIC_REPRESENTATION_ITEM ( )  RATIONAL_B_SPLINE_SURFACE ( (
 ( 1.000000000000000000, 0.7097644798780626818, 1.000000000000000000),
 ( 1.000000000000000000, 0.7096080128847354063, 1.000000000000000000),
 ( 1.000000000000000000, 0.7093877859246700002, 1.000000000000000000),
 ( 1.000000000000000000, 0.7087837316534446597, 1.000000000000000000),
 ( 1.000000000000000000, 0.7085305059914599468, 1.000000000000000000),
 ( 1.000000000000000000, 0.7078957402609113991, 1.000000000000000000),
 ( 1.000000000000000000, 0.7075010273771544789, 1.000000000000000000),
 ( 1.000000000000000000, 0.7067064543823278200, 1.000000000000000000),
 ( 1.000000000000000000, 0.7063134043005300233, 1.000000000000000000),
 ( 1.000000000000000000, 0.7056801599291154803, 1.000000000000000000),
 ( 1.000000000000000000, 0.7054276077845391679, 1.000000000000000000),
 ( 1.000000000000000000, 0.7048252423529660637, 1.000000000000000000),
 ( 1.000000000000000000, 0.7046023681409566697, 1.000000000000000000),
 ( 1.000000000000000000, 0.7044453589051569153, 1.000000000000000000) ) ) 
 REPRESENTATION_ITEM ( '' )  SURFACE ( )  );
#2768=CARTESIAN_POINT ( 'NONE',  ( -38.14293509397970183, 21.94000000000000128, -1.050000000000000044 ) ) ;
#2769=CIRCLE ( 'NONE', #3315, 0.4499999999999990119 ) ;
#2778=AXIS2_PLACEMENT_3D ( 'NONE', #20332, #32893, #7629 ) ;
#2783=EDGE_LOOP ( 'NONE', ( #9441, #19399, #7823, #17093 ) ) ;
#2791=VECTOR ( 'NONE', #12402, 1000.000000000000000 ) ;
#2798=CARTESIAN_POINT ( 'NONE',  ( -42.85764933975779201, 24.74387538314362800, 1.500000000000000000 ) ) ;
#2800=DIRECTION ( 'NONE',  ( 1.000000000000000000, 0.000000000000000000, 0.000000000000000000 ) ) ;
#2808=CARTESIAN_POINT ( 'NONE',  ( -23.54713438637982748, 3.094594691910233841, 6.506829104297265687 ) ) ;
#2814=CARTESIAN_POINT ( 'NONE',  ( -50.81000000000000227, -10.96999999999998643, 0.000000000000000000 ) ) ;
#2815=CARTESIAN_POINT ( 'NONE',  ( -56.41635936944848595, 0.01859738704150220093, -1.012721741759385230 ) ) ;
#2816=UNCERTAINTY_MEASURE_WITH_UNIT (LENGTH_MEASURE( 1.000000000000000082E-05 ), #25162, 'distance_accuracy_value', 'NONE');
#2818=VERTEX_POINT ( 'NONE', #33014 ) ;
#2827=AXIS2_PLACEMENT_3D ( 'NONE', #11334, #8826, #19180 ) ;
#2854=CARTESIAN_POINT ( 'NONE',  ( -50.81000000000000227, -10.96999999999998643, 9.000000000000000000 ) ) ;
#2857=CARTESIAN_POINT ( 'NONE',  ( 108.2963982961846199, 19.82862259121970183, -2.249089808652653399 ) ) ;
#2860=CARTESIAN_POINT ( 'NONE',  ( -41.86373177837819526, -16.13513036599590222, 5.128141679950119602 ) ) ;
#2865=AXIS2_PLACEMENT_3D ( 'NONE', #14796, #7619, #2104 ) ;
#2876=DIRECTION ( 'NONE',  ( -1.000000000000000000, 0.000000000000000000, 0.000000000000000000 ) ) ;
#2888=ORIENTED_EDGE ( 'NONE', *, *, #16398, .F. ) ;
#2889=EDGE_CURVE ( 'NONE', #13391, #8881, #22661, .T. ) ;
#2892=CARTESIAN_POINT ( 'NONE',  ( -17.54156717296799783, 14.33342533202398705, 1.873879510985751118 ) ) ;
#2903=VECTOR ( 'NONE', #11574, 1000.000000000000227 ) ;
#2905=CARTESIAN_POINT ( 'NONE',  ( 25.25107927536528507, 18.67207037203893094, 1.499999999999350075 ) ) ;
#2912=CARTESIAN_POINT ( 'NONE',  ( 0.6708088701982989344, 0.000000000000000000, 4.629213727441584325 ) ) ;
#2914=CARTESIAN_POINT ( 'NONE',  ( -23.77648227443687290, 18.46223496596753577, 1.773004750130224627 ) ) ;
#2926=VECTOR ( 'NONE', #12888, 1000.000000000000114 ) ;
#2939=LINE ( 'NONE', #547, #28823 ) ;
#2942=LINE ( 'NONE', #33007, #26755 ) ;
#2977=ORIENTED_EDGE ( 'NONE', *, *, #28566, .T. ) ;
#2983=CARTESIAN_POINT ( 'NONE',  ( 12.16606561763909156, 4.796759898857955839, 1.050000000000000266 ) ) ;
#2988=EDGE_CURVE ( 'NONE', #10930, #1782, #15785, .T. ) ;
#3001=ORIENTED_EDGE ( 'NONE', *, *, #30795, .T. ) ;
#3008=( BOUNDED_CURVE ( )  B_SPLINE_CURVE ( 3, ( #22851, #25523, #7646, #30232 ),
 .UNSPECIFIED., .F., .F. ) 
 B_SPLINE_CURVE_WITH_KNOTS ( ( 4, 4 ),
 ( 4.712388980384689674, 6.457718232379018097 ),
 .UNSPECIFIED. ) 
 CURVE ( )  GEOMETRIC_REPRESENTATION_ITEM ( )  RATIONAL_B_SPLINE_CURVE ( ( 1.000000000000000000, 0.7618584064576930936, 0.7618584064576930936, 1.000000000000000000 ) ) 
 REPRESENTATION_ITEM ( '' )  );
#3020=CARTESIAN_POINT ( 'NONE',  ( 9.282537329959909655, 0.2172754300399158400, -1.041239158277187160 ) ) ;
#3023=CARTESIAN_POINT ( 'NONE',  ( -53.95513674679793326, 5.522463357794191730, 1.050000000000049116 ) ) ;
#3031=CARTESIAN_POINT ( 'NONE',  ( -0.2059365608663963898, 0.000000000000000000, 1.000000000000000000 ) ) ;
#3037=ADVANCED_FACE ( 'NONE', ( #8267 ), #31792, .T. ) ;
#3043=CARTESIAN_POINT ( 'NONE',  ( -17.72558274912641352, 7.737767392030566072, 2.044195425586785575 ) ) ;
#3048=EDGE_CURVE ( 'NONE', #21704, #31255, #23452, .T. ) ;
#3055=CARTESIAN_POINT ( 'NONE',  ( 10.43095328441111924, 21.14375246189590030, 1.508259000770582059 ) ) ;
#3065=CARTESIAN_POINT ( 'NONE',  ( -27.17337974022411373, 17.29073355517597221, 1.801206419975863504 ) ) ;
#3072=DIRECTION ( 'NONE',  ( 0.4809547266710044178, 0.000000000000000000, 0.8767454310646958238 ) ) ;
#3085=DIRECTION ( 'NONE',  ( 1.000000000000000000, 0.000000000000000000, 0.000000000000000000 ) ) ;
#3087=EDGE_LOOP ( 'NONE', ( #31399, #11921, #26994, #23042, #9489, #893, #6213, #18000, #28377 ) ) ;
#3092=CARTESIAN_POINT ( 'NONE',  ( -2.506063600758156262, 0.4999999999999998890, -1.500000000000000000 ) ) ;
#3094=ORIENTED_EDGE ( 'NONE', *, *, #7936, .F. ) ;
#3097=CARTESIAN_POINT ( 'NONE',  ( -30.19127229040104865, 4.968489494181039134, 5.500000000000000000 ) ) ;
#3107=EDGE_LOOP ( 'NONE', ( #12674, #26991, #18510, #12080 ) ) ;
#3111=ORIENTED_EDGE ( 'NONE', *, *, #3176, .T. ) ;
#3129=CARTESIAN_POINT ( 'NONE',  ( 13.78505948480717436, 7.589837197045443240, 1.050000000000000044 ) ) ;
#3136=PLANE ( 'NONE',  #19811 ) ;
#3161=CARTESIAN_POINT ( 'NONE',  ( 25.69812813987159217, 19.01643737707301085, -1.364233426705607322 ) ) ;
#3163=CARTESIAN_POINT ( 'NONE',  ( 108.3358876115613896, 20.04851468097726652, -1.779919050530493152 ) ) ;
#3164=EDGE_LOOP ( 'NONE', ( #16853, #8105, #31208, #7752, #8675 ) ) ;
#3176=EDGE_CURVE ( 'NONE', #11755, #3662, #20113, .T. ) ;
#3181=CARTESIAN_POINT ( 'NONE',  ( -57.12917293608614955, -2.964366234459024696, 5.871858320049880398 ) ) ;
#3200=VERTEX_POINT ( 'NONE', #20922 ) ;
#3201=LINE ( 'NONE', #2705, #2289 ) ;
#3202=CARTESIAN_POINT ( 'NONE',  ( 19.03564543755645033, 14.58476759517576404, 1.050000000000000044 ) ) ;
#3207=EDGE_LOOP ( 'NONE', ( #17401, #1431, #1390, #30988 ) ) ;
#3210=CARTESIAN_POINT ( 'NONE',  ( -24.45920507959942469, 18.39788475725609374, 1.774545360836604191 ) ) ;
#3214=CARTESIAN_POINT ( 'NONE',  ( 15.55254023221931448, 20.42149909151575216, 5.412820279296878923 ) ) ;
#3215=CARTESIAN_POINT ( 'NONE',  ( 15.28872660057389155, 20.76088595412472415, 4.629213727441584325 ) ) ;
#3218=AXIS2_PLACEMENT_3D ( 'NONE', #31470, #1040, #28643 ) ;
#3239=CARTESIAN_POINT ( 'NONE',  ( 107.9166483397147687, 17.71402499141862208, 3.339827141515659292 ) ) ;
#3247=DIRECTION ( 'NONE',  ( 0.000000000000000000, 0.000000000000000000, 1.000000000000000000 ) ) ;
#3256=LINE ( 'NONE', #18616, #4436 ) ;
#3257=EDGE_CURVE ( 'NONE', #18014, #22155, #21100, .T. ) ;
#3269=EDGE_CURVE ( 'NONE', #3747, #19054, #16038, .T. ) ;
#3280=DIRECTION ( 'NONE',  ( -0.1327696077594705815, 0.9911469271785068313, 0.000000000000000000 ) ) ;
#3283=CARTESIAN_POINT ( 'NONE',  ( 14.90130905634548952, 9.429294031743246762, 1.050000000000000044 ) ) ;
#3288=VECTOR ( 'NONE', #5424, 1000.000000000000000 ) ;
#3308=CARTESIAN_POINT ( 'NONE',  ( 108.1156589233281267, 18.82219444680281484, 4.414476567109669958 ) ) ;
#3315=AXIS2_PLACEMENT_3D ( 'NONE', #19026, #16177, #21055 ) ;
#3320=AXIS2_PLACEMENT_3D ( 'NONE', #2044, #30151, #7046 ) ;
#3325=CARTESIAN_POINT ( 'NONE',  ( 8.917260909444884476, 0.3029815364085644558, 1.471149382586864895 ) ) ;
#3333=VECTOR ( 'NONE', #17046, 1000.000000000000000 ) ;
#3338=AXIS2_PLACEMENT_3D ( 'NONE', #8701, #18240, #29108 ) ;
#3353=CARTESIAN_POINT ( 'NONE',  ( -59.04079763661544433, -4.690551911666260843, 5.310642798857019287 ) ) ;
#3355=CARTESIAN_POINT ( 'NONE',  ( -47.25352234179201361, 16.22999999999998266, -1.050000000000000044 ) ) ;
#3359=AXIS2_PLACEMENT_3D ( 'NONE', #12499, #1982, #22707 ) ;
#3365=AXIS2_PLACEMENT_3D ( 'NONE', #29577, #11512, #18694 ) ;
#3372=CARTESIAN_POINT ( 'NONE',  ( -23.54713438637982748, 8.275374457817616047, 8.599999999999999645 ) ) ;
#3377=CARTESIAN_POINT ( 'NONE',  ( 16.02030197382709176, 11.87192001622980264, -1.500000000000000222 ) ) ;
#3380=CARTESIAN_POINT ( 'NONE',  ( 13.48007872897105841, 7.959851041527245208, 1.500000000000000000 ) ) ;
#3383=EDGE_CURVE ( 'NONE', #11370, #11079, #9469, .T. ) ;
#3386=ADVANCED_FACE ( 'NONE', ( #29566 ), #18168, .F. ) ;
#3388=CIRCLE ( 'NONE', #12984, 0.4500000000000025646 ) ;
#3393=CARTESIAN_POINT ( 'NONE',  ( -17.31779044994511807, 7.339147416616279784, 1.500000000000000000 ) ) ;
#3399=CARTESIAN_POINT ( 'NONE',  ( 9.300899703876350344, 0.2440751071713773424, 1.049978936837301369 ) ) ;
#3404=CARTESIAN_POINT ( 'NONE',  ( 108.1156589233279135, 18.82219444680288234, -4.397958565568440115 ) ) ;
#3410=CARTESIAN_POINT ( 'NONE',  ( -32.42885140446504977, -0.0003384977252881313063, 1.500000000000000000 ) ) ;
#3412=CARTESIAN_POINT ( 'NONE',  ( 108.0946594595236689, 20.79497418261435016, -1.491968323836175836 ) ) ;
#3422=EDGE_LOOP ( 'NONE', ( #1336, #9888, #30047, #31410, #29574, #25023 ) ) ;
#3423=CARTESIAN_POINT ( 'NONE',  ( 9.924500721901809541, 1.154815372706009535, -1.050000000000000044 ) ) ;
#3431=CARTESIAN_POINT ( 'NONE',  ( 107.6235316907398243, 18.91057310341846787, -4.397958565568440115 ) ) ;
#3435=ORIENTED_EDGE ( 'NONE', *, *, #30694, .T. ) ;
#3446=CARTESIAN_POINT ( 'NONE',  ( 110.2274383572228942, 17.36892446252421962, -4.612695725900422872 ) ) ;
#3447=PRODUCT_DEFINITION_FORMATION_WITH_SPECIFIED_SOURCE ( 'ANY', '', #32741, .NOT_KNOWN. ) ;
#3456=ORIENTED_EDGE ( 'NONE', *, *, #30110, .T. ) ;
#3469=DIRECTION ( 'NONE',  ( -1.000000000000000000, 0.000000000000000000, 0.000000000000000000 ) ) ;
#3484=EDGE_CURVE ( 'NONE', #7787, #17721, #27690, .T. ) ;
#3487=CARTESIAN_POINT ( 'NONE',  ( 15.55254023221933046, 20.42149909151570597, -5.396302277755718357 ) ) ;
#3490=EDGE_LOOP ( 'NONE', ( #467, #13667, #10919, #26507 ) ) ;
#3505=CARTESIAN_POINT ( 'NONE',  ( 24.97738509828242925, 18.93945643846228677, -1.491740999229418829 ) ) ;
#3510=CARTESIAN_POINT ( 'NONE',  ( 108.3190031596522260, 19.95449539046050447, 1.997040456489197036 ) ) ;
#3512=ORIENTED_EDGE ( 'NONE', *, *, #14084, .F. ) ;
#3513=ORIENTED_EDGE ( 'NONE', *, *, #32952, .F. ) ;
#3522=CARTESIAN_POINT ( 'NONE',  ( -58.35079223774033608, -4.003636301679985188, 5.522895031407148103 ) ) ;
#3541=CARTESIAN_POINT ( 'NONE',  ( 11.68041589746584208, 4.858256445636988552, -1.499999999999999778 ) ) ;
#3544=CARTESIAN_POINT ( 'NONE',  ( 21.51801198777054935, 16.55905037250783352, 1.050000000000117284 ) ) ;
#3552=CARTESIAN_POINT ( 'NONE',  ( -18.25325501504504189, 6.775292334730776744, 2.070007460140761868 ) ) ;
#3564=ADVANCED_FACE ( 'NONE', ( #18006 ), #28193, .F. ) ;
#3566=ORIENTED_EDGE ( 'NONE', *, *, #346, .F. ) ;
#3574=CARTESIAN_POINT ( 'NONE',  ( 107.9617357165269595, 17.96508929613819916, 3.877315172376031960 ) ) ;
#3575=ORIENTED_EDGE ( 'NONE', *, *, #9562, .T. ) ;
#3576=CARTESIAN_POINT ( 'NONE',  ( 15.22955465171501999, 10.73977884020718854, -1.500000000000000000 ) ) ;
#3580=CARTESIAN_POINT ( 'NONE',  ( -50.81000000000000227, -10.96999999999998643, 8.628141679950115162 ) ) ;
#3582=DIRECTION ( 'NONE',  ( -0.000000000000000000, -0.3746065934159164001, 0.9271838545667856479 ) ) ;
#3594=ORIENTED_EDGE ( 'NONE', *, *, #244, .F. ) ;
#3595=DIRECTION ( 'NONE',  ( -0.000000000000000000, -0.000000000000000000, -1.000000000000000000 ) ) ;
#3597=ADVANCED_FACE ( 'NONE', ( #23677 ), #31227, .T. ) ;
#3603=CARTESIAN_POINT ( 'NONE',  ( 0.6708088701982988233, 0.000000000000000000, 4.629213727441584325 ) ) ;
#3619=FACE_OUTER_BOUND ( 'NONE', #22284, .T. ) ;
#3625=CARTESIAN_POINT ( 'NONE',  ( 108.1156589233279419, 18.82219444680297116, 4.414476567109417715 ) ) ;
#3629=EDGE_CURVE ( 'NONE', #31255, #25309, #796, .T. ) ;
#3630=CARTESIAN_POINT ( 'NONE',  ( 108.1105447920915594, 18.79371694613778843, 4.475313644716053751 ) ) ;
#3636=EDGE_CURVE ( 'NONE', #7325, #6067, #8021, .T. ) ;
#3658=CARTESIAN_POINT ( 'NONE',  ( -56.71071518287084245, 0.7496615022747109558, -1.050000000000000044 ) ) ;
#3662=VERTEX_POINT ( 'NONE', #22646 ) ;
#3667=DIRECTION ( 'NONE',  ( 0.8660254037844409281, -0.4999999999999960587, 0.000000000000000000 ) ) ;
#3675=ADVANCED_FACE ( 'NONE', ( #10249 ), #17924, .F. ) ;
#3678=FACE_OUTER_BOUND ( 'NONE', #399, .T. ) ;
#3691=CARTESIAN_POINT ( 'NONE',  ( 11.28219953675240994, 4.179024087153581313, 1.500000000000000000 ) ) ;
#3696=CARTESIAN_POINT ( 'NONE',  ( -41.30970132048468457, -16.45499999999997343, 1.500000000000000000 ) ) ;
#3703=CARTESIAN_POINT ( 'NONE',  ( 9.284416849710916964, 0.2200169608700019708, 1.043104428712757326 ) ) ;
#3706=B_SPLINE_CURVE_WITH_KNOTS ( 'NONE', 3,
 ( #11653, #22201, #16994, #29728, #11822, #6806, #16844, #14481, #26884, #14311, #1633, #12003 ),
 .UNSPECIFIED., .F., .F.,
 ( 4, 2, 2, 2, 2, 4 ),
 ( 3.496446946337351263E-18, 0.0007549536553621100056, 0.001132430483043158232, 0.001321168896883682942, 0.001415538103803949633, 0.001509907310724215891 ),
 .UNSPECIFIED. ) ;
#3709=CARTESIAN_POINT ( 'NONE',  ( -40.61087657765956038, -10.96999999999998643, 5.871858320049875957 ) ) ;
#3723=CARTESIAN_POINT ( 'NONE',  ( 14.33714415250651797, 9.363647757017387718, -1.500000000000000000 ) ) ;
#3733=DIRECTION ( 'NONE',  ( 0.000000000000000000, -0.9271838545667856479, -0.3746065934159162891 ) ) ;
#3741=CARTESIAN_POINT ( 'NONE',  ( 8.901867736793462882, 0.07845480144340738482, -1.317219896051736505 ) ) ;
#3744=FACE_OUTER_BOUND ( 'NONE', #13307, .T. ) ;
#3745=EDGE_LOOP ( 'NONE', ( #15810, #6831, #9396, #4234, #28439 ) ) ;
#3746=DIRECTION ( 'NONE',  ( 0.8660254037844399289, -0.4999999999999977796, 0.000000000000000000 ) ) ;
#3747=VERTEX_POINT ( 'NONE', #5088 ) ;
#3771=CARTESIAN_POINT ( 'NONE',  ( 14.23800746264082839, 22.11259878822725966, -1.491740999229417941 ) ) ;
#3773=EDGE_CURVE ( 'NONE', #15394, #6161, #18593, .T. ) ;
#3774=CONICAL_SURFACE ( 'NONE', #21380, 2.524999999999999911, 0.7853981633974627119 ) ;
#3780=CARTESIAN_POINT ( 'NONE',  ( 108.0375372059708212, 18.38718189920101764, 4.618926104085890216 ) ) ;
#3787=CARTESIAN_POINT ( 'NONE',  ( -41.71978369837230360, -15.85293847936788580, 5.221339267391799766 ) ) ;
#3788=EDGE_LOOP ( 'NONE', ( #25671, #5889, #8770, #4793 ) ) ;
#3793=AXIS2_PLACEMENT_3D ( 'NONE', #26516, #14124, #6266 ) ;
#3794=ORIENTED_EDGE ( 'NONE', *, *, #28410, .F. ) ;
#3803=CARTESIAN_POINT ( 'NONE',  ( 9.578960313758919654, 17.92714876365089793, 5.412820279296879811 ) ) ;
#3815=CYLINDRICAL_SURFACE ( 'NONE', #25303, 0.5000000000000004441 ) ;
#3822=EDGE_CURVE ( 'NONE', #4740, #436, #28312, .T. ) ;
#3832=DIRECTION ( 'NONE',  ( 0.000000000000000000, -0.9271838545667856479, -0.3746065934159165667 ) ) ;
#3833=CARTESIAN_POINT ( 'NONE',  ( -60.07995281065674931, -10.96999999999998465, 9.000000000000000000 ) ) ;
#3836=CARTESIAN_POINT ( 'NONE',  ( -59.75626822162180218, -5.804869634004078627, 5.128141679950119602 ) ) ;
#3837=AXIS2_PLACEMENT_3D ( 'NONE', #29860, #14798, #7285 ) ;
#3846=ADVANCED_FACE ( 'NONE', ( #544 ), #16116, .T. ) ;
#3847=ORIENTED_EDGE ( 'NONE', *, *, #6395, .T. ) ;
#3848=CIRCLE ( 'NONE', #106, 10.52000000000000135 ) ;
#3856=ORIENTED_EDGE ( 'NONE', *, *, #6396, .T. ) ;
#3867=DIRECTION ( 'NONE',  ( 0.1503837331804358246, -0.08682408883346498518, -0.9848077530122080203 ) ) ;
#3887=EDGE_LOOP ( 'NONE', ( #8734, #7038, #5437, #23306, #4 ) ) ;
#3898=ORIENTED_EDGE ( 'NONE', *, *, #15879, .T. ) ;
#3900=CARTESIAN_POINT ( 'NONE',  ( 19.01933586171005786, 14.56926017569804443, -1.050000000000000044 ) ) ;
#3928=CARTESIAN_POINT ( 'NONE',  ( 78.59573142019985426, 24.17918843217023550, -5.396302277755718357 ) ) ;
#3937=CYLINDRICAL_SURFACE ( 'NONE', #19187, 0.4500000000000025646 ) ;
#3943=CARTESIAN_POINT ( 'NONE',  ( 17.41559371906258136, 18.02474698348859050, 1.508259000770581615 ) ) ;
#3963=CARTESIAN_POINT ( 'NONE',  ( 108.0120074800398982, 18.24502231166869493, 4.476406828366910950 ) ) ;
#3968=CYLINDRICAL_SURFACE ( 'NONE', #15666, 0.4499999999999999001 ) ;
#3971=ORIENTED_EDGE ( 'NONE', *, *, #26513, .T. ) ;
#3985=CARTESIAN_POINT ( 'NONE',  ( 13.41780342409107973, 19.07609913100965571, 4.629213727441584325 ) ) ;
#3986=EDGE_CURVE ( 'NONE', #21393, #24740, #26220, .T. ) ;
#4005=CARTESIAN_POINT ( 'NONE',  ( -59.01620623031298152, -4.767884042047559667, 5.493143919433970623 ) ) ;
#4010=CARTESIAN_POINT ( 'NONE',  ( 107.9195515681658435, 17.73019131299352935, -3.358191939550565497 ) ) ;
#4011=EDGE_CURVE ( 'NONE', #19054, #32515, #12331, .T. ) ;
#4032=CARTESIAN_POINT ( 'NONE',  ( 13.17780055412413454, 21.79273496866543169, 1.386556541278284094 ) ) ;
#4037=CARTESIAN_POINT ( 'NONE',  ( -17.64511778006428599, 14.89308641508515585, 1.500000000000212719 ) ) ;
#4052=EDGE_LOOP ( 'NONE', ( #15808, #6055, #10166, #4353, #14565, #15838 ) ) ;
#4055=( BOUNDED_SURFACE ( )  B_SPLINE_SURFACE ( 3, 2, ( 
 ( #1410, #6580, #13421 ),
 ( #23641, #764, #10946 ),
 ( #21147, #31347, #18617 ),
 ( #28812, #5907, #16100 ) ),
 .UNSPECIFIED., .F., .F., .F. ) 
 B_SPLINE_SURFACE_WITH_KNOTS ( ( 4, 4 ),
 ( 3, 3 ),
 ( 0.000000000000000000, 0.003454001599076465465 ),
 ( 0.000000000000000000, 1.000000000000000000 ),
 .UNSPECIFIED. ) 
 GEOMETRIC_REPRESENTATION_ITEM ( )  RATIONAL_B_SPLINE_SURFACE ( (
 ( 1.000000000000000000, 0.7097644798780626818, 1.000000000000000000),
 ( 1.000000000000000000, 0.7097691176663369905, 1.000000000000000000),
 ( 1.000000000000000000, 0.7097737773069662248, 1.000000000000000000),
 ( 1.000000000000000000, 0.7097784590644244940, 1.000000000000000000) ) ) 
 REPRESENTATION_ITEM ( '' )  SURFACE ( )  );
#4062=CARTESIAN_POINT ( 'NONE',  ( -23.54713438637982748, 8.275374457817619600, 8.600000000000004974 ) ) ;
#4063=CARTESIAN_POINT ( 'NONE',  ( -30.51827900900859447, 4.402097243136374516, 5.049999999999999822 ) ) ;
#4065=CARTESIAN_POINT ( 'NONE',  ( 11.83739209453320740, 5.126178544244889501, -1.500000000000000000 ) ) ;
#4081=DIRECTION ( 'NONE',  ( 0.000000000000000000, -0.9205048534524477022, 0.3907311284892561742 ) ) ;
#4084=EDGE_CURVE ( 'NONE', #9305, #29668, #1658, .T. ) ;
#4085=CARTESIAN_POINT ( 'NONE',  ( 79.17573959169237696, 22.98125563777605151, -4.612695725900423760 ) ) ;
#4096=ADVANCED_FACE ( 'NONE', ( #2037 ), #12209, .T. ) ;
#4111=DIRECTION ( 'NONE',  ( -5.361488761196502513E-16, 1.000000000000000000, 0.000000000000000000 ) ) ;
#4118=CARTESIAN_POINT ( 'NONE',  ( 107.3033141393571981, 17.10611366274323331, -3.000076723692274960 ) ) ;
#4122=ORIENTED_EDGE ( 'NONE', *, *, #15321, .F. ) ;
#4133=CARTESIAN_POINT ( 'NONE',  ( 9.149098621172166546, 18.06225657836807841, 4.629213727441584325 ) ) ;
#4134=EDGE_LOOP ( 'NONE', ( #7495, #6868, #25711, #27032 ) ) ;
#4140=ORIENTED_EDGE ( 'NONE', *, *, #10311, .F. ) ;
#4143=CARTESIAN_POINT ( 'NONE',  ( -1.082681991931091492, 0.000000000000000000, 4.629213727441584325 ) ) ;
#4159=FACE_OUTER_BOUND ( 'NONE', #13084, .T. ) ;
#4172=CARTESIAN_POINT ( 'NONE',  ( 9.513442983150083521, 1.350987762931694647, -1.500000000000000444 ) ) ;
#4173=EDGE_LOOP ( 'NONE', ( #25861, #16720, #14284, #32183, #6832, #15793, #30963, #10003, #21188, #31609, #14023, #6192, #5159, #7832, #13280, #32765 ) ) ;
#4179=CARTESIAN_POINT ( 'NONE',  ( 13.62547635268498780, 21.94000000000002970, 1.050000000000000044 ) ) ;
#4188=DIRECTION ( 'NONE',  ( 1.000000000000000000, 0.000000000000000000, 0.000000000000000000 ) ) ;
#4199=CARTESIAN_POINT ( 'NONE',  ( -53.55623634834322644, 5.485000000000006537, 1.500000000000000888 ) ) ;
#4202=ORIENTED_EDGE ( 'NONE', *, *, #20906, .F. ) ;
#4208=VERTEX_POINT ( 'NONE', #22258 ) ;
#4210=FACE_OUTER_BOUND ( 'NONE', #27037, .T. ) ;
#4229=CARTESIAN_POINT ( 'NONE',  ( -61.68687437218811453, -10.96999999999998643, 2.028141679950118625 ) ) ;
#4234=ORIENTED_EDGE ( 'NONE', *, *, #21044, .F. ) ;
#4241=ORIENTED_EDGE ( 'NONE', *, *, #19595, .T. ) ;
#4245=DIRECTION ( 'NONE',  ( 0.000000000000000000, -0.000000000000000000, 1.000000000000000000 ) ) ;
#4247=CARTESIAN_POINT ( 'NONE',  ( -28.64263641446437347, 5.485000000000014531, 1.500000000000000000 ) ) ;
#4252=EDGE_CURVE ( 'NONE', #31255, #1418, #11788, .T. ) ;
#4274=ORIENTED_EDGE ( 'NONE', *, *, #6708, .T. ) ;
#4286=CARTESIAN_POINT ( 'NONE',  ( 9.909835366851556415, 1.133397303054362037, -1.050000000000000266 ) ) ;
#4298=VERTEX_POINT ( 'NONE', #13194 ) ;
#4304=DIRECTION ( 'NONE',  ( -1.000000000000000000, 0.000000000000000000, 0.000000000000000000 ) ) ;
#4306=VECTOR ( 'NONE', #22189, 1000.000000000000000 ) ;
#4313=CARTESIAN_POINT ( 'NONE',  ( -29.97923030674312983, 9.414801368908669588, 1.999766382938328313 ) ) ;
#4333=LINE ( 'NONE', #21568, #11230 ) ;
#4347=EDGE_CURVE ( 'NONE', #8185, #17721, #5948, .T. ) ;
#4353=ORIENTED_EDGE ( 'NONE', *, *, #3773, .T. ) ;
#4370=VERTEX_POINT ( 'NONE', #29092 ) ;
#4377=VECTOR ( 'NONE', #25290, 1000.000000000000227 ) ;
#4378=DIRECTION ( 'NONE',  ( -0.8476835837759374437, 0.5305021600302710638, 0.000000000000000000 ) ) ;
#4381=DIRECTION ( 'NONE',  ( 0.000000000000000000, -1.000000000000000000, 0.000000000000000000 ) ) ;
#4393=CARTESIAN_POINT ( 'NONE',  ( 23.60846595399739911, 18.33789664323239421, -1.500000000000000000 ) ) ;
#4394=CARTESIAN_POINT ( 'NONE',  ( 8.911384905465460804, 0.2172754300401000538, -1.412391582771750365 ) ) ;
#4396=CARTESIAN_POINT ( 'NONE',  ( 9.282537329959909655, 0.2172754300399125094, 1.041239158277188048 ) ) ;
#4400=CARTESIAN_POINT ( 'NONE',  ( 2.382865613620174905, -1.226387906749791482E-16, 1.292893218813452982 ) ) ;
#4403=CARTESIAN_POINT ( 'NONE',  ( -38.14293509397970183, 21.94000000000000128, 1.500000000000000000 ) ) ;
#4406=AXIS2_PLACEMENT_3D ( 'NONE', #23165, #87, #10093 ) ;
#4408=CIRCLE ( 'NONE', #27878, 0.05000000000000143219 ) ;
#4413=CIRCLE ( 'NONE', #2827, 10.95101833074431852 ) ;
#4417=LINE ( 'NONE', #14249, #25818 ) ;
#4430=FACE_OUTER_BOUND ( 'NONE', #15913, .T. ) ;
#4432=ORIENTED_EDGE ( 'NONE', *, *, #25378, .F. ) ;
#4436=VECTOR ( 'NONE', #13117, 1000.000000000000000 ) ;
#4438=DIRECTION ( 'NONE',  ( 0.000000000000000000, 1.000000000000000000, 0.000000000000000000 ) ) ;
#4441=CARTESIAN_POINT ( 'NONE',  ( -56.61120226097368402, 0.1221716369093696630, -1.032972126671726221 ) ) ;
#4456=CIRCLE ( 'NONE', #12989, 10.19912342234043834 ) ;
#4460=VECTOR ( 'NONE', #32921, 1000.000000000000000 ) ;
#4461=CIRCLE ( 'NONE', #23145, 6.035938585833444670 ) ;
#4480=CARTESIAN_POINT ( 'NONE',  ( -41.30970132048468457, -16.45499999999997343, 1.500000000000000000 ) ) ;
#4484=CARTESIAN_POINT ( 'NONE',  ( 8.900602013106571064, 0.09531162291654332597, 1.304562659182832540 ) ) ;
#4489=CARTESIAN_POINT ( 'NONE',  ( 107.6901625442183672, 19.30163305711951338, -4.728018791096159745 ) ) ;
#4532=CARTESIAN_POINT ( 'NONE',  ( 13.61462910219950473, 21.93664948940024928, 1.110678092886302260 ) ) ;
#4538=CARTESIAN_POINT ( 'NONE',  ( -20.19984785985500508, 17.54567542505805733, 1.795026885182644749 ) ) ;
#4539=CARTESIAN_POINT ( 'NONE',  ( -30.01044711289841516, 13.10789634492816447, 1.904575337205761887 ) ) ;
#4548=AXIS2_PLACEMENT_3D ( 'NONE', #22580, #32300, #12193 ) ;
#4549=CARTESIAN_POINT ( 'NONE',  ( 13.62547635268498780, 21.94000000000002970, 1.050000000000000044 ) ) ;
#4552=VERTEX_POINT ( 'NONE', #31032 ) ;
#4561=DIRECTION ( 'NONE',  ( 0.9563911903463306885, -1.156482317317869713E-14, 0.2920888409849449752 ) ) ;
#4563=CARTESIAN_POINT ( 'NONE',  ( 22.43659417819815616, 17.13630711803212492, -1.050000000000000044 ) ) ;
#4573=CARTESIAN_POINT ( 'NONE',  ( 108.2840637929627832, 19.75993920996065967, -3.567582149746106435 ) ) ;
#4576=ORIENTED_EDGE ( 'NONE', *, *, #4084, .T. ) ;
#4585=LINE ( 'NONE', #1741, #23682 ) ;
#4612=ADVANCED_FACE ( 'NONE', ( #30542 ), #13279, .T. ) ;
#4617=CARTESIAN_POINT ( 'NONE',  ( 16.36487458112951643, 19.37645981759113667, -4.612695725900422872 ) ) ;
#4625=ORIENTED_EDGE ( 'NONE', *, *, #28956, .F. ) ;
#4627=ORIENTED_EDGE ( 'NONE', *, *, #3383, .T. ) ;
#4629=CARTESIAN_POINT ( 'NONE',  ( 9.295274190224857236, 0.2358592590667328848, -1.049999640971083892 ) ) ;
#4642=EDGE_CURVE ( 'NONE', #18387, #25095, #2215, .T. ) ;
#4645=CARTESIAN_POINT ( 'NONE',  ( -56.44230307511855216, 0.02673048711865717159, -1.015476362562965251 ) ) ;
#4657=ORIENTED_EDGE ( 'NONE', *, *, #3484, .T. ) ;
#4685=DIRECTION ( 'NONE',  ( -0.9164966213036979115, 0.4000424266736042900, 0.000000000000000000 ) ) ;
#4690=CARTESIAN_POINT ( 'NONE',  ( -16.41799616858202171, 10.20678673897635313, 1.500000000000000000 ) ) ;
#4691=CARTESIAN_POINT ( 'NONE',  ( -30.67627260417763679, 10.20678673897636912, 1.500000000000000000 ) ) ;
#4699=DIRECTION ( 'NONE',  ( 0.000000000000000000, 1.000000000000000000, 0.000000000000000000 ) ) ;
#4707=CARTESIAN_POINT ( 'NONE',  ( 108.0435829116943438, 18.42084677419104821, -5.131407418483624028 ) ) ;
#4711=VERTEX_POINT ( 'NONE', #20478 ) ;
#4723=EDGE_CURVE ( 'NONE', #15974, #14650, #2942, .T. ) ;
#4728=PLANE ( 'NONE',  #10264 ) ;
#4730=FACE_OUTER_BOUND ( 'NONE', #14846, .T. ) ;
#4736=EDGE_CURVE ( 'NONE', #7787, #14600, #8072, .T. ) ;
#4740=VERTEX_POINT ( 'NONE', #30845 ) ;
#4744=ORIENTED_EDGE ( 'NONE', *, *, #25298, .T. ) ;
#4758=ADVANCED_FACE ( 'NONE', ( #23142 ), #29435, .T. ) ;
#4759=CARTESIAN_POINT ( 'NONE',  ( 14.23800746264080885, 22.11259878822730229, -1.491740999229417941 ) ) ;
#4762=FACE_OUTER_BOUND ( 'NONE', #25079, .T. ) ;
#4772=CARTESIAN_POINT ( 'NONE',  ( -53.45715098423449518, 5.485000000000009202, 1.500000000000000000 ) ) ;
#4790=LINE ( 'NONE', #27536, #23700 ) ;
#4793=ORIENTED_EDGE ( 'NONE', *, *, #3822, .T. ) ;
#4800=CARTESIAN_POINT ( 'NONE',  ( -56.77795429543039774, 0.4641589773180558320, -1.049999627028684879 ) ) ;
#4808=VECTOR ( 'NONE', #8412, 1000.000000000000227 ) ;
#4843=AXIS2_PLACEMENT_3D ( 'NONE', #8037, #10397, #5562 ) ;
#4847=CARTESIAN_POINT ( 'NONE',  ( -24.38478530838886371, 4.195786794270493836, 1.500000000001213474 ) ) ;
#4857=EDGE_CURVE ( 'NONE', #10930, #15521, #14475, .T. ) ;
#4861=CARTESIAN_POINT ( 'NONE',  ( 108.0732742559233515, 18.58617989449696140, -4.624430632823066212 ) ) ;
#4863=CARTESIAN_POINT ( 'NONE',  ( -17.11836807087407664, 9.444159879341990305, 1.999016699742306891 ) ) ;
#4875=VECTOR ( 'NONE', #9633, 1000.000000000000227 ) ;
#4878=ORIENTED_EDGE ( 'NONE', *, *, #13433, .T. ) ;
#4880=VECTOR ( 'NONE', #16871, 1000.000000000000000 ) ;
#4896=DIRECTION ( 'NONE',  ( -1.000000000000000000, 0.000000000000000000, 0.000000000000000000 ) ) ;
#4909=CARTESIAN_POINT ( 'NONE',  ( 108.0068349480237515, 18.21621961241920573, -4.398253369385427547 ) ) ;
#4912=VECTOR ( 'NONE', #28066, 1000.000000000000000 ) ;
#4916=LINE ( 'NONE', #14408, #18792 ) ;
#4917=FACE_OUTER_BOUND ( 'NONE', #24499, .T. ) ;
#4924=PLANE ( 'NONE',  #30084 ) ;
#4949=VECTOR ( 'NONE', #671, 1000.000000000000227 ) ;
#4954=DIRECTION ( 'NONE',  ( -0.1327696077594705815, 0.9911469271785068313, 0.000000000000000000 ) ) ;
#4961=VECTOR ( 'NONE', #5817, 1000.000000000000000 ) ;
#4966=AXIS2_PLACEMENT_3D ( 'NONE', #32471, #27606, #4381 ) ;
#4970=VERTEX_POINT ( 'NONE', #31815 ) ;
#4973=B_SPLINE_CURVE_WITH_KNOTS ( 'NONE', 3,
 ( #18038, #21357, #15514, #13503, #5982, #28576, #7845, #23716, #2857, #26061, #3163, #337, #20722 ),
 .UNSPECIFIED., .F., .F.,
 ( 4, 3, 3, 3, 4 ),
 ( 8.673617379884034509E-19, 0.0008924055619933561265, 0.001784811123946879966, 0.002677216685860944918, 0.003343752506362699349 ),
 .UNSPECIFIED. ) ;
#4981=DIRECTION ( 'NONE',  ( 0.000000000000000000, -0.9271838545667856479, -0.3746065934159162891 ) ) ;
#4988=CARTESIAN_POINT ( 'NONE',  ( -56.69596708151924247, 0.1891862907730448851, -1.417079347435143966 ) ) ;
#5032=CARTESIAN_POINT ( 'NONE',  ( 13.41780342409107973, 19.07609913100965571, -4.612695725900421984 ) ) ;
#5036=CARTESIAN_POINT ( 'NONE',  ( -25.27811764180047760, 4.185543752813269514, 2.140960162089065033 ) ) ;
#5039=CARTESIAN_POINT ( 'NONE',  ( -2.794738735352966685, 0.000000000000000000, 1.508259000770582059 ) ) ;
#5050=CARTESIAN_POINT ( 'NONE',  ( -22.63903668291242610, 18.41081583916481534, 1.774234584568461726 ) ) ;
#5058=CYLINDRICAL_SURFACE ( 'NONE', #29935, 0.4500000000000025646 ) ;
#5066=EDGE_LOOP ( 'NONE', ( #20249, #27638, #30882, #1150, #9852, #7439, #12246 ) ) ;
#5088=CARTESIAN_POINT ( 'NONE',  ( -47.25352234179201361, 16.22999999999998266, 1.500000000000000000 ) ) ;
#5104=CARTESIAN_POINT ( 'NONE',  ( 77.65715268217998357, 26.11770293189133341, -1.491740999229417941 ) ) ;
#5115=ORIENTED_EDGE ( 'NONE', *, *, #29562, .T. ) ;
#5120=CARTESIAN_POINT ( 'NONE',  ( 13.62547635268498780, 21.94000000000002970, -1.050000000000000044 ) ) ;
#5156=CARTESIAN_POINT ( 'NONE',  ( 107.9828061044025418, 18.08241752981144046, 5.008628968642859114 ) ) ;
#5159=ORIENTED_EDGE ( 'NONE', *, *, #25102, .F. ) ;
#5177=CARTESIAN_POINT ( 'NONE',  ( -41.25971018530405843, -14.96514855415592216, 5.309652167554829383 ) ) ;
#5188=CARTESIAN_POINT ( 'NONE',  ( -29.77647832281393647, 7.339147416615578123, 1.500000000000000000 ) ) ;
#5192=CARTESIAN_POINT ( 'NONE',  ( -56.33578448492038859, 0.003046479527604620090, 0.000000000000000000 ) ) ;
#5199=CARTESIAN_POINT ( 'NONE',  ( 107.6331050892701739, 18.97529836792814706, -5.039948469649382368 ) ) ;
#5209=CARTESIAN_POINT ( 'NONE',  ( -42.46793790805479318, 24.51887538314362658, 1.050000000000000044 ) ) ;
#5211=CARTESIAN_POINT ( 'NONE',  ( 11.90652295052632503, 20.12228623747235901, 4.629213727441584325 ) ) ;
#5224=FACE_OUTER_BOUND ( 'NONE', #20476, .T. ) ;
#5245=CARTESIAN_POINT ( 'NONE',  ( -40.27879340802675046, -12.50360960397076404, 5.949999999999999289 ) ) ;
#5247=CYLINDRICAL_SURFACE ( 'NONE', #26778, 0.5000000000000000000 ) ;
#5259=CARTESIAN_POINT ( 'NONE',  ( 107.6996442589674103, 19.35565155597529596, 4.629213727441584325 ) ) ;
#5274=DIRECTION ( 'NONE',  ( -0.000000000000000000, -0.000000000000000000, 1.000000000000000000 ) ) ;
#5289=CARTESIAN_POINT ( 'NONE',  ( 21.39187852382935517, 16.47248925749085302, 1.050000000000000044 ) ) ;
#5296=CARTESIAN_POINT ( 'NONE',  ( -50.81000000000000227, -10.96999999999998643, 9.000000000000000000 ) ) ;
#5302=CARTESIAN_POINT ( 'NONE',  ( -56.77373628060693278, 0.4264188904495926913, -1.049552654929835072 ) ) ;
#5321=EDGE_CURVE ( 'NONE', #30095, #10281, #25548, .T. ) ;
#5333=CARTESIAN_POINT ( 'NONE',  ( -59.75626822162180218, -5.804869634004078627, 5.128141679950119602 ) ) ;
#5336=FACE_OUTER_BOUND ( 'NONE', #26738, .T. ) ;
#5338=CARTESIAN_POINT ( 'NONE',  ( -53.72801162551947840, 5.497307881342318403, 1.430198536305348656 ) ) ;
#5340=ORIENTED_EDGE ( 'NONE', *, *, #27574, .T. ) ;
#5359=CARTESIAN_POINT ( 'NONE',  ( 107.9372220951237011, 17.82858777955670249, -4.726288973428885321 ) ) ;
#5361=CARTESIAN_POINT ( 'NONE',  ( -16.95666531389092313, 12.15481017292670884, 1.928847951723336784 ) ) ;
#5365=ORIENTED_EDGE ( 'NONE', *, *, #20622, .T. ) ;
#5366=CARTESIAN_POINT ( 'NONE',  ( -30.51827900900860158, 4.402097243136374516, 5.500000000000000000 ) ) ;
#5372=FACE_BOUND ( 'NONE', #23120, .T. ) ;
#5373=CARTESIAN_POINT ( 'NONE',  ( 24.28956136216245199, 18.19040579244978773, 1.050000000000177458 ) ) ;
#5382=CIRCLE ( 'NONE', #21381, 2.099999999999990319 ) ;
#5388=CYLINDRICAL_SURFACE ( 'NONE', #1757, 0.5000000000000004441 ) ;
#5404=AXIS2_PLACEMENT_3D ( 'NONE', #25371, #14667, #12153 ) ;
#5406=CARTESIAN_POINT ( 'NONE',  ( -40.82392219421588209, -13.09203557865092371, 5.845255965757442773 ) ) ;
#5412=VERTEX_POINT ( 'NONE', #6639 ) ;
#5415=DIRECTION ( 'NONE',  ( 0.000000000000000000, 0.000000000000000000, 1.000000000000000000 ) ) ;
#5416=CARTESIAN_POINT ( 'NONE',  ( -41.77414131929176477, -16.18685544166627821, 1.949999999999999734 ) ) ;
#5419=CARTESIAN_POINT ( 'NONE',  ( -32.18774808610336180, -0.0003384977252905707612, 3.357274007152141415 ) ) ;
#5423=AXIS2_PLACEMENT_3D ( 'NONE', #14783, #20000, #24981 ) ;
#5424=DIRECTION ( 'NONE',  ( -1.000000000000000000, 0.000000000000000000, 0.000000000000000000 ) ) ;
#5428=CIRCLE ( 'NONE', #11834, 0.4999999999999988898 ) ;
#5437=ORIENTED_EDGE ( 'NONE', *, *, #14246, .F. ) ;
#5461=ORIENTED_EDGE ( 'NONE', *, *, #4857, .F. ) ;
#5474=B_SPLINE_CURVE_WITH_KNOTS ( 'NONE', 3,
 ( #31407, #15854, #21361, #3510, #16185, #26409, #21544, #18384, #5673, #13665, #23869, #26064, #11156 ),
 .UNSPECIFIED., .F., .F.,
 ( 4, 3, 3, 3, 4 ),
 ( 0.000000000000000000, 0.0006665428069513527464, 0.001558946041704377004, 0.002451349276496870774, 0.003343752511328988881 ),
 .UNSPECIFIED. ) ;
#5490=CARTESIAN_POINT ( 'NONE',  ( 107.4480426597792047, 17.91330156492432124, 4.744522527009380042 ) ) ;
#5492=CARTESIAN_POINT ( 'NONE',  ( -23.54713438637982748, 2.832830518764033911, 5.958029102616976935 ) ) ;
#5495=ORIENTED_EDGE ( 'NONE', *, *, #14666, .T. ) ;
#5497=ADVANCED_FACE ( 'NONE', ( #26687 ), #16623, .T. ) ;
#5503=EDGE_CURVE ( 'NONE', #20196, #24740, #1806, .T. ) ;
#5523=EDGE_LOOP ( 'NONE', ( #26810, #108, #12779, #25635 ) ) ;
#5525=FACE_OUTER_BOUND ( 'NONE', #25825, .T. ) ;
#5536=DIRECTION ( 'NONE',  ( -0.000000000000000000, -0.000000000000000000, -1.000000000000000000 ) ) ;
#5540=EDGE_CURVE ( 'NONE', #9701, #14768, #13892, .T. ) ;
#5541=AXIS2_PLACEMENT_3D ( 'NONE', #24526, #11839, #26717 ) ;
#5544=CARTESIAN_POINT ( 'NONE',  ( -30.51827900900859447, 4.402097243136374516, 5.049999999999999822 ) ) ;
#5548=CARTESIAN_POINT ( 'NONE',  ( -18.46086643607116073, 15.89617442677120707, 1.835203429153471344 ) ) ;
#5550=ORIENTED_EDGE ( 'NONE', *, *, #32952, .T. ) ;
#5557=CARTESIAN_POINT ( 'NONE',  ( 16.64984788795954884, 12.68590369525696993, -1.499999999999999778 ) ) ;
#5559=AXIS2_PLACEMENT_3D ( 'NONE', #16450, #26655, #3469 ) ;
#5562=DIRECTION ( 'NONE',  ( -0.1413077769430314268, 0.9899657126261587337, 0.000000000000000000 ) ) ;
#5576=CYLINDRICAL_SURFACE ( 'NONE', #29443, 297.9387600756452912 ) ;
#5579=DIRECTION ( 'NONE',  ( -0.4999999999999954481, -0.8660254037844412611, -0.000000000000000000 ) ) ;
#5582=AXIS2_PLACEMENT_3D ( 'NONE', #31305, #9317, #29221 ) ;
#5589=CARTESIAN_POINT ( 'NONE',  ( 9.282537329959740902, 0.2172754300396697036, -1.050000000000000044 ) ) ;
#5592=SPHERICAL_SURFACE ( 'NONE', #26696, 0.4500000000000000111 ) ;
#5598=DIRECTION ( 'NONE',  ( -0.7821988420038089584, 0.6230288689682847991, 0.000000000000000000 ) ) ;
#5610=CARTESIAN_POINT ( 'NONE',  ( 0.000000000000000000, 0.000000000000000000, 1.500000000000000000 ) ) ;
#5613=CARTESIAN_POINT ( 'NONE',  ( 11.04311965146451158, 15.00000000000000178, 1.508259000770581615 ) ) ;
#5619=CARTESIAN_POINT ( 'NONE',  ( 13.17798765760825574, 21.79280053074250389, -1.386497237026226959 ) ) ;
#5653=CARTESIAN_POINT ( 'NONE',  ( 16.10106094948406863, 19.71584668020014419, -5.396302277755718357 ) ) ;
#5666=DIRECTION ( 'NONE',  ( -0.000000000000000000, -0.000000000000000000, -1.000000000000000000 ) ) ;
#5669=EDGE_CURVE ( 'NONE', #32661, #17424, #17340, .T. ) ;
#5673=CARTESIAN_POINT ( 'NONE',  ( 108.2060071697601558, 19.32528913265312198, 3.339987910135337579 ) ) ;
#5684=EDGE_CURVE ( 'NONE', #10113, #25309, #22844, .T. ) ;
#5695=ORIENTED_EDGE ( 'NONE', *, *, #15869, .F. ) ;
#5697=EDGE_CURVE ( 'NONE', #27222, #18387, #20684, .T. ) ;
#5703=CARTESIAN_POINT ( 'NONE',  ( -1.082681991931092158, 0.000000000000000000, -4.612695725900422872 ) ) ;
#5708=CARTESIAN_POINT ( 'NONE',  ( 15.58693300068916088, 10.49296960295601089, 1.500000000000000000 ) ) ;
#5711=ADVANCED_FACE ( 'NONE', ( #30887 ), #15815, .F. ) ;
#5717=DIRECTION ( 'NONE',  ( -1.000000000000000000, 0.000000000000000000, -0.000000000000000000 ) ) ;
#5731=CARTESIAN_POINT ( 'NONE',  ( 16.36487458112951643, 19.37645981759113312, 4.629213727441584325 ) ) ;
#5739=ORIENTED_EDGE ( 'NONE', *, *, #21114, .F. ) ;
#5747=DIRECTION ( 'NONE',  ( 0.1995114832788637271, -0.000000000000000000, -0.9798954883250904357 ) ) ;
#5749=CARTESIAN_POINT ( 'NONE',  ( 0.6708088701982989344, 0.000000000000000000, -4.612695725900422872 ) ) ;
#5769=( NAMED_UNIT ( * ) PLANE_ANGLE_UNIT ( ) SI_UNIT ( $, .RADIAN. ) );
#5795=DIRECTION ( 'NONE',  ( -0.000000000000000000, -0.000000000000000000, 1.000000000000000000 ) ) ;
#5817=DIRECTION ( 'NONE',  ( 1.049727191138617956E-16, 0.6018150231520437154, 0.7986355100472962709 ) ) ;
#5826=CARTESIAN_POINT ( 'NONE',  ( -57.16979796353925991, -2.912899199960345964, 5.499999999999999112 ) ) ;
#5850=CARTESIAN_POINT ( 'NONE',  ( 12.22374906632087743, 4.895420474198960648, 1.050000000000000044 ) ) ;
#5857=CARTESIAN_POINT ( 'NONE',  ( -29.86094048198892281, 8.975184657953134248, 2.011338252942258986 ) ) ;
#5862=CARTESIAN_POINT ( 'NONE',  ( 47.62814091865205768, 23.65599663307499512, 4.629213727441585213 ) ) ;
#5872=EDGE_CURVE ( 'NONE', #14230, #1418, #24521, .T. ) ;
#5873=FACE_OUTER_BOUND ( 'NONE', #8697, .T. ) ;
#5889=ORIENTED_EDGE ( 'NONE', *, *, #8715, .T. ) ;
#5907=CARTESIAN_POINT ( 'NONE',  ( 107.6659035224683407, 16.31777890981063805, 1.506649871266091401 ) ) ;
#5929=VERTEX_POINT ( 'NONE', #23974 ) ;
#5948=CIRCLE ( 'NONE', #9660, 0.4500000000000008993 ) ;
#5953=CARTESIAN_POINT ( 'NONE',  ( 108.0492846245400926, 18.45259616110433498, 4.648328607135879587 ) ) ;
#5972=AXIS2_PLACEMENT_3D ( 'NONE', #16394, #28779, #26607 ) ;
#5982=CARTESIAN_POINT ( 'NONE',  ( 108.2060074055500394, 19.32529044562417653, -3.323467105140293310 ) ) ;
#5983=ORIENTED_EDGE ( 'NONE', *, *, #1877, .T. ) ;
#5993=CIRCLE ( 'NONE', #15585, 0.5000000000000004441 ) ;
#5995=CARTESIAN_POINT ( 'NONE',  ( -9.288857950784214168, 3.520075575296779835, 1.500000000000000222 ) ) ;
#5996=AXIS2_PLACEMENT_3D ( 'NONE', #22350, #8970, #29374 ) ;
#6000=CARTESIAN_POINT ( 'NONE',  ( -23.54713438637982748, 13.45615422372499914, 10.69317089570273360 ) ) ;
#6009=ORIENTED_EDGE ( 'NONE', *, *, #9139, .T. ) ;
#6010=DIRECTION ( 'NONE',  ( 0.000000000000000000, -0.9271838545667856479, -0.3746065934159163446 ) ) ;
#6012=ORIENTED_EDGE ( 'NONE', *, *, #4011, .T. ) ;
#6017=AXIS2_PLACEMENT_3D ( 'NONE', #11548, #21416, #14207 ) ;
#6019=CARTESIAN_POINT ( 'NONE',  ( 107.9622325421415212, 20.81773585569407459, 1.508259000770582059 ) ) ;
#6029=CARTESIAN_POINT ( 'NONE',  ( 21.15383509118241889, 16.85013971177662384, -1.500000000000000222 ) ) ;
#6036=DIRECTION ( 'NONE',  ( -0.000000000000000000, -0.3746065934159164001, 0.9271838545667856479 ) ) ;
#6041=DIRECTION ( 'NONE',  ( -0.4999999999999981681, -0.8660254037844395958, 0.000000000000000000 ) ) ;
#6042=LINE ( 'NONE', #16538, #14670 ) ;
#6049=CARTESIAN_POINT ( 'NONE',  ( 78.59573142019985426, 24.17918843217023195, 5.412820279296878923 ) ) ;
#6051=DIRECTION ( 'NONE',  ( -0.000000000000000000, -0.000000000000000000, -1.000000000000000000 ) ) ;
#6055=ORIENTED_EDGE ( 'NONE', *, *, #12708, .T. ) ;
#6056=B_SPLINE_CURVE_WITH_KNOTS ( 'NONE', 3,
 ( #7442, #25361, #17641, #27850 ),
 .UNSPECIFIED., .F., .F.,
 ( 4, 4 ),
 ( 0.000000000000000000, 0.0002520312449908130637 ),
 .UNSPECIFIED. ) ;
#6058=DIRECTION ( 'NONE',  ( -0.000000000000000000, -0.000000000000000000, -1.000000000000000000 ) ) ;
#6066=FACE_OUTER_BOUND ( 'NONE', #26407, .T. ) ;
#6067=VERTEX_POINT ( 'NONE', #9932 ) ;
#6076=CARTESIAN_POINT ( 'NONE',  ( 17.54326037862280430, 13.05023557628343056, -1.500000000000000000 ) ) ;
#6088=CARTESIAN_POINT ( 'NONE',  ( -23.54713438637982748, 8.275374457817619600, 8.600000000000004974 ) ) ;
#6106=EDGE_CURVE ( 'NONE', #22604, #13143, #6358, .T. ) ;
#6109=CARTESIAN_POINT ( 'NONE',  ( -0.6528202993443394941, 0.000000000000000000, 5.412820279296878923 ) ) ;
#6114=DIRECTION ( 'NONE',  ( -0.8660254037844399289, 0.4999999999999978906, 0.000000000000000000 ) ) ;
#6137=AXIS2_PLACEMENT_3D ( 'NONE', #6088, #3582, #3733 ) ;
#6138=CARTESIAN_POINT ( 'NONE',  ( 107.6996442589676235, 19.35565155597516807, 4.629213727441722881 ) ) ;
#6149=CARTESIAN_POINT ( 'NONE',  ( 22.29416355858534970, 17.04711948199285843, -1.050000000000000266 ) ) ;
#6154=CARTESIAN_POINT ( 'NONE',  ( 25.18701699284994078, 18.96209959523617172, -1.477901791411339483 ) ) ;
#6155=CARTESIAN_POINT ( 'NONE',  ( -1.152183934781129714E-14, 21.49000000000002331, 1.500000000000000000 ) ) ;
#6158=LINE ( 'NONE', #8825, #4961 ) ;
#6159=DIRECTION ( 'NONE',  ( -0.000000000000000000, 0.000000000000000000, 1.000000000000000000 ) ) ;
#6161=VERTEX_POINT ( 'NONE', #13106 ) ;
#6170=CARTESIAN_POINT ( 'NONE',  ( -57.38987804550299643, -3.170151398038286938, 5.871858310191695907 ) ) ;
#6176=EDGE_CURVE ( 'NONE', #15051, #24398, #13392, .T. ) ;
#6178=ORIENTED_EDGE ( 'NONE', *, *, #9343, .F. ) ;
#6192=ORIENTED_EDGE ( 'NONE', *, *, #23158, .F. ) ;
#6201=CARTESIAN_POINT ( 'NONE',  ( -16.60354855507977234, 9.200062826706011165, 1.500000000000000000 ) ) ;
#6205=CARTESIAN_POINT ( 'NONE',  ( 9.292237988713592856, 0.2314288474955234209, 1.048307530264791287 ) ) ;
#6211=PLANE ( 'NONE',  #5972 ) ;
#6213=ORIENTED_EDGE ( 'NONE', *, *, #4736, .T. ) ;
#6214=CARTESIAN_POINT ( 'NONE',  ( 26.08945412691625521, 19.05746434167071612, -1.050000000000000044 ) ) ;
#6221=EDGE_CURVE ( 'NONE', #23825, #4970, #14906, .T. ) ;
#6227=CARTESIAN_POINT ( 'NONE',  ( 11.67104222964946558, 3.952383228255008429, -1.500000000000829337 ) ) ;
#6229=DIRECTION ( 'NONE',  ( 0.000000000000000000, -0.9271838545667855369, -0.3746065934159163446 ) ) ;
#6234=FACE_BOUND ( 'NONE', #872, .T. ) ;
#6239=CARTESIAN_POINT ( 'NONE',  ( 8.911384905465473238, 0.2172754300402908179, -1.412391582771881371 ) ) ;
#6244=CARTESIAN_POINT ( 'NONE',  ( 47.62814091865205768, 23.65599663307499512, -4.612695725900423760 ) ) ;
#6245=VERTEX_POINT ( 'NONE', #13737 ) ;
#6258=CARTESIAN_POINT ( 'NONE',  ( -53.73534286770232882, 4.623678987564122878, 5.128141679950119602 ) ) ;
#6259=DIRECTION ( 'NONE',  ( -0.000000000000000000, -0.000000000000000000, 1.000000000000000000 ) ) ;
#6266=DIRECTION ( 'NONE',  ( 1.000000000000000000, 0.000000000000000000, 0.000000000000000000 ) ) ;
#6268=DIRECTION ( 'NONE',  ( 0.000000000000000000, -0.9271838545667856479, -0.3746065934159163446 ) ) ;
#6274=DIRECTION ( 'NONE',  ( -0.000000000000000000, 0.000000000000000000, 1.000000000000000000 ) ) ;
#6290=EDGE_LOOP ( 'NONE', ( #15803, #2977, #2135, #2110, #21636 ) ) ;
#6298=ORIENTED_EDGE ( 'NONE', *, *, #13974, .T. ) ;
#6299=CARTESIAN_POINT ( 'NONE',  ( 8.950995676490906661, 0.000000000000000000, 1.008084992930269541 ) ) ;
#6300=DIRECTION ( 'NONE',  ( 0.7895257206258718963, 0.6137174728408810731, 0.000000000000000000 ) ) ;
#6315=CARTESIAN_POINT ( 'NONE',  ( 8.870145747188287189, 0.000000000000000000, -1.000000000000000000 ) ) ;
#6316=CARTESIAN_POINT ( 'NONE',  ( -59.40947820539835789, -5.253841109363955653, 5.268872846900772622 ) ) ;
#6320=ORIENTED_EDGE ( 'NONE', *, *, #15706, .T. ) ;
#6325=ADVANCED_FACE ( 'NONE', ( #4210 ), #2095, .T. ) ;
#6328=LINE ( 'NONE', #11675, #14940 ) ;
#6342=FACE_OUTER_BOUND ( 'NONE', #8492, .T. ) ;
#6344=CARTESIAN_POINT ( 'NONE',  ( 13.44361105969346504, 21.88231906142583938, 1.272599291342047190 ) ) ;
#6350=FACE_OUTER_BOUND ( 'NONE', #10147, .T. ) ;
#6358=B_SPLINE_CURVE_WITH_KNOTS ( 'NONE', 3,
 ( #32686, #14269, #9767, #4441, #2256, #14618, #19491, #24464, #11769, #24819, #29683, #1938, #12110, #22308, #28497, #7590, #30507, #2588 ),
 .UNSPECIFIED., .F., .F.,
 ( 4, 2, 2, 2, 2, 2, 2, 2, 4 ),
 ( 0.000000000000000000, 0.0003646863777415453706, 0.0005470295666123181372, 0.0006382011610477136008, 0.0006837869582654212530, 0.0007065798568742751333, 0.0007179763061787019108, 0.0007236745308309153538, 0.0007293727554831286883 ),
 .UNSPECIFIED. ) ;
#6367=CARTESIAN_POINT ( 'NONE',  ( -38.14293509397969473, 10.97000000000000419, 1.050000000000000044 ) ) ;
#6373=DIRECTION ( 'NONE',  ( 0.2880220749472559572, 0.1662896225033555220, -0.9430753128943462071 ) ) ;
#6375=CARTESIAN_POINT ( 'NONE',  ( 18.71251328246767898, 14.89923106884208615, -1.500000000000000000 ) ) ;
#6383=CIRCLE ( 'NONE', #14362, 302.4235430809786749 ) ;
#6385=LINE ( 'NONE', #14241, #29626 ) ;
#6395=EDGE_CURVE ( 'NONE', #23529, #685, #12844, .T. ) ;
#6396=EDGE_CURVE ( 'NONE', #8403, #17832, #21403, .T. ) ;
#6407=DIRECTION ( 'NONE',  ( -0.4999999999999982236, -0.8660254037844397068, 0.000000000000000000 ) ) ;
#6412=CARTESIAN_POINT ( 'NONE',  ( 13.41780342409107973, 19.07609913100965571, 4.629213727441584325 ) ) ;
#6414=DIRECTION ( 'NONE',  ( -0.000000000000000000, -0.000000000000000000, -1.000000000000000000 ) ) ;
#6419=CARTESIAN_POINT ( 'NONE',  ( -56.77528804678861007, 0.4484486523079136977, 1.857590217363785712 ) ) ;
#6464=DIRECTION ( 'NONE',  ( 0.000000000000000000, 0.000000000000000000, 1.000000000000000000 ) ) ;
#6476=ADVANCED_FACE ( 'NONE', ( #20605 ), #32874, .T. ) ;
#6483=CARTESIAN_POINT ( 'NONE',  ( -2.096054051514731231, 1.210157370878028882, 1.500000000000000000 ) ) ;
#6490=CARTESIAN_POINT ( 'NONE',  ( 107.4385791398478744, 17.85938043952739918, -4.612695725900423760 ) ) ;
#6505=CARTESIAN_POINT ( 'NONE',  ( -53.35155202832373078, 4.845260731991866798, 5.128141679950118714 ) ) ;
#6511=ORIENTED_EDGE ( 'NONE', *, *, #3383, .F. ) ;
#6527=CARTESIAN_POINT ( 'NONE',  ( -27.72185742298243838, 17.09829073722480075, 1.500000000000000000 ) ) ;
#6539=AXIS2_PLACEMENT_3D ( 'NONE', #1949, #17809, #20155 ) ;
#6551=CARTESIAN_POINT ( 'NONE',  ( -53.64896896705157303, 5.489213761225001598, 1.476102572572478344 ) ) ;
#6561=AXIS2_PLACEMENT_3D ( 'NONE', #16486, #6300, #16987 ) ;
#6562=CARTESIAN_POINT ( 'NONE',  ( 13.32584843805069852, 6.791410140808786799, -1.050000000000000044 ) ) ;
#6580=CARTESIAN_POINT ( 'NONE',  ( 107.9275968081481238, 17.77499038371485440, 4.627610784060873783 ) ) ;
#6589=CARTESIAN_POINT ( 'NONE',  ( 2.382865613620175349, 0.5000000000000000000, -1.500000000000000000 ) ) ;
#6601=CARTESIAN_POINT ( 'NONE',  ( 16.36487458112951643, 19.37645981759113312, 4.629213727441584325 ) ) ;
#6627=ORIENTED_EDGE ( 'NONE', *, *, #28906, .F. ) ;
#6637=CARTESIAN_POINT ( 'NONE',  ( 8.911384905465308037, 0.2172754300403238470, -1.412391582772828169 ) ) ;
#6639=CARTESIAN_POINT ( 'NONE',  ( 11.04311965146451158, 15.00000000000000178, -1.491740999229418829 ) ) ;
#6644=CARTESIAN_POINT ( 'NONE',  ( 8.870145747188287189, 0.000000000000000000, 1.000000000000000000 ) ) ;
#6647=ADVANCED_FACE ( 'NONE', ( #16716 ), #8039, .T. ) ;
#6650=CARTESIAN_POINT ( 'NONE',  ( 108.1722781158648417, 19.13747245171689570, -4.846044801720160500 ) ) ;
#6651=DIRECTION ( 'NONE',  ( 1.000000000000000000, 0.000000000000000000, 0.000000000000000000 ) ) ;
#6654=FACE_OUTER_BOUND ( 'NONE', #3207, .T. ) ;
#6664=CARTESIAN_POINT ( 'NONE',  ( -53.95513674679793326, 5.522463357794191730, 1.050000000000049116 ) ) ;
#6671=ORIENTED_EDGE ( 'NONE', *, *, #8308, .F. ) ;
#6682=CARTESIAN_POINT ( 'NONE',  ( 0.000000000000000000, 0.5000000000000000000, 1.500000000000000000 ) ) ;
#6693=CARTESIAN_POINT ( 'NONE',  ( 12.62463379335046376, 21.58553169041389452, 1.499999999999994449 ) ) ;
#6695=CARTESIAN_POINT ( 'NONE',  ( 22.89575061816920254, 17.95407957496613705, 1.500000000000000222 ) ) ;
#6698=CARTESIAN_POINT ( 'NONE',  ( -23.54713438637984169, 18.46223496596754288, 1.773004750130224627 ) ) ;
#6700=FACE_OUTER_BOUND ( 'NONE', #14369, .T. ) ;
#6708=EDGE_CURVE ( 'NONE', #32554, #28100, #7487, .T. ) ;
#6712=ORIENTED_EDGE ( 'NONE', *, *, #21718, .T. ) ;
#6714=ORIENTED_EDGE ( 'NONE', *, *, #13166, .F. ) ;
#6717=ORIENTED_EDGE ( 'NONE', *, *, #29954, .T. ) ;
#6724=ORIENTED_EDGE ( 'NONE', *, *, #11439, .F. ) ;
#6725=CARTESIAN_POINT ( 'NONE',  ( 25.55085174366697487, 19.30847049843654162, -1.500000000000000000 ) ) ;
#6729=ADVANCED_FACE ( 'NONE', ( #5336 ), #32783, .F. ) ;
#6735=EDGE_CURVE ( 'NONE', #10930, #28345, #33028, .T. ) ;
#6779=CARTESIAN_POINT ( 'NONE',  ( 108.0068349480237515, 18.21621961241920573, -4.398253369385427547 ) ) ;
#6784=DIRECTION ( 'NONE',  ( 0.4999999999999981681, 0.8660254037844395958, 0.000000000000000000 ) ) ;
#6793=CARTESIAN_POINT ( 'NONE',  ( 21.39732310845265673, 16.45281003597622416, -1.050000000000000044 ) ) ;
#6798=CARTESIAN_POINT ( 'NONE',  ( 8.930755659325139817, 0.4999999999999980571, -1.500000000000000000 ) ) ;
#6803=CARTESIAN_POINT ( 'NONE',  ( 2.652619124157556740, 0.000000000000000000, -1.000000000000000000 ) ) ;
#6806=CARTESIAN_POINT ( 'NONE',  ( 25.89197189428493218, 19.03682222646506261, 1.281348668662838586 ) ) ;
#6829=DIRECTION ( 'NONE',  ( 0.4999999999999977796, 0.8660254037844398178, 0.000000000000000000 ) ) ;
#6831=ORIENTED_EDGE ( 'NONE', *, *, #995, .T. ) ;
#6832=ORIENTED_EDGE ( 'NONE', *, *, #12853, .F. ) ;
#6840=DIRECTION ( 'NONE',  ( -0.000000000000000000, 0.000000000000000000, 1.000000000000000000 ) ) ;
#6841=CARTESIAN_POINT ( 'NONE',  ( -59.41331340564917696, -5.243606251429877574, 5.221013976802370671 ) ) ;
#6849=CARTESIAN_POINT ( 'NONE',  ( -26.97068441990215959, 17.65690804191583396, 1.500000000000000000 ) ) ;
#6851=ADVANCED_FACE ( 'NONE', ( #24324 ), #18202, .F. ) ;
#6858=DIRECTION ( 'NONE',  ( 0.1736481776669307198, 0.000000000000000000, -0.9848077530122080203 ) ) ;
#6862=EDGE_LOOP ( 'NONE', ( #27717, #15991, #24479, #18268 ) ) ;
#6863=CARTESIAN_POINT ( 'NONE',  ( 17.32050807568873552, 10.00000000000002309, 4.629213727441584325 ) ) ;
#6864=EDGE_LOOP ( 'NONE', ( #1038, #19327, #9749, #6012, #12226 ) ) ;
#6865=CARTESIAN_POINT ( 'NONE',  ( 8.930755659325141593, 0.5000000000000008882, 1.500000000000000000 ) ) ;
#6868=ORIENTED_EDGE ( 'NONE', *, *, #13651, .F. ) ;
#6869=CARTESIAN_POINT ( 'NONE',  ( -50.81000000000000227, -10.96999999999998643, 5.700000000000000178 ) ) ;
#6871=CARTESIAN_POINT ( 'NONE',  ( 107.7536796087345294, 16.80655079293032017, 1.395761063491601783 ) ) ;
#6874=CARTESIAN_POINT ( 'NONE',  ( 9.065183082710470686, 0.01785380481418076190, -1.195037335522168176 ) ) ;
#6894=ORIENTED_EDGE ( 'NONE', *, *, #5540, .F. ) ;
#6904=VERTEX_POINT ( 'NONE', #26765 ) ;
#6921=DIRECTION ( 'NONE',  ( -1.000000000000000000, 4.336808689942013792E-15, 0.000000000000000000 ) ) ;
#6922=LINE ( 'NONE', #17118, #22131 ) ;
#6943=SHAPE_DEFINITION_REPRESENTATION ( #24407, #27351 ) ;
#6949=DIRECTION ( 'NONE',  ( 0.4999999999999978906, 0.8660254037844398178, 0.000000000000000000 ) ) ;
#6972=CARTESIAN_POINT ( 'NONE',  ( -56.28351068137280322, 0.4500000000000000111, 0.000000000000000000 ) ) ;
#6978=AXIS2_PLACEMENT_3D ( 'NONE', #20826, #18327, #17998 ) ;
#6983=AXIS2_PLACEMENT_3D ( 'NONE', #16670, #30067, #17166 ) ;
#7014=AXIS2_PLACEMENT_3D ( 'NONE', #32402, #29366, #12604 ) ;
#7018=CARTESIAN_POINT ( 'NONE',  ( -18.23565129703368726, 15.66456206417224806, 1.840856759657562680 ) ) ;
#7027=ORIENTED_EDGE ( 'NONE', *, *, #11089, .F. ) ;
#7035=( BOUNDED_SURFACE ( )  B_SPLINE_SURFACE ( 1, 3, ( 
 ( #32839, #9738, #19966, #22785 ),
 ( #10061, #20274, #12235, #12411 ) ),
 .UNSPECIFIED., .F., .F., .F. ) 
 B_SPLINE_SURFACE_WITH_KNOTS ( ( 2, 2 ),
 ( 4, 4 ),
 ( 0.000000000000000000, 1.000000000000000000 ),
 ( 0.000000000000000000, 1.000000000000000000 ),
 .UNSPECIFIED. ) 
 GEOMETRIC_REPRESENTATION_ITEM ( )  RATIONAL_B_SPLINE_SURFACE ( (
 ( 1.000000000000000000, 0.9917560313531952332, 0.9917560313531952332, 1.000000000000000000),
 ( 1.000000000000000000, 0.9917560313531952332, 0.9917560313531952332, 1.000000000000000000) ) ) 
 REPRESENTATION_ITEM ( '' )  SURFACE ( )  );
#7038=ORIENTED_EDGE ( 'NONE', *, *, #1877, .F. ) ;
#7046=DIRECTION ( 'NONE',  ( -0.4999999999999977240, -0.8660254037844399289, 0.000000000000000000 ) ) ;
#7061=VECTOR ( 'NONE', #18788, 1000.000000000000227 ) ;
#7065=AXIS2_PLACEMENT_3D ( 'NONE', #6869, #9386, #2201 ) ;
#7066=CARTESIAN_POINT ( 'NONE',  ( 108.1156589233279135, 18.82219444680288589, -4.397958565568439226 ) ) ;
#7079=CARTESIAN_POINT ( 'NONE',  ( -50.81000000000000227, -10.96999999999998643, 1.500000000000000000 ) ) ;
#7089=DIRECTION ( 'NONE',  ( -0.000000000000000000, -0.000000000000000000, -1.000000000000000000 ) ) ;
#7103=CARTESIAN_POINT ( 'NONE',  ( 5.865515302491369987, 15.00000000000000178, -1.491740999229417941 ) ) ;
#7110=CARTESIAN_POINT ( 'NONE',  ( -50.81000000000000227, -10.96999999999998643, 5.500000000000000000 ) ) ;
#7111=DIRECTION ( 'NONE',  ( -0.000000000000000000, -0.3746065934159164001, 0.9271838545667856479 ) ) ;
#7117=ADVANCED_FACE ( 'NONE', ( #948 ), #18649, .F. ) ;
#7123=AXIS2_PLACEMENT_3D ( 'NONE', #2372, #20089, #32307 ) ;
#7126=LINE ( 'NONE', #4617, #17266 ) ;
#7142=CARTESIAN_POINT ( 'NONE',  ( 9.302055952181040865, 0.2457637073014105056, -1.050000000000000044 ) ) ;
#7162=CARTESIAN_POINT ( 'NONE',  ( -56.32730583845947336, 0.4233724216868345325, -1.495526720789816189 ) ) ;
#7163=DIRECTION ( 'NONE',  ( 0.4999999999999978351, 0.8660254037844398178, 0.000000000000000000 ) ) ;
#7185=CARTESIAN_POINT ( 'NONE',  ( -42.24752261775680040, -15.91354862156815031, 5.049999999999999822 ) ) ;
#7190=ORIENTED_EDGE ( 'NONE', *, *, #22372, .T. ) ;
#7199=CARTESIAN_POINT ( 'NONE',  ( 10.07348277749544074, 2.217756237939506381, 1.500000000000000000 ) ) ;
#7201=CARTESIAN_POINT ( 'NONE',  ( -19.46330280939116619, 17.00757181511099603, 1.808020238517410672 ) ) ;
#7203=CARTESIAN_POINT ( 'NONE',  ( -23.54713438637982748, 4.195786794269684705, 1.499999999999999112 ) ) ;
#7217=ADVANCED_FACE ( 'NONE', ( #9280 ), #17313, .T. ) ;
#7218=CARTESIAN_POINT ( 'NONE',  ( 108.0972248732595631, 18.71954638228143253, -5.110367419609437967 ) ) ;
#7221=EDGE_CURVE ( 'NONE', #23082, #30095, #8603, .T. ) ;
#7223=ORIENTED_EDGE ( 'NONE', *, *, #5321, .T. ) ;
#7225=DIRECTION ( 'NONE',  ( -0.000000000000000000, 0.000000000000000000, 1.000000000000000000 ) ) ;
#7238=CARTESIAN_POINT ( 'NONE',  ( 108.3798353887421655, 20.29323324528482431, -1.257911982557052832 ) ) ;
#7241=VERTEX_POINT ( 'NONE', #19498 ) ;
#7247=DIRECTION ( 'NONE',  ( 0.4999999999999978351, 0.8660254037844399289, 0.000000000000000000 ) ) ;
#7256=DIRECTION ( 'NONE',  ( 1.000000000000000000, 0.000000000000000000, 0.000000000000000000 ) ) ;
#7282=CARTESIAN_POINT ( 'NONE',  ( -61.78000000000001535, -10.96999999999998820, 1.500000000000000000 ) ) ;
#7285=DIRECTION ( 'NONE',  ( 1.000000000000000000, 0.000000000000000000, 0.000000000000000000 ) ) ;
#7292=FACE_OUTER_BOUND ( 'NONE', #18594, .T. ) ;
#7304=ADVANCED_FACE ( 'NONE', ( #30023 ), #26231, .F. ) ;
#7309=CARTESIAN_POINT ( 'NONE',  ( -56.77769102277633095, 0.5030464795276023970, -1.499999999999993117 ) ) ;
#7318=CARTESIAN_POINT ( 'NONE',  ( 108.0381133239749687, 18.39038995157331158, 4.615673165465349115 ) ) ;
#7319=ADVANCED_FACE ( 'NONE', ( #4762 ), #25147, .T. ) ;
#7325=VERTEX_POINT ( 'NONE', #2445 ) ;
#7342=DIRECTION ( 'NONE',  ( 1.000000000000000000, 0.000000000000000000, 0.000000000000000000 ) ) ;
#7352=CARTESIAN_POINT ( 'NONE',  ( -28.75976233758147771, 6.805598625774648802, 1.499999999998557820 ) ) ;
#7363=DIRECTION ( 'NONE',  ( -0.000000000000000000, -0.000000000000000000, -1.000000000000000000 ) ) ;
#7367=CARTESIAN_POINT ( 'NONE',  ( -17.53440904309154647, 8.148348245851819271, 2.033243229306796351 ) ) ;
#7402=VERTEX_POINT ( 'NONE', #5613 ) ;
#7410=DIRECTION ( 'NONE',  ( 0.4999999999999967804, 0.8660254037844405950, 0.000000000000000000 ) ) ;
#7415=FACE_OUTER_BOUND ( 'NONE', #6862, .T. ) ;
#7434=CIRCLE ( 'NONE', #12774, 297.9387600756452912 ) ;
#7439=ORIENTED_EDGE ( 'NONE', *, *, #28088, .T. ) ;
#7442=CARTESIAN_POINT ( 'NONE',  ( 24.97738509828242925, 18.93945643846228677, -1.491740999229418829 ) ) ;
#7444=ORIENTED_EDGE ( 'NONE', *, *, #6106, .F. ) ;
#7450=EDGE_CURVE ( 'NONE', #19201, #2610, #9675, .T. ) ;
#7453=DIRECTION ( 'NONE',  ( 0.000000000000000000, 0.000000000000000000, -1.000000000000000000 ) ) ;
#7454=CARTESIAN_POINT ( 'NONE',  ( 7.577572045913244736, 15.00000000000000178, 4.629213727441584325 ) ) ;
#7460=CARTESIAN_POINT ( 'NONE',  ( -56.36676944933713429, 0.006999862979873096649, -1.006932307331389609 ) ) ;
#7487=B_SPLINE_CURVE_WITH_KNOTS ( 'NONE', 3,
 ( #22385, #14032, #1361, #11536, #21731, #18041, #23051, #10012, #30269, #20389, #30116, #25405, #17385 ),
 .UNSPECIFIED., .F., .F.,
 ( 4, 3, 3, 3, 4 ),
 ( 1.301042606982605321E-18, 0.0006642486831287936454, 0.001556668540121195800, 0.002449088397071176593, 0.003341508253979123301 ),
 .UNSPECIFIED. ) ;
#7494=CARTESIAN_POINT ( 'NONE',  ( 107.6696042164950740, 19.18437618895796248, 4.906253902711251058 ) ) ;
#7495=ORIENTED_EDGE ( 'NONE', *, *, #20871, .T. ) ;
#7505=CARTESIAN_POINT ( 'NONE',  ( 12.61464622672343516, 16.97301654637829671, -1.491740999229419273 ) ) ;
#7519=CARTESIAN_POINT ( 'NONE',  ( -23.54713438637982748, 10.61651369059875272, 9.545881648375194928 ) ) ;
#7527=CARTESIAN_POINT ( 'NONE',  ( -21.12071669798443452, 17.96555046547580048, 1.784921029145990046 ) ) ;
#7530=AXIS2_PLACEMENT_3D ( 'NONE', #32377, #1591, #2092 ) ;
#7531=ORIENTED_EDGE ( 'NONE', *, *, #25545, .F. ) ;
#7536=CIRCLE ( 'NONE', #31580, 0.9999999999999991118 ) ;
#7556=DIRECTION ( 'NONE',  ( -0.000000000000000000, -0.000000000000000000, -1.000000000000000000 ) ) ;
#7575=ORIENTED_EDGE ( 'NONE', *, *, #23084, .T. ) ;
#7578=CARTESIAN_POINT ( 'NONE',  ( -41.04909327648282158, -14.04690330772141316, 5.700934511681481354 ) ) ;
#7587=DIRECTION ( 'NONE',  ( 1.000000000000000000, 0.000000000000000000, 0.000000000000000000 ) ) ;
#7590=CARTESIAN_POINT ( 'NONE',  ( -56.33890164103149800, 0.003417460827233314170, -1.001984214669649820 ) ) ;
#7596=CIRCLE ( 'NONE', #4406, 0.4499999999999999001 ) ;
#7601=DIRECTION ( 'NONE',  ( 0.000000000000000000, 0.000000000000000000, 1.000000000000000000 ) ) ;
#7614=CARTESIAN_POINT ( 'NONE',  ( 9.282537329959909655, 0.2172754300399158400, -1.041239158277187160 ) ) ;
#7615=CARTESIAN_POINT ( 'NONE',  ( 24.72695737054825926, 18.91229966141139229, 1.500000000000000000 ) ) ;
#7619=DIRECTION ( 'NONE',  ( 0.000000000000000000, 0.000000000000000000, 1.000000000000000000 ) ) ;
#7629=DIRECTION ( 'NONE',  ( 0.000000000000000000, 0.9848077530122081313, 0.1736481776669305255 ) ) ;
#7636=CARTESIAN_POINT ( 'NONE',  ( 17.44299375779232264, 12.90469621563894798, 1.049999999999999378 ) ) ;
#7646=CARTESIAN_POINT ( 'NONE',  ( -31.85664627820676387, -0.0003384977252905707612, 1.731076043996917724 ) ) ;
#7654=CARTESIAN_POINT ( 'NONE',  ( -56.77769102277633806, 0.5030464795276025081, -1.050000000000000044 ) ) ;
#7656=VERTEX_POINT ( 'NONE', #24600 ) ;
#7668=DIRECTION ( 'NONE',  ( -0.1413077769430314268, 0.9899657126261587337, 0.000000000000000000 ) ) ;
#7670=LINE ( 'NONE', #17870, #4912 ) ;
#7676=EDGE_CURVE ( 'NONE', #29447, #16073, #9993, .T. ) ;
#7685=DIRECTION ( 'NONE',  ( -0.8660254037844442587, 0.4999999999999902300, 0.000000000000000000 ) ) ;
#7699=CARTESIAN_POINT ( 'NONE',  ( 107.9622325421415212, 20.81773585569407459, -1.491740999229417941 ) ) ;
#7700=CIRCLE ( 'NONE', #31716, 10.43371088333262087 ) ;
#7702=CARTESIAN_POINT ( 'NONE',  ( -30.19835004250544586, 10.24026612823149662, 1.500000000000003109 ) ) ;
#7707=LINE ( 'NONE', #28420, #1751 ) ;
#7719=CARTESIAN_POINT ( 'NONE',  ( -17.30305273768104612, 8.786760116294463074, 2.016332066590946770 ) ) ;
#7730=DIRECTION ( 'NONE',  ( -0.4999999999999978906, -0.8660254037844397068, -9.233562054644581322E-18 ) ) ;
#7731=CARTESIAN_POINT ( 'NONE',  ( 26.23173791223905837, 19.12152673998438601, 1.050000000000000044 ) ) ;
#7738=ORIENTED_EDGE ( 'NONE', *, *, #8704, .T. ) ;
#7739=DIRECTION ( 'NONE',  ( 0.000000000000000000, 0.9056868434498948073, 0.4239473335235944829 ) ) ;
#7740=CARTESIAN_POINT ( 'NONE',  ( -26.98657589828505721, 17.41894840571574576, 1.798104102373871971 ) ) ;
#7752=ORIENTED_EDGE ( 'NONE', *, *, #6708, .F. ) ;
#7776=ADVANCED_FACE ( 'NONE', ( #12895 ), #5576, .F. ) ;
#7779=CARTESIAN_POINT ( 'NONE',  ( 11.04311965146451335, 15.00000000000000355, 1.500000000000000000 ) ) ;
#7787=VERTEX_POINT ( 'NONE', #2561 ) ;
#7789=CARTESIAN_POINT ( 'NONE',  ( 9.038457413085614789, 1.187263343935665344E-16, -1.016831166589732938 ) ) ;
#7807=DIRECTION ( 'NONE',  ( 0.8528685319524443864, -0.4924038765061020118, 0.1736481776669307753 ) ) ;
#7819=CARTESIAN_POINT ( 'NONE',  ( -56.31355482043776561, 0.1467473176864696194, -1.355220493667176118 ) ) ;
#7820=DIRECTION ( 'NONE',  ( 0.000000000000000000, -0.000000000000000000, -1.000000000000000000 ) ) ;
#7823=ORIENTED_EDGE ( 'NONE', *, *, #22872, .F. ) ;
#7826=ADVANCED_FACE ( 'NONE', ( #6350 ), #27080, .T. ) ;
#7827=CARTESIAN_POINT ( 'NONE',  ( 108.0843398541090039, 18.64779751147721143, 4.615451654196422560 ) ) ;
#7832=ORIENTED_EDGE ( 'NONE', *, *, #9153, .F. ) ;
#7845=CARTESIAN_POINT ( 'NONE',  ( 108.2511990071235175, 19.57693511493973659, -2.786268106232082431 ) ) ;
#7846=ORIENTED_EDGE ( 'NONE', *, *, #5872, .T. ) ;
#7868=CARTESIAN_POINT ( 'NONE',  ( 108.0329590114848486, 18.36168870583371415, -4.580901328277968254 ) ) ;
#7881=DIRECTION ( 'NONE',  ( -0.000000000000000000, -0.000000000000000000, 1.000000000000000000 ) ) ;
#7889=FACE_OUTER_BOUND ( 'NONE', #2783, .T. ) ;
#7893=FACE_OUTER_BOUND ( 'NONE', #32325, .T. ) ;
#7899=B_SPLINE_CURVE_WITH_KNOTS ( 'NONE', 3,
 ( #31720, #2059, #12406, #11301, #19767, #22626, #20119, #22438, #27779, #12230 ),
 .UNSPECIFIED., .F., .F.,
 ( 4, 2, 2, 2, 4 ),
 ( -5.999999992670980713E-08, 0.0004826161079609663949, 0.0009652922159218595751, 0.001447968323882752647, 0.001930644431843645719 ),
 .UNSPECIFIED. ) ;
#7905=ORIENTED_EDGE ( 'NONE', *, *, #28906, .T. ) ;
#7906=CARTESIAN_POINT ( 'NONE',  ( -41.00655594638332246, -14.01733579338419311, 5.522895031406394040 ) ) ;
#7914=ORIENTED_EDGE ( 'NONE', *, *, #1345, .T. ) ;
#7923=CARTESIAN_POINT ( 'NONE',  ( 7.577572045913244736, 15.00000000000000178, -4.612695725900422872 ) ) ;
#7929=ADVANCED_FACE ( 'NONE', ( #32455 ), #22396, .T. ) ;
#7935=EDGE_CURVE ( 'NONE', #23082, #3747, #3848, .T. ) ;
#7936=EDGE_CURVE ( 'NONE', #32685, #10930, #32128, .T. ) ;
#7941=FACE_OUTER_BOUND ( 'NONE', #28836, .T. ) ;
#7957=CARTESIAN_POINT ( 'NONE',  ( -23.54713438637982748, 8.275374457817619600, 8.600000000000003197 ) ) ;
#7958=DIRECTION ( 'NONE',  ( 0.000000000000000000, 0.000000000000000000, 1.000000000000000000 ) ) ;
#7961=ORIENTED_EDGE ( 'NONE', *, *, #21321, .T. ) ;
#7966=ADVANCED_FACE ( 'NONE', ( #24404 ), #30524, .F. ) ;
#7983=ORIENTED_EDGE ( 'NONE', *, *, #25146, .T. ) ;
#7988=CARTESIAN_POINT ( 'NONE',  ( 9.256550853498360709, 0.1793056638302361061, 1.452626841518512402 ) ) ;
#7994=EDGE_CURVE ( 'NONE', #7241, #10104, #12693, .T. ) ;
#7998=CARTESIAN_POINT ( 'NONE',  ( 108.1156589233279135, 18.82219444680288234, -4.397958565568440115 ) ) ;
#7999=EDGE_LOOP ( 'NONE', ( #15733, #14030, #16637, #2241, #23227 ) ) ;
#8008=LINE ( 'NONE', #15362, #27195 ) ;
#8021=CIRCLE ( 'NONE', #1112, 0.4500000000000003442 ) ;
#8024=CARTESIAN_POINT ( 'NONE',  ( -21.32474236360683406, 4.412344421670777450, 2.134689491126265271 ) ) ;
#8037=CARTESIAN_POINT ( 'NONE',  ( 56.97280603064898941, -277.2763395528616002, 1.508259000770582059 ) ) ;
#8039=TOROIDAL_SURFACE ( 'NONE', #32075, 10.51999999999999957, 0.4500000000000000111 ) ;
#8064=AXIS2_PLACEMENT_3D ( 'NONE', #1097, #797, #6268 ) ;
#8066=CARTESIAN_POINT ( 'NONE',  ( -41.25643961544781035, -14.95835580254835051, 5.310642798856784808 ) ) ;
#8072=LINE ( 'NONE', #15270, #28908 ) ;
#8073=EDGE_CURVE ( 'NONE', #28455, #28296, #19866, .T. ) ;
#8082=CARTESIAN_POINT ( 'NONE',  ( -1.082681991931091714, 0.000000000000000000, -4.612695725900422872 ) ) ;
#8084=CARTESIAN_POINT ( 'NONE',  ( -30.51827900900859802, 4.402097243136377180, 5.049999999999999822 ) ) ;
#8087=CARTESIAN_POINT ( 'NONE',  ( 107.9618353151786181, 20.81780380167319677, 1.508259000770582059 ) ) ;
#8090=CIRCLE ( 'NONE', #630, 10.87687437218811581 ) ;
#8099=ORIENTED_EDGE ( 'NONE', *, *, #19166, .F. ) ;
#8102=EDGE_CURVE ( 'NONE', #1079, #4970, #27404, .T. ) ;
#8105=ORIENTED_EDGE ( 'NONE', *, *, #28059, .F. ) ;
#8127=CIRCLE ( 'NONE', #2266, 0.4500000000000008438 ) ;
#8131=ORIENTED_EDGE ( 'NONE', *, *, #21321, .F. ) ;
#8152=CARTESIAN_POINT ( 'NONE',  ( 11.90652295052632503, 20.12228623747235901, -4.612695725900421984 ) ) ;
#8158=AXIS2_PLACEMENT_3D ( 'NONE', #24725, #12175, #22375 ) ;
#8171=CIRCLE ( 'NONE', #8684, 0.4499999999999999001 ) ;
#8175=CIRCLE ( 'NONE', #31152, 0.4499999999999997891 ) ;
#8184=VERTEX_POINT ( 'NONE', #9596 ) ;
#8185=VERTEX_POINT ( 'NONE', #9784 ) ;
#8192=DIRECTION ( 'NONE',  ( -0.4922101374339078461, -0.7179542890850304504, -0.4922101374328877177 ) ) ;
#8197=DIRECTION ( 'NONE',  ( -0.1413077769430314268, 0.9899657126261587337, 0.000000000000000000 ) ) ;
#8200=DIRECTION ( 'NONE',  ( -8.326672684688674053E-17, -0.3746065934159164001, 0.9271838545667857590 ) ) ;
#8205=AXIS2_PLACEMENT_3D ( 'NONE', #26083, #26575, #10533 ) ;
#8221=DIRECTION ( 'NONE',  ( 0.4999999999999978351, 0.8660254037844398178, 0.000000000000000000 ) ) ;
#8253=CARTESIAN_POINT ( 'NONE',  ( 15.05218482013242820, 8.633077639384330482, -1.050000000000000044 ) ) ;
#8258=ORIENTED_EDGE ( 'NONE', *, *, #28059, .T. ) ;
#8261=CARTESIAN_POINT ( 'NONE',  ( 2.636537196392334970, 0.4393720697977969714, -1.497239384009418917 ) ) ;
#8267=FACE_OUTER_BOUND ( 'NONE', #18574, .T. ) ;
#8274=DIRECTION ( 'NONE',  ( 1.000000000000000000, 0.000000000000000000, 0.000000000000000000 ) ) ;
#8276=VERTEX_POINT ( 'NONE', #27161 ) ;
#8288=ORIENTED_EDGE ( 'NONE', *, *, #9523, .F. ) ;
#8299=CARTESIAN_POINT ( 'NONE',  ( 19.70572127725480982, 15.17811413760662198, 1.050000000000000044 ) ) ;
#8308=EDGE_CURVE ( 'NONE', #24602, #14512, #28946, .T. ) ;
#8322=ORIENTED_EDGE ( 'NONE', *, *, #21053, .F. ) ;
#8327=CARTESIAN_POINT ( 'NONE',  ( 9.192617927958238511, 0.08611596088385638226, 1.322472180770136729 ) ) ;
#8349=DIRECTION ( 'NONE',  ( -0.4999999999999977796, -0.8660254037844398178, 0.000000000000000000 ) ) ;
#8354=ORIENTED_EDGE ( 'NONE', *, *, #12424, .F. ) ;
#8362=ORIENTED_EDGE ( 'NONE', *, *, #23951, .F. ) ;
#8369=ORIENTED_EDGE ( 'NONE', *, *, #25298, .F. ) ;
#8371=CARTESIAN_POINT ( 'NONE',  ( 16.52153293541288548, 12.50053646836298427, 1.500000000000000000 ) ) ;
#8374=FACE_BOUND ( 'NONE', #15543, .T. ) ;
#8384=CARTESIAN_POINT ( 'NONE',  ( -19.58167718253661604, 5.525525355233698477, 1.499999999999569011 ) ) ;
#8389=CARTESIAN_POINT ( 'NONE',  ( 5.865515302491369098, 15.00000000000000000, -1.491740999229417941 ) ) ;
#8391=CARTESIAN_POINT ( 'NONE',  ( -56.71071518287084245, 0.7496615022747066259, 1.500000000000000000 ) ) ;
#8403=VERTEX_POINT ( 'NONE', #26489 ) ;
#8412=DIRECTION ( 'NONE',  ( 0.4999999999999978906, 0.8660254037844399289, -0.000000000000000000 ) ) ;
#8433=ORIENTED_EDGE ( 'NONE', *, *, #13414, .F. ) ;
#8449=EDGE_CURVE ( 'NONE', #30480, #13484, #16424, .T. ) ;
#8463=CARTESIAN_POINT ( 'NONE',  ( 8.901201215455847304, 15.00000000000002132, -5.396302277755718357 ) ) ;
#8473=EDGE_CURVE ( 'NONE', #12070, #18469, #20261, .T. ) ;
#8475=CARTESIAN_POINT ( 'NONE',  ( 12.27700767694853390, 19.86581740147262209, 5.412820279296879811 ) ) ;
#8484=CARTESIAN_POINT ( 'NONE',  ( 13.62547635268498070, 21.94000000000005102, -1.491740999229417941 ) ) ;
#8492=EDGE_LOOP ( 'NONE', ( #21193, #12523, #5550, #21603, #1427, #16188 ) ) ;
#8510=DIRECTION ( 'NONE',  ( -1.000000000000000000, 0.000000000000000000, 0.000000000000000000 ) ) ;
#8513=ADVANCED_FACE ( 'NONE', ( #14097 ), #4055, .T. ) ;
#8521=CARTESIAN_POINT ( 'NONE',  ( 16.18510121775752353, 12.06909784052177237, 1.500000000000000000 ) ) ;
#8527=CARTESIAN_POINT ( 'NONE',  ( -24.45088912031106076, 4.048764718688453002, 2.144778699193373939 ) ) ;
#8532=CARTESIAN_POINT ( 'NONE',  ( 79.17573959169237696, 22.98125563777605151, 4.629213727441585213 ) ) ;
#8542=DIRECTION ( 'NONE',  ( 0.4999999999999982236, 0.8660254037844398178, 0.000000000000000000 ) ) ;
#8567=LINE ( 'NONE', #18776, #30652 ) ;
#8588=ORIENTED_EDGE ( 'NONE', *, *, #21699, .F. ) ;
#8603=CIRCLE ( 'NONE', #7530, 0.4499999999999999001 ) ;
#8615=AXIS2_PLACEMENT_3D ( 'NONE', #470, #10651, #28564 ) ;
#8620=CYLINDRICAL_SURFACE ( 'NONE', #14521, 0.4499999999999990119 ) ;
#8625=VECTOR ( 'NONE', #5795, 1000.000000000000000 ) ;
#8633=VECTOR ( 'NONE', #24598, 1000.000000000000000 ) ;
#8634=CONICAL_SURFACE ( 'NONE', #1181, 10.97000000000001485, 0.1745329251994333364 ) ;
#8644=CARTESIAN_POINT ( 'NONE',  ( 8.007433738499960540, 15.00000000000002132, 5.412820279296878923 ) ) ;
#8645=EDGE_LOOP ( 'NONE', ( #4140, #11588, #30294, #28596 ) ) ;
#8647=CARTESIAN_POINT ( 'NONE',  ( 25.98173092684325880, 19.04622029248877269, -1.226162093883974125 ) ) ;
#8669=AXIS2_PLACEMENT_3D ( 'NONE', #29790, #27452, #17055 ) ;
#8675=ORIENTED_EDGE ( 'NONE', *, *, #15869, .T. ) ;
#8684=AXIS2_PLACEMENT_3D ( 'NONE', #13515, #987, #490 ) ;
#8690=( GEOMETRIC_REPRESENTATION_CONTEXT ( 3 ) GLOBAL_UNCERTAINTY_ASSIGNED_CONTEXT ( ( #2816 ) ) GLOBAL_UNIT_ASSIGNED_CONTEXT ( ( #25162, #5769, #10955 ) ) REPRESENTATION_CONTEXT ( 'NONE', 'WORKASPACE' ) );
#8697=EDGE_LOOP ( 'NONE', ( #11474, #19122, #17865, #24315 ) ) ;
#8699=CARTESIAN_POINT ( 'NONE',  ( 9.923352537987668143, 1.153138503447697749, 1.050000000000000044 ) ) ;
#8701=CARTESIAN_POINT ( 'NONE',  ( -50.81000000000000227, -10.96999999999998643, 9.000000000000000000 ) ) ;
#8702=CARTESIAN_POINT ( 'NONE',  ( -56.77537022611499395, 0.4514244267945254907, 2.028141679927229379 ) ) ;
#8704=EDGE_CURVE ( 'NONE', #22357, #8954, #12414, .T. ) ;
#8708=CARTESIAN_POINT ( 'NONE',  ( -28.62968855526470691, 6.563152521750583723, 2.075789994699551499 ) ) ;
#8711=CARTESIAN_POINT ( 'NONE',  ( -21.88206647074803968, 4.362210445734582720, 1.500000000000000000 ) ) ;
#8715=EDGE_CURVE ( 'NONE', #29681, #32685, #26283, .T. ) ;
#8734=ORIENTED_EDGE ( 'NONE', *, *, #19166, .T. ) ;
#8749=DIRECTION ( 'NONE',  ( -1.000000000000000000, 0.000000000000000000, 0.000000000000000000 ) ) ;
#8750=DIRECTION ( 'NONE',  ( -1.000000000000000000, 0.000000000000000000, 0.000000000000000000 ) ) ;
#8756=VECTOR ( 'NONE', #14164, 1000.000000000000000 ) ;
#8764=CARTESIAN_POINT ( 'NONE',  ( 16.36487458112949511, 19.37645981759117575, -4.612695725900422872 ) ) ;
#8767=CARTESIAN_POINT ( 'NONE',  ( 17.32050807568873552, 10.00000000000002309, -1.491740999229417941 ) ) ;
#8770=ORIENTED_EDGE ( 'NONE', *, *, #2240, .F. ) ;
#8786=CARTESIAN_POINT ( 'NONE',  ( -56.77633738153843979, 0.4614026863384942390, 1.995096760105839362 ) ) ;
#8794=CARTESIAN_POINT ( 'NONE',  ( 108.3721138249345728, 20.25023653045810690, -2.520993486554220286 ) ) ;
#8804=CARTESIAN_POINT ( 'NONE',  ( 7.577572045913208321, 15.00000000000002132, -4.612695725900422872 ) ) ;
#8815=CARTESIAN_POINT ( 'NONE',  ( 22.75143042797981252, 17.32866418988431079, -1.049999999999999822 ) ) ;
#8825=CARTESIAN_POINT ( 'NONE',  ( -23.54713438637982748, 12.65740340961132304, 3.359978791489319772 ) ) ;
#8826=DIRECTION ( 'NONE',  ( -0.000000000000000000, -0.000000000000000000, -1.000000000000000000 ) ) ;
#8848=CARTESIAN_POINT ( 'NONE',  ( -50.81000000000000227, -10.96999999999998643, 5.700000000000000178 ) ) ;
#8861=ORIENTED_EDGE ( 'NONE', *, *, #1519, .F. ) ;
#8881=VERTEX_POINT ( 'NONE', #8389 ) ;
#8887=DIRECTION ( 'NONE',  ( -0.000000000000000000, -0.3746065934159164001, 0.9271838545667856479 ) ) ;
#8888=EDGE_CURVE ( 'NONE', #6067, #18014, #11585, .T. ) ;
#8891=CARTESIAN_POINT ( 'NONE',  ( 17.20462742525712585, 13.34747051462077927, -1.500000000000000000 ) ) ;
#8907=EDGE_LOOP ( 'NONE', ( #22458, #7027, #17259, #1267 ) ) ;
#8913=ORIENTED_EDGE ( 'NONE', *, *, #20438, .F. ) ;
#8923=FACE_OUTER_BOUND ( 'NONE', #31110, .T. ) ;
#8948=CARTESIAN_POINT ( 'NONE',  ( -41.34821589589207491, -14.97033716811276527, 5.482725084223756262 ) ) ;
#8954=VERTEX_POINT ( 'NONE', #31457 ) ;
#8962=CARTESIAN_POINT ( 'NONE',  ( 9.282537329960032224, 0.2172754300400924765, 1.041239158277174504 ) ) ;
#8970=DIRECTION ( 'NONE',  ( -1.000000000000000000, 0.000000000000000000, 0.000000000000000000 ) ) ;
#8973=DIRECTION ( 'NONE',  ( 0.2880220749472531261, 0.1662896225033515807, -0.9430753128943476504 ) ) ;
#9010=CARTESIAN_POINT ( 'NONE',  ( 13.49488892923315220, 21.89889427266717092, 1.242426148748663195 ) ) ;
#9015=CARTESIAN_POINT ( 'NONE',  ( -23.54713438637982748, 4.195786794269684705, 1.499999999999999112 ) ) ;
#9021=ORIENTED_EDGE ( 'NONE', *, *, #3048, .T. ) ;
#9042=CARTESIAN_POINT ( 'NONE',  ( 11.28452421127990135, 4.182904784596867209, -1.500000000000000000 ) ) ;
#9051=LINE ( 'NONE', #2057, #4377 ) ;
#9059=DIRECTION ( 'NONE',  ( -0.4809547266710045288, -0.000000000000000000, -0.8767454310646958238 ) ) ;
#9096=( BOUNDED_SURFACE ( )  B_SPLINE_SURFACE ( 3, 2, ( 
 ( #13168, #8327, #28872 ),
 ( #23707, #26212, #3325 ),
 ( #30914, #7988, #15843 ),
 ( #18181, #16169, #13654 ) ),
 .UNSPECIFIED., .F., .F., .F. ) 
 B_SPLINE_SURFACE_WITH_KNOTS ( ( 4, 4 ),
 ( 3, 3 ),
 ( 0.0001475438429531535209, 0.0001830289614101955511 ),
 ( 0.000000000000000000, 1.000000000000000000 ),
 .UNSPECIFIED. ) 
 GEOMETRIC_REPRESENTATION_ITEM ( )  RATIONAL_B_SPLINE_SURFACE ( (
 ( 1.000000000000000000, 0.8123215895924797980, 1.000000000000000000),
 ( 1.000000000000000000, 0.7824045309858685959, 1.000000000000000000),
 ( 1.000000000000000000, 0.7465390509822480425, 1.000000000000000000),
 ( 1.000000000000000000, 0.7071067812051371471, 1.000000000000000000) ) ) 
 REPRESENTATION_ITEM ( '' )  SURFACE ( )  );
#9105=CARTESIAN_POINT ( 'NONE',  ( -40.82415311671282865, -13.09326638694065359, 5.845147494867474869 ) ) ;
#9106=VERTEX_POINT ( 'NONE', #5192 ) ;
#9108=EDGE_LOOP ( 'NONE', ( #23287, #24232, #8913, #2475 ) ) ;
#9117=AXIS2_PLACEMENT_3D ( 'NONE', #14856, #9361, #4685 ) ;
#9123=ORIENTED_EDGE ( 'NONE', *, *, #4857, .T. ) ;
#9125=CARTESIAN_POINT ( 'NONE',  ( 9.127968561342536091, 0.03517121848165041115, 1.257822814154217816 ) ) ;
#9128=AXIS2_PLACEMENT_3D ( 'NONE', #1269, #13765, #18633 ) ;
#9139=EDGE_CURVE ( 'NONE', #10337, #21393, #30627, .T. ) ;
#9152=CARTESIAN_POINT ( 'NONE',  ( 107.7451628514262723, 16.75912612768599885, -1.277591108513651097 ) ) ;
#9153=EDGE_CURVE ( 'NONE', #16073, #4552, #7707, .T. ) ;
#9156=EDGE_LOOP ( 'NONE', ( #31127, #11678, #8354, #23610 ) ) ;
#9159=EDGE_CURVE ( 'NONE', #20999, #23780, #845, .T. ) ;
#9174=( BOUNDED_CURVE ( )  B_SPLINE_CURVE ( 3, ( #17960, #20788, #8261, #30848 ),
 .UNSPECIFIED., .F., .F. ) 
 B_SPLINE_CURVE_WITH_KNOTS ( ( 4, 4 ),
 ( 4.712388980384688786, 4.894398194314031336 ),
 .UNSPECIFIED. ) 
 CURVE ( )  GEOMETRIC_REPRESENTATION_ITEM ( )  RATIONAL_B_SPLINE_CURVE ( ( 1.000000000000000000, 0.9972412918903137413, 0.9972412918903137413, 1.000000000000000000 ) ) 
 REPRESENTATION_ITEM ( '' )  );
#9180=CARTESIAN_POINT ( 'NONE',  ( -59.04504500748983986, -4.696780627829411969, 5.309652175818544428 ) ) ;
#9187=CARTESIAN_POINT ( 'NONE',  ( 14.84491886980558029, 10.18391468479282302, 1.500000000000000222 ) ) ;
#9201=DIRECTION ( 'NONE',  ( 0.4999999999999978351, 0.8660254037844399289, 0.000000000000000000 ) ) ;
#9203=CIRCLE ( 'NONE', #12438, 0.4500000000000000111 ) ;
#9209=ORIENTED_EDGE ( 'NONE', *, *, #30795, .F. ) ;
#9223=CARTESIAN_POINT ( 'NONE',  ( 10.13996510774097004, 2.320984940005466513, -1.500000000000000000 ) ) ;
#9224=CARTESIAN_POINT ( 'NONE',  ( 8.960941058736720422, 0.001013528757996738161, -1.090795311548453661 ) ) ;
#9232=AXIS2_PLACEMENT_3D ( 'NONE', #5039, #18052, #8349 ) ;
#9237=B_SPLINE_CURVE_WITH_KNOTS ( 'NONE', 3,
 ( #28218, #24889, #2000, #14836, #25036, #11146, #10655, #473 ),
 .UNSPECIFIED., .F., .F.,
 ( 4, 2, 2, 4 ),
 ( 4.445333154581480097E-17, 0.0001981427792172239224, 0.0003962855584344033926, 0.0007925711168687612487 ),
 .UNSPECIFIED. ) ;
#9248=VECTOR ( 'NONE', #6858, 1000.000000000000000 ) ;
#9268=CARTESIAN_POINT ( 'NONE',  ( -40.27879340802675046, -12.50360960397076404, 5.500000000000000000 ) ) ;
#9270=CARTESIAN_POINT ( 'NONE',  ( -56.55840490054024627, 0.08005089788804982398, 1.499999999999999112 ) ) ;
#9272=AXIS2_PLACEMENT_3D ( 'NONE', #9726, #23276, #30819 ) ;
#9278=EDGE_CURVE ( 'NONE', #18474, #2818, #29086, .T. ) ;
#9280=FACE_OUTER_BOUND ( 'NONE', #14995, .T. ) ;
#9295=VERTEX_POINT ( 'NONE', #847 ) ;
#9299=ORIENTED_EDGE ( 'NONE', *, *, #5684, .T. ) ;
#9305=VERTEX_POINT ( 'NONE', #11024 ) ;
#9317=DIRECTION ( 'NONE',  ( -0.4999999999999982236, -0.8660254037844397068, 0.000000000000000000 ) ) ;
#9322=CARTESIAN_POINT ( 'NONE',  ( -26.97533405509228999, 5.021485087457022267, 2.117863293439079531 ) ) ;
#9335=CARTESIAN_POINT ( 'NONE',  ( 56.97280603064898941, -277.2763395528616002, 0.000000000000000000 ) ) ;
#9343=EDGE_CURVE ( 'NONE', #14512, #18387, #3388, .T. ) ;
#9347=DIRECTION ( 'NONE',  ( 0.8660254037844399289, -0.4999999999999978906, 0.000000000000000000 ) ) ;
#9357=ORIENTED_EDGE ( 'NONE', *, *, #21003, .T. ) ;
#9359=ORIENTED_EDGE ( 'NONE', *, *, #29310, .F. ) ;
#9361=DIRECTION ( 'NONE',  ( -0.000000000000000000, -0.000000000000000000, -1.000000000000000000 ) ) ;
#9364=CARTESIAN_POINT ( 'NONE',  ( -16.89591873025416646, 10.24026612823045035, 1.500000000000111910 ) ) ;
#9365=CARTESIAN_POINT ( 'NONE',  ( -23.54713438637982748, 18.46223496596754288, 1.773004750130224627 ) ) ;
#9366=DIRECTION ( 'NONE',  ( -0.000000000000000000, 0.000000000000000000, 1.000000000000000000 ) ) ;
#9373=EDGE_CURVE ( 'NONE', #29856, #18979, #29529, .T. ) ;
#9378=( BOUNDED_SURFACE ( )  B_SPLINE_SURFACE ( 3, 1, ( 
 ( #26644, #18808 ),
 ( #6109, #13919 ),
 ( #16292, #26502 ),
 ( #3603, #10783 ) ),
 .UNSPECIFIED., .F., .F., .F. ) 
 B_SPLINE_SURFACE_WITH_KNOTS ( ( 4, 4 ),
 ( 2, 2 ),
 ( 0.000000000000000000, 1.000000000000000000 ),
 ( 0.000000000000000000, 1.000000000000000000 ),
 .UNSPECIFIED. ) 
 GEOMETRIC_REPRESENTATION_ITEM ( )  RATIONAL_B_SPLINE_SURFACE ( (
 ( 1.000000000000000000, 1.000000000000000000),
 ( 0.6539698177806696489, 0.6539698177806696489),
 ( 0.6539698177806696489, 0.6539698177806696489),
 ( 1.000000000000000000, 1.000000000000000000) ) ) 
 REPRESENTATION_ITEM ( '' )  SURFACE ( )  );
#9386=DIRECTION ( 'NONE',  ( -0.000000000000000000, -0.000000000000000000, -1.000000000000000000 ) ) ;
#9396=ORIENTED_EDGE ( 'NONE', *, *, #16311, .F. ) ;
#9401=FACE_OUTER_BOUND ( 'NONE', #9108, .T. ) ;
#9411=DIRECTION ( 'NONE',  ( -1.000000000000000000, 0.000000000000000000, 0.000000000000000000 ) ) ;
#9419=ORIENTED_EDGE ( 'NONE', *, *, #3629, .T. ) ;
#9441=ORIENTED_EDGE ( 'NONE', *, *, #7676, .F. ) ;
#9456=CARTESIAN_POINT ( 'NONE',  ( 13.78291618757655712, 7.586155849071186452, -1.050000000000000044 ) ) ;
#9458=CARTESIAN_POINT ( 'NONE',  ( -56.71071518287084245, 0.7496615022747066259, 1.500000000000000000 ) ) ;
#9459=CARTESIAN_POINT ( 'NONE',  ( 16.36487458112951643, 19.37645981759113312, 4.629213727441584325 ) ) ;
#9462=CARTESIAN_POINT ( 'NONE',  ( 8.870145747188287189, 0.000000000000000000, 1.000000000000000000 ) ) ;
#9469=LINE ( 'NONE', #17165, #28858 ) ;
#9472=DIRECTION ( 'NONE',  ( -8.326672684688674053E-17, -0.3746065934159164001, 0.9271838545667857590 ) ) ;
#9474=CARTESIAN_POINT ( 'NONE',  ( -23.54713438637982748, 18.90773822806172433, 2.000000000000000000 ) ) ;
#9489=ORIENTED_EDGE ( 'NONE', *, *, #28864, .F. ) ;
#9511=DIRECTION ( 'NONE',  ( 1.000000000000000000, 0.000000000000000000, 0.000000000000000000 ) ) ;
#9513=CARTESIAN_POINT ( 'NONE',  ( -17.31779044994511096, 15.08866638674220084, 1.500000000000000000 ) ) ;
#9523=EDGE_CURVE ( 'NONE', #17424, #25915, #17264, .T. ) ;
#9542=CARTESIAN_POINT ( 'NONE',  ( 25.73836023340754409, 18.89938647777091418, -1.500000000000000000 ) ) ;
#9562=EDGE_CURVE ( 'NONE', #2818, #30095, #708, .T. ) ;
#9564=ORIENTED_EDGE ( 'NONE', *, *, #15452, .F. ) ;
#9565=CARTESIAN_POINT ( 'NONE',  ( 108.4602224094689547, 20.74085989589476497, 1.491071325085251864 ) ) ;
#9568=ORIENTED_EDGE ( 'NONE', *, *, #12708, .F. ) ;
#9595=B_SPLINE_CURVE_WITH_KNOTS ( 'NONE', 3,
 ( #3181, #23554, #19199, #14503, #26904, #27057, #24224, #21866, #32425, #3836 ),
 .UNSPECIFIED., .F., .F.,
 ( 4, 2, 2, 2, 4 ),
 ( 0.000000000000000000, 0.0009905218478212184617, 0.001981043695642436923, 0.002971565543463655385, 0.003962087391284873847 ),
 .UNSPECIFIED. ) ;
#9596=CARTESIAN_POINT ( 'NONE',  ( -23.54713438637982748, 10.61651369059875272, 9.545881648375194928 ) ) ;
#9630=CIRCLE ( 'NONE', #22457, 12.49867430706168570 ) ;
#9633=DIRECTION ( 'NONE',  ( 0.4809547266710045843, 0.000000000000000000, -0.8767454310646957127 ) ) ;
#9635=AXIS2_PLACEMENT_3D ( 'NONE', #7957, #601, #2623 ) ;
#9639=CARTESIAN_POINT ( 'NONE',  ( -56.63828291323059716, 0.1160565766146929301, -1.359003754613687720 ) ) ;
#9646=CARTESIAN_POINT ( 'NONE',  ( -23.54713438637982748, 3.520075575296777171, 1.500000000000000000 ) ) ;
#9654=AXIS2_PLACEMENT_3D ( 'NONE', #25483, #14932, #24978 ) ;
#9660=AXIS2_PLACEMENT_3D ( 'NONE', #5544, #15725, #18900 ) ;
#9663=B_SPLINE_CURVE_WITH_KNOTS ( 'NONE', 3,
 ( #23401, #27755, #20423, #25935, #15376, #10384, #20593, #8024, #30802, #20901, #12556, #18223, #23256, #17912, #30640, #18062, #25763, #3043, #7367, #7719, #28251, #4863, #15047, #28103, #13198, #25583, #5361, #15546, #28436, #2892, #25267, #22759, #5548, #359, #13057, #32967, #10036, #22910, #20247, #7527, #17733, #16, #27942, #5050, #15227, #2538 ),
 .UNSPECIFIED., .F., .F.,
 ( 4, 2, 2, 2, 2, 2, 2, 2, 2, 2, 2, 2, 2, 2, 2, 2, 2, 2, 2, 2, 2, 2, 4 ),
 ( 0.02194255756287339515, 0.02262812102983364701, 0.02331368449679389887, 0.02399924796375415073, 0.02468481143071440259, 0.02605593836463490631, 0.02674150183159515470, 0.02742706529855539963, 0.02879819223247589641, 0.03016931916639639319, 0.03085488263335664505, 0.03154044610031689344, 0.03291157303423739022, 0.03428269996815789394, 0.03565382690207839073, 0.03702495383599889445, 0.03839608076991939123, 0.03908164423687963962, 0.03976720770383988801, 0.04113833463776038479, 0.04182389810472063318, 0.04250946157168088158, 0.04388058850560139224 ),
 .UNSPECIFIED. ) ;
#9675=CIRCLE ( 'NONE', #28373, 297.9387600756452343 ) ;
#9689=CARTESIAN_POINT ( 'NONE',  ( -20.12358435285846170, 17.65690804191476460, 1.499999999999999778 ) ) ;
#9691=VECTOR ( 'NONE', #250, 1000.000000000000000 ) ;
#9698=CARTESIAN_POINT ( 'NONE',  ( -45.71000000000000085, -10.96999999999998643, 5.700000000000000178 ) ) ;
#9700=CARTESIAN_POINT ( 'NONE',  ( 2.382865613620175349, 0.000000000000000000, 1.508259000770581615 ) ) ;
#9701=VERTEX_POINT ( 'NONE', #5492 ) ;
#9721=CARTESIAN_POINT ( 'NONE',  ( 9.192617927958343316, 0.08611596088385929659, -1.322472180770059014 ) ) ;
#9725=ORIENTED_EDGE ( 'NONE', *, *, #18364, .T. ) ;
#9726=CARTESIAN_POINT ( 'NONE',  ( -56.32770133515838040, 0.5000000000000000000, -1.050000000000000044 ) ) ;
#9735=CARTESIAN_POINT ( 'NONE',  ( -2.506063600758156262, 0.4999999999999998890, 1.500000000000000000 ) ) ;
#9738=CARTESIAN_POINT ( 'NONE',  ( 45.78962651942645579, 26.61627915917710041, 1.508259000770581837 ) ) ;
#9739=CIRCLE ( 'NONE', #12847, 8.025310301077736241 ) ;
#9741=CIRCLE ( 'NONE', #12941, 0.9999999999999991118 ) ;
#9749=ORIENTED_EDGE ( 'NONE', *, *, #28864, .T. ) ;
#9765=FACE_OUTER_BOUND ( 'NONE', #6864, .T. ) ;
#9767=CARTESIAN_POINT ( 'NONE',  ( -56.73266014122250311, 0.2590449313022686884, -1.045342064611400446 ) ) ;
#9773=CARTESIAN_POINT ( 'NONE',  ( 107.9424804437600756, 20.70775667334615378, 1.742830623350447361 ) ) ;
#9784=CARTESIAN_POINT ( 'NONE',  ( -30.08790297335274389, 4.402097243136376292, 5.181439978443226124 ) ) ;
#9792=DIRECTION ( 'NONE',  ( -0.4809547266710039182, 0.000000000000000000, 0.8767454310646960458 ) ) ;
#9797=EDGE_LOOP ( 'NONE', ( #19528, #11633, #21261, #17938 ) ) ;
#9808=CARTESIAN_POINT ( 'NONE',  ( -56.76324651597856530, 0.6586745643427850405, 1.499999999999941158 ) ) ;
#9821=CARTESIAN_POINT ( 'NONE',  ( 79.92595492699416582, 21.43178168691304819, -1.491740999229419273 ) ) ;
#9828=CARTESIAN_POINT ( 'NONE',  ( -56.31962101169892065, 0.2221239435922897909, -1.416967151343360376 ) ) ;
#9835=CARTESIAN_POINT ( 'NONE',  ( -29.41021809322157310, 5.485000000000014531, 1.500000000000000000 ) ) ;
#9848=B_SPLINE_CURVE_WITH_KNOTS ( 'NONE', 3,
 ( #20038, #126, #23007, #33051, #22702, #10124 ),
 .UNSPECIFIED., .F., .F.,
 ( 4, 2, 4 ),
 ( -6.833360019735199612E-06, 0.0003895853402124996290, 0.0007860040404447344534 ),
 .UNSPECIFIED. ) ;
#9852=ORIENTED_EDGE ( 'NONE', *, *, #19013, .T. ) ;
#9862=DIRECTION ( 'NONE',  ( -0.000000000000000000, -0.000000000000000000, -1.000000000000000000 ) ) ;
#9868=CARTESIAN_POINT ( 'NONE',  ( 8.930755659325141593, 0.5000000000000008882, 1.500000000000000000 ) ) ;
#9883=CARTESIAN_POINT ( 'NONE',  ( 107.4928421713820086, 18.16941992634724201, -4.994310381140683930 ) ) ;
#9888=ORIENTED_EDGE ( 'NONE', *, *, #29350, .F. ) ;
#9897=CARTESIAN_POINT ( 'NONE',  ( 21.26379237082032247, 16.93099014934048441, 1.500000000000000222 ) ) ;
#9906=CARTESIAN_POINT ( 'NONE',  ( 107.6996442589674103, 19.35565155597527109, -4.612695725900422872 ) ) ;
#9918=CARTESIAN_POINT ( 'NONE',  ( 108.3721138247593814, 20.25023653042131144, 2.537511488057705655 ) ) ;
#9925=EDGE_LOOP ( 'NONE', ( #1661, #12177, #21382 ) ) ;
#9927=DIRECTION ( 'NONE',  ( -0.000000000000000000, 0.3746065934159164001, -0.9271838545667856479 ) ) ;
#9931=ORIENTED_EDGE ( 'NONE', *, *, #30900, .F. ) ;
#9932=CARTESIAN_POINT ( 'NONE',  ( 9.302055952193859056, 0.2457637073201327793, 1.049999999999999822 ) ) ;
#9935=CARTESIAN_POINT ( 'NONE',  ( 107.8351701702616197, 20.11025589396474444, 3.017643035989555411 ) ) ;
#9968=ADVANCED_BREP_SHAPE_REPRESENTATION ( '', ( #21573, #2865 ), #8690 ) ;
#9981=CARTESIAN_POINT ( 'NONE',  ( -56.42282546612280925, 0.008325373391011687066, -1.141662625959267707 ) ) ;
#9988=CARTESIAN_POINT ( 'NONE',  ( 108.0119342731779284, 18.24461466697532686, 4.475534541203948891 ) ) ;
#9993=( BOUNDED_CURVE ( )  B_SPLINE_CURVE ( 3, ( #9735, #11737, #19274, #22129 ),
 .UNSPECIFIED., .F., .F. ) 
 B_SPLINE_CURVE_WITH_KNOTS ( ( 4, 4 ),
 ( 4.712388980384689674, 6.283185307179586232 ),
 .UNSPECIFIED. ) 
 CURVE ( )  GEOMETRIC_REPRESENTATION_ITEM ( )  RATIONAL_B_SPLINE_CURVE ( ( 1.000000000000000000, 0.8047378541243649375, 0.8047378541243649375, 1.000000000000000000 ) ) 
 REPRESENTATION_ITEM ( '' )  );
#10003=ORIENTED_EDGE ( 'NONE', *, *, #12400, .T. ) ;
#10012=CARTESIAN_POINT ( 'NONE',  ( 107.8941083086932196, 17.58851320481917213, -3.054550927624524626 ) ) ;
#10013=CARTESIAN_POINT ( 'NONE',  ( -37.80541082197543545, 18.90773822806172433, 1.500000000000000222 ) ) ;
#10029=LINE ( 'NONE', #7519, #32725 ) ;
#10034=CARTESIAN_POINT ( 'NONE',  ( 107.9828715491437094, 18.08278195199847715, -4.992355932524864315 ) ) ;
#10036=CARTESIAN_POINT ( 'NONE',  ( -19.57725484400670624, 17.02906325615838767, 1.807551478622768215 ) ) ;
#10046=CARTESIAN_POINT ( 'NONE',  ( 25.25352962636571874, 18.67320858063204270, -1.500000000000117906 ) ) ;
#10056=CARTESIAN_POINT ( 'NONE',  ( -60.31029867951531998, -5.485000000000005649, 1.500000000000000000 ) ) ;
#10059=( BOUNDED_SURFACE ( )  B_SPLINE_SURFACE ( 3, 2, ( 
 ( #19782, #14254, #14761 ),
 ( #26983, #12096, #27639 ),
 ( #24958, #9918, #12244 ),
 ( #27132, #9565, #29991 ) ),
 .UNSPECIFIED., .F., .F., .F. ) 
 B_SPLINE_SURFACE_WITH_KNOTS ( ( 4, 4 ),
 ( 3, 3 ),
 ( 0.000000000000000000, 0.003477590727847893522 ),
 ( 0.000000000000000000, 1.000000000000000000 ),
 .UNSPECIFIED. ) 
 GEOMETRIC_REPRESENTATION_ITEM ( )  RATIONAL_B_SPLINE_SURFACE ( (
 ( 1.000000000000000000, 0.7044453589051415943, 1.000000000000000000),
 ( 1.000000000000000000, 0.7044500455793978322, 1.000000000000000000),
 ( 1.000000000000000000, 0.7044547099242082222, 1.000000000000000000),
 ( 1.000000000000000000, 0.7044593522111542994, 1.000000000000000000) ) ) 
 REPRESENTATION_ITEM ( '' )  SURFACE ( )  );
#10061=CARTESIAN_POINT ( 'NONE',  ( 15.28872660057386845, 20.76088595412476678, 4.629213727441584325 ) ) ;
#10088=CARTESIAN_POINT ( 'NONE',  ( -30.51827900900860158, 4.845260731991870351, 5.128141679950118714 ) ) ;
#10093=DIRECTION ( 'NONE',  ( 0.000000000000000000, 5.782411586589358033E-15, -1.000000000000000000 ) ) ;
#10103=CARTESIAN_POINT ( 'NONE',  ( 0.000000000000000000, 0.5000000000000000000, 1.000000000000000000 ) ) ;
#10104=VERTEX_POINT ( 'NONE', #26460 ) ;
#10113=VERTEX_POINT ( 'NONE', #8391 ) ;
#10124=CARTESIAN_POINT ( 'NONE',  ( 107.1772993348646281, 16.40207914262226296, -1.491740999229418829 ) ) ;
#10125=LINE ( 'NONE', #20349, #4875 ) ;
#10130=CARTESIAN_POINT ( 'NONE',  ( -56.37198679362065690, 0.002873736814589079782, -1.088637985230049621 ) ) ;
#10141=FACE_OUTER_BOUND ( 'NONE', #1800, .T. ) ;
#10143=CARTESIAN_POINT ( 'NONE',  ( 107.9622325421415212, 20.81773585569407459, 1.508259000770582059 ) ) ;
#10146=DIRECTION ( 'NONE',  ( -0.000000000000000000, -0.000000000000000000, -1.000000000000000000 ) ) ;
#10147=EDGE_LOOP ( 'NONE', ( #17745, #28750, #1844, #21459 ) ) ;
#10160=DIRECTION ( 'NONE',  ( 0.4999999999999978906, 0.8660254037844398178, -0.000000000000000000 ) ) ;
#10166=ORIENTED_EDGE ( 'NONE', *, *, #16396, .T. ) ;
#10176=CARTESIAN_POINT ( 'NONE',  ( 107.7448119175622736, 19.60714374054428788, -4.075483440861804141 ) ) ;
#10185=CIRCLE ( 'NONE', #23005, 297.9387600756452912 ) ;
#10214=CARTESIAN_POINT ( 'NONE',  ( 26.23173791223905837, 19.12152673998438601, 1.500000000000000000 ) ) ;
#10220=EDGE_CURVE ( 'NONE', #8881, #8276, #14555, .T. ) ;
#10224=CARTESIAN_POINT ( 'NONE',  ( -24.68599574654897211, 18.35914888252920463, 1.775473033787586363 ) ) ;
#10247=EDGE_CURVE ( 'NONE', #28172, #29681, #22255, .T. ) ;
#10249=FACE_OUTER_BOUND ( 'NONE', #32607, .T. ) ;
#10264=AXIS2_PLACEMENT_3D ( 'NONE', #29187, #6274, #22281 ) ;
#10268=AXIS2_PLACEMENT_3D ( 'NONE', #13077, #5717, #13372 ) ;
#10273=PLANE ( 'NONE',  #25329 ) ;
#10281=VERTEX_POINT ( 'NONE', #4549 ) ;
#10298=VERTEX_POINT ( 'NONE', #29627 ) ;
#10301=CIRCLE ( 'NONE', #8158, 3.250000000000002665 ) ;
#10311=EDGE_CURVE ( 'NONE', #28455, #9295, #1724, .T. ) ;
#10324=CARTESIAN_POINT ( 'NONE',  ( -56.31570190716953306, 0.1700137493292786239, -1.377075300692550908 ) ) ;
#10331=CARTESIAN_POINT ( 'NONE',  ( 107.5865239920538698, 18.70770258647741358, 5.148154074928823043 ) ) ;
#10336=AXIS2_PLACEMENT_3D ( 'NONE', #21450, #26969, #8750 ) ;
#10337=VERTEX_POINT ( 'NONE', #16675 ) ;
#10363=ORIENTED_EDGE ( 'NONE', *, *, #9159, .F. ) ;
#10371=LINE ( 'NONE', #3031, #10843 ) ;
#10383=ORIENTED_EDGE ( 'NONE', *, *, #7994, .T. ) ;
#10384=CARTESIAN_POINT ( 'NONE',  ( -21.97225858583376734, 4.201001019271233261, 2.140550196716301201 ) ) ;
#10396=LINE ( 'NONE', #26096, #16679 ) ;
#10397=DIRECTION ( 'NONE',  ( -0.000000000000000000, -0.000000000000000000, -1.000000000000000000 ) ) ;
#10404=CARTESIAN_POINT ( 'NONE',  ( -23.54713438637982748, 18.46223496596754288, 1.773004750130224627 ) ) ;
#10409=LINE ( 'NONE', #20619, #167 ) ;
#10421=CARTESIAN_POINT ( 'NONE',  ( -40.38425638691331443, -12.81449853570765995, 5.500000000000000888 ) ) ;
#10451=CARTESIAN_POINT ( 'NONE',  ( 12.62440642364078514, 21.58543435044974856, -1.499999999999994893 ) ) ;
#10469=( BOUNDED_CURVE ( )  B_SPLINE_CURVE ( 3, ( #9835, #30086, #27394, #24878 ),
 .UNSPECIFIED., .F., .F. ) 
 B_SPLINE_CURVE_WITH_KNOTS ( ( 4, 4 ),
 ( 5.261730470397909976, 7.304640143961260712 ),
 .UNSPECIFIED. ) 
 CURVE ( )  GEOMETRIC_REPRESENTATION_ITEM ( )  RATIONAL_B_SPLINE_CURVE ( ( 1.000000000000000000, 0.6814171464877621931, 0.6814171464877621931, 1.000000000000000000 ) ) 
 REPRESENTATION_ITEM ( '' )  );
#10478=CARTESIAN_POINT ( 'NONE',  ( 7.577572045913244736, 15.00000000000000178, 4.629213727441584325 ) ) ;
#10481=EDGE_CURVE ( 'NONE', #16163, #27055, #26887, .T. ) ;
#10484=CARTESIAN_POINT ( 'NONE',  ( -1.082681991931092158, 0.000000000000000000, -4.612695725900422872 ) ) ;
#10533=DIRECTION ( 'NONE',  ( 0.000000000000000000, 0.9059606027152153906, 0.4233620038783403872 ) ) ;
#10534=ORIENTED_EDGE ( 'NONE', *, *, #12845, .T. ) ;
#10537=ORIENTED_EDGE ( 'NONE', *, *, #20840, .F. ) ;
#10545=CARTESIAN_POINT ( 'NONE',  ( 9.149098621172166546, 18.06225657836807841, 4.629213727441584325 ) ) ;
#10546=CARTESIAN_POINT ( 'NONE',  ( 23.81497248412561873, 17.93793532016357517, 1.050000000000000044 ) ) ;
#10553=ADVANCED_FACE ( 'NONE', ( #27867 ), #31112, .T. ) ;
#10554=CARTESIAN_POINT ( 'NONE',  ( -29.56299279204132091, 14.30956982362833152, 1.874474774381077458 ) ) ;
#10574=CARTESIAN_POINT ( 'NONE',  ( -40.91822763088380555, -13.69660594212654914, 5.550376981476465410 ) ) ;
#10577=CARTESIAN_POINT ( 'NONE',  ( 108.3631332966649410, 20.50195487734757904, -1.437511512156359972 ) ) ;
#10596=DIRECTION ( 'NONE',  ( -0.000000000000000000, 0.000000000000000000, 1.000000000000000000 ) ) ;
#10622=CARTESIAN_POINT ( 'NONE',  ( -53.35155202832373078, 4.402097243136370963, 5.500000000000000000 ) ) ;
#10628=DIRECTION ( 'NONE',  ( 0.000000000000000000, 0.000000000000000000, -1.000000000000000000 ) ) ;
#10643=CARTESIAN_POINT ( 'NONE',  ( 108.0492188137333471, 18.45222970056496692, 4.641158654489260904 ) ) ;
#10651=DIRECTION ( 'NONE',  ( 0.4922101374339195035, 0.7179542890850474368, -0.4922101374328513579 ) ) ;
#10655=CARTESIAN_POINT ( 'NONE',  ( -56.32779077071818818, 0.3678964383417479556, -1.500000000000000000 ) ) ;
#10663=CARTESIAN_POINT ( 'NONE',  ( 9.302055952181039089, 0.2457637073014079521, -1.050000000000000044 ) ) ;
#10680=EDGE_LOOP ( 'NONE', ( #24234, #19478, #31386, #3456, #14260, #4657, #12170 ) ) ;
#10683=AXIS2_PLACEMENT_3D ( 'NONE', #4247, #16612, #16950 ) ;
#10696=CARTESIAN_POINT ( 'NONE',  ( 56.97280603064898941, -277.2763395528616002, 1.508259000770581615 ) ) ;
#10702=CARTESIAN_POINT ( 'NONE',  ( 17.56297300348760615, 13.04222886887431798, 1.050000000000000044 ) ) ;
#10713=AXIS2_PLACEMENT_3D ( 'NONE', #3580, #18461, #8749 ) ;
#10719=DIRECTION ( 'NONE',  ( 0.4999999999999977796, 0.8660254037844398178, 0.000000000000000000 ) ) ;
#10730=CARTESIAN_POINT ( 'NONE',  ( 108.0493349993913341, 18.45287666815344352, -4.631887712010465563 ) ) ;
#10739=CARTESIAN_POINT ( 'NONE',  ( -30.51827900900859802, 4.402097243136377180, 5.049999999999999822 ) ) ;
#10749=DIRECTION ( 'NONE',  ( 0.000000000000000000, -0.9059606027152153906, 0.4233620038783403872 ) ) ;
#10750=LINE ( 'NONE', #5419, #29985 ) ;
#10767=CARTESIAN_POINT ( 'NONE',  ( 13.49495119401204413, 21.89891421162703011, -1.242381988985816532 ) ) ;
#10783=CARTESIAN_POINT ( 'NONE',  ( 9.331062908042635939, 15.00000000000000178, 4.629213727441584325 ) ) ;
#10789=ORIENTED_EDGE ( 'NONE', *, *, #32437, .F. ) ;
#10818=AXIS2_PLACEMENT_3D ( 'NONE', #2550, #20435, #20604 ) ;
#10833=VECTOR ( 'NONE', #29874, 1000.000000000000000 ) ;
#10842=DIRECTION ( 'NONE',  ( -1.000000000000000000, 0.000000000000000000, 0.000000000000000000 ) ) ;
#10843=VECTOR ( 'NONE', #2876, 1000.000000000000000 ) ;
#10850=VECTOR ( 'NONE', #6784, 1000.000000000000114 ) ;
#10864=VERTEX_POINT ( 'NONE', #22156 ) ;
#10865=CARTESIAN_POINT ( 'NONE',  ( -53.72801162551947840, 5.497307881342318403, 1.430198536305348656 ) ) ;
#10889=DIRECTION ( 'NONE',  ( 1.000000000000000000, -1.447395388606377867E-16, 3.132748819842649948E-17 ) ) ;
#10890=CARTESIAN_POINT ( 'NONE',  ( 12.22374906563888963, 4.895420474595863602, 1.499999999999170441 ) ) ;
#10903=CARTESIAN_POINT ( 'NONE',  ( -19.48091229030179150, 5.440830098942543103, 2.106297401565688787 ) ) ;
#10904=CARTESIAN_POINT ( 'NONE',  ( 47.40009415622113664, 24.02318594975524491, 5.412820279296879811 ) ) ;
#10918=DIRECTION ( 'NONE',  ( 0.6195800045172923376, -0.7849335118354624496, 0.000000000000000000 ) ) ;
#10919=ORIENTED_EDGE ( 'NONE', *, *, #26232, .F. ) ;
#10928=CARTESIAN_POINT ( 'NONE',  ( 17.32050807568873552, 10.00000000000002309, 1.508259000770581615 ) ) ;
#10930=VERTEX_POINT ( 'NONE', #9268 ) ;
#10931=CARTESIAN_POINT ( 'NONE',  ( 107.5147077154356481, 18.30459826903478771, 4.414771370926589000 ) ) ;
#10946=CARTESIAN_POINT ( 'NONE',  ( 107.9195515681646214, 17.73019131298662643, 3.374709941095086041 ) ) ;
#10952=CARTESIAN_POINT ( 'NONE',  ( 109.6329156864505165, 19.01855260168436246, -4.612695725900422872 ) ) ;
#10955=( NAMED_UNIT ( * ) SI_UNIT ( $, .STERADIAN. ) SOLID_ANGLE_UNIT ( ) );
#10957=ORIENTED_EDGE ( 'NONE', *, *, #13974, .F. ) ;
#10958=CARTESIAN_POINT ( 'NONE',  ( 17.41559371906258136, 18.02474698348859405, 1.508259000770581615 ) ) ;
#10969=CARTESIAN_POINT ( 'NONE',  ( -53.35155202832373078, 4.402097243136370963, 5.049999999999999822 ) ) ;
#10984=CARTESIAN_POINT ( 'NONE',  ( -27.13750370378988919, 4.491141813158496809, 1.500000000000000000 ) ) ;
#10988=CARTESIAN_POINT ( 'NONE',  ( 107.6901504273134975, 19.30156402555556028, 4.744684166805590131 ) ) ;
#11005=DIRECTION ( 'NONE',  ( 0.000000000000000000, 0.000000000000000000, -1.000000000000000000 ) ) ;
#11008=VERTEX_POINT ( 'NONE', #5703 ) ;
#11021=CARTESIAN_POINT ( 'NONE',  ( -58.99735576046915497, -4.718558500561493396, 5.402788590778398792 ) ) ;
#11024=CARTESIAN_POINT ( 'NONE',  ( 9.331062908042635939, 15.00000000000000178, 4.629213727441584325 ) ) ;
#11044=CARTESIAN_POINT ( 'NONE',  ( 14.84037634778394299, 10.17686136595211366, -1.499999999999999778 ) ) ;
#11047=CARTESIAN_POINT ( 'NONE',  ( 10.51841884079962064, 2.077444665211660713, 1.050000000000000044 ) ) ;
#11052=CARTESIAN_POINT ( 'NONE',  ( -28.89553135701950737, 6.931071537538192828, 2.065847295955301366 ) ) ;
#11065=CARTESIAN_POINT ( 'NONE',  ( 108.0191616676854665, 18.28485965138728986, -4.516253933250887975 ) ) ;
#11072=CARTESIAN_POINT ( 'NONE',  ( 108.2141205071562098, 20.71718940879397763, -1.479437267284251067 ) ) ;
#11074=ORIENTED_EDGE ( 'NONE', *, *, #20734, .F. ) ;
#11078=CARTESIAN_POINT ( 'NONE',  ( 108.0068349480237515, 18.21621961241920573, 4.414771370926588112 ) ) ;
#11079=VERTEX_POINT ( 'NONE', #18527 ) ;
#11080=CARTESIAN_POINT ( 'NONE',  ( 15.00732532914695305, 9.584243417931569198, -1.050000000000000044 ) ) ;
#11081=CARTESIAN_POINT ( 'NONE',  ( -2.558315521542159132, 0.4094970184090410137, -1.491740999229417941 ) ) ;
#11083=CARTESIAN_POINT ( 'NONE',  ( 8.901201215455881055, 15.00000000000000000, -5.396302277755718357 ) ) ;
#11085=CARTESIAN_POINT ( 'NONE',  ( 8.911384905465473238, 0.2172754300402908179, -1.412391582771881371 ) ) ;
#11086=B_SPLINE_CURVE_WITH_KNOTS ( 'NONE', 3,
 ( #27034, #29873, #26690, #13977, #21841, #19524 ),
 .UNSPECIFIED., .F., .F.,
 ( 4, 2, 4 ),
 ( 0.000000000000000000, 0.0003933473255787851234, 0.0007866946511575702468 ),
 .UNSPECIFIED. ) ;
#11087=DIRECTION ( 'NONE',  ( 0.000000000000000000, -0.9056868434500645604, 0.4239473335232317175 ) ) ;
#11089=EDGE_CURVE ( 'NONE', #20196, #10337, #12427, .T. ) ;
#11103=SHAPE_REPRESENTATION_RELATIONSHIP ( 'NONE' , 'NONE' ,  #27351, #9968 ) ;
#11104=ORIENTED_EDGE ( 'NONE', *, *, #3986, .T. ) ;
#11111=ORIENTED_EDGE ( 'NONE', *, *, #16629, .T. ) ;
#11127=DIRECTION ( 'NONE',  ( -0.000000000000000000, -0.3746065934159164001, 0.9271838545667856479 ) ) ;
#11137=CARTESIAN_POINT ( 'NONE',  ( -41.24084109483541027, -14.66809682074130627, 5.561913827905596186 ) ) ;
#11145=EDGE_CURVE ( 'NONE', #17732, #23082, #27035, .T. ) ;
#11146=CARTESIAN_POINT ( 'NONE',  ( -56.32245079178366609, 0.2385709902195854437, -1.445874915207051581 ) ) ;
#11156=CARTESIAN_POINT ( 'NONE',  ( 108.1156589233279419, 18.82219444680297116, 4.414476567109417715 ) ) ;
#11170=CARTESIAN_POINT ( 'NONE',  ( -57.83188187760648447, -3.114258703770785619, 5.486698823786428925 ) ) ;
#11173=DIRECTION ( 'NONE',  ( -0.000000000000000000, -0.000000000000000000, -1.000000000000000000 ) ) ;
#11179=EDGE_CURVE ( 'NONE', #18045, #29668, #30094, .T. ) ;
#11193=LINE ( 'NONE', #23752, #18182 ) ;
#11196=CARTESIAN_POINT ( 'NONE',  ( 13.32340444539593349, 6.787188996065617985, 1.500000000000829781 ) ) ;
#11203=CARTESIAN_POINT ( 'NONE',  ( -23.54713438638086842, 3.998227953278294944, 2.146185852361370383 ) ) ;
#11205=EDGE_CURVE ( 'NONE', #6245, #15051, #26875, .T. ) ;
#11206=CARTESIAN_POINT ( 'NONE',  ( -17.81720712383456728, 7.575660699117379160, 1.500000000000110578 ) ) ;
#11209=CARTESIAN_POINT ( 'NONE',  ( 0.000000000000000000, 0.000000000000000000, -1.500000000000000000 ) ) ;
#11211=AXIS2_PLACEMENT_3D ( 'NONE', #30842, #2247, #12745 ) ;
#11226=CARTESIAN_POINT ( 'NONE',  ( 107.9622325421415212, 20.81773585569407459, -1.491740999229417941 ) ) ;
#11230=VECTOR ( 'NONE', #6829, 1000.000000000000114 ) ;
#11234=CARTESIAN_POINT ( 'NONE',  ( 107.8941086082324432, 17.58851487277170023, 3.071072500904354463 ) ) ;
#11237=CIRCLE ( 'NONE', #24036, 0.4500000000000025646 ) ;
#11246=AXIS2_PLACEMENT_3D ( 'NONE', #31903, #6464, #6651 ) ;
#11254=AXIS2_PLACEMENT_3D ( 'NONE', #33041, #26020, #3280 ) ;
#11264=CARTESIAN_POINT ( 'NONE',  ( 16.10106094948405797, 19.71584668020019038, -5.396302277755718357 ) ) ;
#11301=CARTESIAN_POINT ( 'NONE',  ( 107.6244361484700534, 18.92564684440470657, -5.076485033663518109 ) ) ;
#11328=CARTESIAN_POINT ( 'NONE',  ( -31.52072750637464083, 0.5000000000000022204, 1.500000000000000000 ) ) ;
#11334=CARTESIAN_POINT ( 'NONE',  ( 17.32050807568873552, 10.00000000000002309, -4.612695725900422872 ) ) ;
#11340=( BOUNDED_SURFACE ( )  B_SPLINE_SURFACE ( 1, 3, ( 
 ( #26821, #28569, #6412, #6601 ),
 ( #1083, #16798, #16610, #3943 ) ),
 .UNSPECIFIED., .F., .F., .F. ) 
 B_SPLINE_SURFACE_WITH_KNOTS ( ( 2, 2 ),
 ( 4, 4 ),
 ( 0.000000000000000000, 1.000000000000000000 ),
 ( 0.000000000000000000, 1.000000000000000000 ),
 .UNSPECIFIED. ) 
 GEOMETRIC_REPRESENTATION_ITEM ( )  RATIONAL_B_SPLINE_SURFACE ( (
 ( 1.000000000000000000, 0.9321687722090974404, 0.9321687722090974404, 1.000000000000000000),
 ( 1.000000000000000000, 0.9321687722090974404, 0.9321687722090974404, 1.000000000000000000) ) ) 
 REPRESENTATION_ITEM ( '' )  SURFACE ( )  );
#11348=ORIENTED_EDGE ( 'NONE', *, *, #24095, .F. ) ;
#11351=CARTESIAN_POINT ( 'NONE',  ( -57.40374817251313999, -2.616512360834425621, 5.500000000000000000 ) ) ;
#11356=CARTESIAN_POINT ( 'NONE',  ( 107.7536796087345294, 16.80655079293032017, -1.379243061950440108 ) ) ;
#11362=VECTOR ( 'NONE', #5536, 1000.000000000000000 ) ;
#11370=VERTEX_POINT ( 'NONE', #17489 ) ;
#11381=CARTESIAN_POINT ( 'NONE',  ( 19.03564543760834482, 14.58476759512525334, 1.500000000000000000 ) ) ;
#11417=FACE_OUTER_BOUND ( 'NONE', #11457, .T. ) ;
#11420=CARTESIAN_POINT ( 'NONE',  ( 16.51080712756689195, 12.51274273092968592, -1.500000000000000000 ) ) ;
#11425=DIRECTION ( 'NONE',  ( 1.000000000000000000, 0.000000000000000000, 0.000000000000000000 ) ) ;
#11439=EDGE_CURVE ( 'NONE', #293, #8403, #19680, .T. ) ;
#11442=ORIENTED_EDGE ( 'NONE', *, *, #17467, .T. ) ;
#11455=CIRCLE ( 'NONE', #26922, 0.9999999999999991118 ) ;
#11457=EDGE_LOOP ( 'NONE', ( #10789, #8131, #5340, #4878 ) ) ;
#11470=CARTESIAN_POINT ( 'NONE',  ( -2.558315521542159132, 0.4094970184090410137, -1.491740999229417941 ) ) ;
#11474=ORIENTED_EDGE ( 'NONE', *, *, #25085, .F. ) ;
#11477=VECTOR ( 'NONE', #3867, 1000.000000000000000 ) ;
#11478=CARTESIAN_POINT ( 'NONE',  ( 107.2357173345097578, 16.72967893420071661, -2.193670894733765309 ) ) ;
#11488=CARTESIAN_POINT ( 'NONE',  ( 9.302055952181039089, 0.2457637073014079521, -1.050000000000000044 ) ) ;
#11494=CARTESIAN_POINT ( 'NONE',  ( -50.81000000000000227, -10.96999999999998643, 9.000000000000000000 ) ) ;
#11512=DIRECTION ( 'NONE',  ( -0.000000000000000000, -0.000000000000000000, -1.000000000000000000 ) ) ;
#11536=CARTESIAN_POINT ( 'NONE',  ( 107.8039769746389425, 17.08662637267895690, -1.979454822623186949 ) ) ;
#11547=CARTESIAN_POINT ( 'NONE',  ( -30.09452540745392923, 13.10954151769360720, 1.499999999999227507 ) ) ;
#11548=CARTESIAN_POINT ( 'NONE',  ( -23.54713438637982748, 8.275374457817617824, 8.599999999999999645 ) ) ;
#11552=DIRECTION ( 'NONE',  ( 0.7822388118548811997, -0.4516257885949860884, 0.4291113938172938513 ) ) ;
#11553=ORIENTED_EDGE ( 'NONE', *, *, #25102, .T. ) ;
#11555=LINE ( 'NONE', #26119, #21561 ) ;
#11569=EDGE_CURVE ( 'NONE', #17732, #11755, #707, .T. ) ;
#11574=DIRECTION ( 'NONE',  ( 0.4809547266710045843, 0.000000000000000000, -0.8767454310646957127 ) ) ;
#11579=DESIGN_CONTEXT ( 'detailed design', #2234, 'design' ) ;
#11585=B_SPLINE_CURVE_WITH_KNOTS ( 'NONE', 3,
 ( #26457, #16389, #3399, #29120, #16051, #6205, #26600, #1374, #3703, #21747 ),
 .UNSPECIFIED., .F., .F.,
 ( 4, 3, 3, 4 ),
 ( 2.268813642641003460E-14, 3.069467774972272057E-06, 2.471397395936450551E-05, 3.618126716052627069E-05 ),
 .UNSPECIFIED. ) ;
#11588=ORIENTED_EDGE ( 'NONE', *, *, #23419, .F. ) ;
#11591=CARTESIAN_POINT ( 'NONE',  ( 109.7786606840771952, 18.61415246516070354, -5.396302277755718357 ) ) ;
#11594=ORIENTED_EDGE ( 'NONE', *, *, #23713, .T. ) ;
#11595=ORIENTED_EDGE ( 'NONE', *, *, #5669, .T. ) ;
#11600=ORIENTED_EDGE ( 'NONE', *, *, #26078, .T. ) ;
#11605=LINE ( 'NONE', #26649, #2733 ) ;
#11623=EDGE_CURVE ( 'NONE', #28172, #4208, #25839, .T. ) ;
#11627=CARTESIAN_POINT ( 'NONE',  ( 107.1965041332822324, 16.51130747298126167, -1.725725757970127505 ) ) ;
#11633=ORIENTED_EDGE ( 'NONE', *, *, #12400, .F. ) ;
#11639=CARTESIAN_POINT ( 'NONE',  ( 20.95640594539235835, 16.13890008475014071, -1.050000000000000044 ) ) ;
#11649=ORIENTED_EDGE ( 'NONE', *, *, #30354, .F. ) ;
#11653=CARTESIAN_POINT ( 'NONE',  ( 24.72695737054825926, 18.91229966141139229, 1.500000000000000000 ) ) ;
#11664=CARTESIAN_POINT ( 'NONE',  ( -59.75626822162179508, -5.804869634004071521, 5.128141679950119602 ) ) ;
#11669=CARTESIAN_POINT ( 'NONE',  ( 107.2640681281359178, 16.88755960000225897, -2.532220120516956552 ) ) ;
#11675=CARTESIAN_POINT ( 'NONE',  ( -2.794738735352966685, 0.000000000000000000, 1.508259000770582059 ) ) ;
#11678=ORIENTED_EDGE ( 'NONE', *, *, #23114, .F. ) ;
#11682=EDGE_CURVE ( 'NONE', #28172, #28865, #15686, .T. ) ;
#11690=CARTESIAN_POINT ( 'NONE',  ( -58.25958745446412479, -3.632822961816825291, 5.448103880042390657 ) ) ;
#11691=LINE ( 'NONE', #24246, #22090 ) ;
#11697=CARTESIAN_POINT ( 'NONE',  ( -17.74503016599027916, 14.86020659576482039, 1.860696004609410315 ) ) ;
#11698=CARTESIAN_POINT ( 'NONE',  ( -30.18078978763795561, 12.16064947808525787, 1.928605623396606683 ) ) ;
#11713=( BOUNDED_SURFACE ( )  B_SPLINE_SURFACE ( 1, 3, ( 
 ( #11775, #26837, #24328, #27154 ),
 ( #21324, #16958, #31527, #19315 ) ),
 .UNSPECIFIED., .F., .F., .F. ) 
 B_SPLINE_SURFACE_WITH_KNOTS ( ( 2, 2 ),
 ( 4, 4 ),
 ( 0.000000000000000000, 1.000000000000000000 ),
 ( 0.000000000000000000, 1.000000000000000000 ),
 .UNSPECIFIED. ) 
 GEOMETRIC_REPRESENTATION_ITEM ( )  RATIONAL_B_SPLINE_SURFACE ( (
 ( 1.000000000000000000, 0.9917560313531952332, 0.9917560313531952332, 1.000000000000000000),
 ( 1.000000000000000000, 0.9917560313531952332, 0.9917560313531952332, 1.000000000000000000) ) ) 
 REPRESENTATION_ITEM ( '' )  SURFACE ( )  );
#11737=CARTESIAN_POINT ( 'NONE',  ( -2.675165579483918421, 0.2071067811865475727, 1.500000000000000000 ) ) ;
#11740=ORIENTED_EDGE ( 'NONE', *, *, #6735, .F. ) ;
#11745=B_SPLINE_CURVE_WITH_KNOTS ( 'NONE', 3,
 ( #28077, #30774, #12346, #14699, #2009, #22382, #12680, #7494, #20386, #22566 ),
 .UNSPECIFIED., .F., .F.,
 ( 4, 2, 2, 2, 4 ),
 ( -5.999999992363981562E-08, 0.0004826362445849100968, 0.0009653324891697438346, 0.001448028733754577789, 0.001930724978339411419 ),
 .UNSPECIFIED. ) ;
#11755=VERTEX_POINT ( 'NONE', #21497 ) ;
#11762=ORIENTED_EDGE ( 'NONE', *, *, #15821, .T. ) ;
#11769=CARTESIAN_POINT ( 'NONE',  ( -56.39515584769779366, 0.01341171002345545316, -1.010295832186372422 ) ) ;
#11775=CARTESIAN_POINT ( 'NONE',  ( 16.36487458112949511, 19.37645981759117575, 4.629213727441584325 ) ) ;
#11776=CARTESIAN_POINT ( 'NONE',  ( 15.28872660057388799, 20.76088595412472415, -4.612695725900421984 ) ) ;
#11777=AXIS2_PLACEMENT_3D ( 'NONE', #29679, #6114, #1086 ) ;
#11784=CARTESIAN_POINT ( 'NONE',  ( 108.1033190332167351, 18.75348106957532579, 4.532405376036182432 ) ) ;
#11788=CIRCLE ( 'NONE', #16048, 0.4500000000000021205 ) ;
#11790=CARTESIAN_POINT ( 'NONE',  ( -50.81000000000000227, -10.96999999999998643, 5.871858320049875957 ) ) ;
#11805=CIRCLE ( 'NONE', #9117, 12.49867430706171767 ) ;
#11814=CARTESIAN_POINT ( 'NONE',  ( -56.28351068136514357, 0.000000000000000000, 0.000000000000000000 ) ) ;
#11822=CARTESIAN_POINT ( 'NONE',  ( 25.71957259916088390, 19.01870514234148857, 1.360524438179210538 ) ) ;
#11823=CYLINDRICAL_SURFACE ( 'NONE', #5582, 0.4500000000000025646 ) ;
#11834=AXIS2_PLACEMENT_3D ( 'NONE', #3431, #19271, #11087 ) ;
#11839=DIRECTION ( 'NONE',  ( -0.000000000000000000, -0.000000000000000000, -1.000000000000000000 ) ) ;
#11855=AXIS2_PLACEMENT_3D ( 'NONE', #25613, #388, #17582 ) ;
#11857=VECTOR ( 'NONE', #16687, 1000.000000000000000 ) ;
#11883=DIRECTION ( 'NONE',  ( -1.000000000000000000, 0.000000000000000000, 0.000000000000000000 ) ) ;
#11890=EDGE_LOOP ( 'NONE', ( #2888, #15220, #28278, #27491 ) ) ;
#11894=AXIS2_PLACEMENT_3D ( 'NONE', #28127, #7556, #22283 ) ;
#11902=AXIS2_PLACEMENT_3D ( 'NONE', #8848, #13838, #8510 ) ;
#11904=ORIENTED_EDGE ( 'NONE', *, *, #32458, .T. ) ;
#11905=CARTESIAN_POINT ( 'NONE',  ( 8.923848839947336131, 0.3991291121161160138, 1.500000000000000000 ) ) ;
#11915=CARTESIAN_POINT ( 'NONE',  ( 20.83472080799475989, 16.60661545279006290, -1.500000000000000000 ) ) ;
#11921=ORIENTED_EDGE ( 'NONE', *, *, #11145, .T. ) ;
#11936=VERTEX_POINT ( 'NONE', #22160 ) ;
#11975=ORIENTED_EDGE ( 'NONE', *, *, #15680, .T. ) ;
#11978=DIRECTION ( 'NONE',  ( 0.000000000000000000, 0.000000000000000000, 1.000000000000000000 ) ) ;
#12003=CARTESIAN_POINT ( 'NONE',  ( 26.08945412691624099, 19.05746434167065928, 1.050000000000000044 ) ) ;
#12005=ADVANCED_FACE ( 'NONE', ( #269 ), #13111, .T. ) ;
#12010=CARTESIAN_POINT ( 'NONE',  ( -26.58934670263598932, 4.786513315057209894, 2.124342492591765996 ) ) ;
#12020=LINE ( 'NONE', #19699, #30100 ) ;
#12022=DIRECTION ( 'NONE',  ( -0.000000000000000000, -0.000000000000000000, -1.000000000000000000 ) ) ;
#12045=CARTESIAN_POINT ( 'NONE',  ( 107.4385791398478744, 17.85938043952733878, 4.629213727441584325 ) ) ;
#12046=FACE_OUTER_BOUND ( 'NONE', #896, .T. ) ;
#12049=CARTESIAN_POINT ( 'NONE',  ( -21.80695521468690146, 18.27315738579030935, 1.777518634817766063 ) ) ;
#12050=CARTESIAN_POINT ( 'NONE',  ( -28.85861747572623059, 15.66456206417216102, 1.840856759657213848 ) ) ;
#12070=VERTEX_POINT ( 'NONE', #11085 ) ;
#12075=CARTESIAN_POINT ( 'NONE',  ( 26.23135861748343700, 19.12135596485594746, -1.050000000000000044 ) ) ;
#12076=CARTESIAN_POINT ( 'NONE',  ( 8.914564461877821699, -1.485434449214014388E-07, -1.044418714689423711 ) ) ;
#12080=ORIENTED_EDGE ( 'NONE', *, *, #12206, .F. ) ;
#12081=DIRECTION ( 'NONE',  ( 1.000000000000000000, 5.361488761196502513E-16, -0.000000000000000000 ) ) ;
#12096=CARTESIAN_POINT ( 'NONE',  ( 108.2840637929470091, 19.75993920999055931, 3.584100151297118231 ) ) ;
#12098=EDGE_CURVE ( 'NONE', #24740, #21393, #12453, .T. ) ;
#12103=ORIENTED_EDGE ( 'NONE', *, *, #7676, .T. ) ;
#12108=DIRECTION ( 'NONE',  ( -0.000000000000000000, -0.000000000000000000, -1.000000000000000000 ) ) ;
#12110=CARTESIAN_POINT ( 'NONE',  ( -56.35010546049321789, 0.004916966322057593312, -1.004378502258694628 ) ) ;
#12128=CARTESIAN_POINT ( 'NONE',  ( -0.000000000000000000, 0.5000000000000000000, -1.000000000000000000 ) ) ;
#12130=LINE ( 'NONE', #7282, #2129 ) ;
#12152=DIRECTION ( 'NONE',  ( 0.4999999999999977796, 0.8660254037844398178, 0.000000000000000000 ) ) ;
#12153=DIRECTION ( 'NONE',  ( -0.1413077769430314268, 0.9899657126261587337, 0.000000000000000000 ) ) ;
#12167=ORIENTED_EDGE ( 'NONE', *, *, #12269, .T. ) ;
#12170=ORIENTED_EDGE ( 'NONE', *, *, #267, .T. ) ;
#12175=DIRECTION ( 'NONE',  ( 0.000000000000000000, 0.000000000000000000, -1.000000000000000000 ) ) ;
#12177=ORIENTED_EDGE ( 'NONE', *, *, #18920, .T. ) ;
#12193=DIRECTION ( 'NONE',  ( 0.8660254037844409281, -0.4999999999999960587, 0.000000000000000000 ) ) ;
#12194=EDGE_CURVE ( 'NONE', #17962, #17857, #14087, .T. ) ;
#12206=EDGE_CURVE ( 'NONE', #25095, #2157, #8567, .T. ) ;
#12208=ORIENTED_EDGE ( 'NONE', *, *, #8888, .T. ) ;
#12209=CYLINDRICAL_SURFACE ( 'NONE', #17658, 297.9387600756452343 ) ;
#12222=CARTESIAN_POINT ( 'NONE',  ( 8.878230740118540965, 3.506306759228156664E-16, -1.080849929302612367 ) ) ;
#12226=ORIENTED_EDGE ( 'NONE', *, *, #19417, .T. ) ;
#12230=CARTESIAN_POINT ( 'NONE',  ( 107.4385791398478602, 17.85938043952733878, -4.612695725900422872 ) ) ;
#12235=CARTESIAN_POINT ( 'NONE',  ( 78.40736801748178664, 24.56822898102832653, 4.629213727441585213 ) ) ;
#12244=CARTESIAN_POINT ( 'NONE',  ( 107.8757006203288142, 20.33592830972715504, 2.535883260025156183 ) ) ;
#12246=ORIENTED_EDGE ( 'NONE', *, *, #10247, .F. ) ;
#12259=AXIS2_PLACEMENT_3D ( 'NONE', #16060, #8542, #18748 ) ;
#12265=B_SPLINE_CURVE_WITH_KNOTS ( 'NONE', 3,
 ( #21272, #16256, #10577, #11072, #3412, #11226 ),
 .UNSPECIFIED., .F., .F.,
 ( 4, 2, 4 ),
 ( -6.819812922326889058E-06, 0.0003932617828678426023, 0.0007933433786580120200 ),
 .UNSPECIFIED. ) ;
#12269=EDGE_CURVE ( 'NONE', #17891, #20953, #15773, .T. ) ;
#12280=AXIS2_PLACEMENT_3D ( 'NONE', #14118, #12108, #24318 ) ;
#12292=ORIENTED_EDGE ( 'NONE', *, *, #12642, .F. ) ;
#12297=CARTESIAN_POINT ( 'NONE',  ( -56.77537022611499395, 0.4514244267945254907, 2.028141679927229379 ) ) ;
#12298=DIRECTION ( 'NONE',  ( -0.000000000000000000, -0.000000000000000000, -1.000000000000000000 ) ) ;
#12304=ORIENTED_EDGE ( 'NONE', *, *, #13414, .T. ) ;
#12308=FACE_OUTER_BOUND ( 'NONE', #17023, .T. ) ;
#12313=CARTESIAN_POINT ( 'NONE',  ( -56.28660922948461121, 0.003949738777827453869, -1.069323361021561558 ) ) ;
#12331=( BOUNDED_CURVE ( )  B_SPLINE_CURVE ( 3, ( #16904, #4199, #6551, #29788 ),
 .UNSPECIFIED., .F., .F. ) 
 B_SPLINE_CURVE_WITH_KNOTS ( ( 4, 4 ),
 ( 5.051426171356965256, 5.615871152429257940 ),
 .UNSPECIFIED. ) 
 CURVE ( )  GEOMETRIC_REPRESENTATION_ITEM ( )  RATIONAL_B_SPLINE_CURVE ( ( 1.000000000000000000, 0.9736259116362534494, 0.9736259116362534494, 1.000000000000000000 ) ) 
 REPRESENTATION_ITEM ( '' )  );
#12341=ORIENTED_EDGE ( 'NONE', *, *, #23419, .T. ) ;
#12346=CARTESIAN_POINT ( 'NONE',  ( 107.4685439760147432, 18.03024793969074935, 4.906145018174012939 ) ) ;
#12347=EDGE_LOOP ( 'NONE', ( #24853, #22074, #28765, #32620, #21312 ) ) ;
#12363=CARTESIAN_POINT ( 'NONE',  ( -22.67670559979717382, 18.46223496596762459, 1.773004750130064533 ) ) ;
#12373=DIRECTION ( 'NONE',  ( 0.000000000000000000, 0.000000000000000000, -1.000000000000000000 ) ) ;
#12377=AXIS2_PLACEMENT_3D ( 'NONE', #2814, #20353, #18159 ) ;
#12379=CARTESIAN_POINT ( 'NONE',  ( 107.5346493233867875, 18.40935155254226174, -5.110104196312056146 ) ) ;
#12392=CARTESIAN_POINT ( 'NONE',  ( 22.89387586468013325, 17.41384229115070426, -1.050000000000117950 ) ) ;
#12393=CARTESIAN_POINT ( 'NONE',  ( 25.54995566824271336, 19.30806704599434553, 1.500000000000000000 ) ) ;
#12396=EDGE_CURVE ( 'NONE', #22604, #17057, #2362, .T. ) ;
#12400=EDGE_CURVE ( 'NONE', #18469, #23780, #15395, .T. ) ;
#12402=DIRECTION ( 'NONE',  ( -0.1503837331804358524, 0.08682408883346492967, -0.9848077530122080203 ) ) ;
#12406=CARTESIAN_POINT ( 'NONE',  ( 107.6696441609669819, 19.18460445470642739, -4.889496736489043371 ) ) ;
#12411=CARTESIAN_POINT ( 'NONE',  ( 109.6329156864505165, 19.01855260168436246, 4.629213727441584325 ) ) ;
#12414=LINE ( 'NONE', #12900, #27873 ) ;
#12422=ORIENTED_EDGE ( 'NONE', *, *, #27217, .F. ) ;
#12424=EDGE_CURVE ( 'NONE', #17962, #9305, #230, .T. ) ;
#12427=CIRCLE ( 'NONE', #14575, 3.250000000000002665 ) ;
#12436=DIRECTION ( 'NONE',  ( 0.1441052676711226943, 0.9895623637898898206, 0.000000000000000000 ) ) ;
#12438=AXIS2_PLACEMENT_3D ( 'NONE', #18543, #8192, #16007 ) ;
#12453=CIRCLE ( 'NONE', #10336, 3.250000000000002665 ) ;
#12463=AXIS2_PLACEMENT_3D ( 'NONE', #31789, #29258, #16534 ) ;
#12468=ORIENTED_EDGE ( 'NONE', *, *, #1345, .F. ) ;
#12483=CARTESIAN_POINT ( 'NONE',  ( -54.00754732910517930, 5.431685566383787744, 1.345424820068321425 ) ) ;
#12488=VECTOR ( 'NONE', #31205, 1000.000000000000000 ) ;
#12491=ORIENTED_EDGE ( 'NONE', *, *, #24185, .T. ) ;
#12499=CARTESIAN_POINT ( 'NONE',  ( -50.81000000000000227, -10.96999999999998643, 8.549999999999998934 ) ) ;
#12500=CARTESIAN_POINT ( 'NONE',  ( -56.32770133515839461, 0.5000000000000000000, -1.500000000000000000 ) ) ;
#12523=ORIENTED_EDGE ( 'NONE', *, *, #28579, .T. ) ;
#12531=CARTESIAN_POINT ( 'NONE',  ( -40.73102457812986898, -13.75294349655999326, 5.448103877476410339 ) ) ;
#12532=CARTESIAN_POINT ( 'NONE',  ( -31.80959807272228090, -0.0003384977252891612984, 0.000000000000000000 ) ) ;
#12537=EDGE_CURVE ( 'NONE', #21273, #1079, #27977, .T. ) ;
#12554=CARTESIAN_POINT ( 'NONE',  ( 107.4385791398479029, 17.85938043952739562, -4.612695725900423760 ) ) ;
#12556=CARTESIAN_POINT ( 'NONE',  ( -20.10769817351002331, 5.029112325015176133, 2.117653528444686906 ) ) ;
#12566=CARTESIAN_POINT ( 'NONE',  ( 26.23135861748343345, 19.12135596485594746, -1.500000000000000000 ) ) ;
#12573=ORIENTED_EDGE ( 'NONE', *, *, #20135, .T. ) ;
#12574=DIRECTION ( 'NONE',  ( 0.07591486983605109928, 0.4227239498242779114, -0.9030733053206351224 ) ) ;
#12582=FACE_OUTER_BOUND ( 'NONE', #25654, .T. ) ;
#12599=ORIENTED_EDGE ( 'NONE', *, *, #30993, .T. ) ;
#12604=DIRECTION ( 'NONE',  ( -0.1356223135424326209, 0.9907606108790346644, 0.000000000000000000 ) ) ;
#12606=ADVANCED_FACE ( 'NONE', ( #32411 ), #3815, .T. ) ;
#12609=CARTESIAN_POINT ( 'NONE',  ( 107.9029849834811614, 20.48784698331989773, 2.211997423210143143 ) ) ;
#12626=VERTEX_POINT ( 'NONE', #23584 ) ;
#12635=CARTESIAN_POINT ( 'NONE',  ( -41.77414131929176477, -16.18685544166627821, 1.949999999999999956 ) ) ;
#12636=DIRECTION ( 'NONE',  ( 0.000000000000000000, 0.000000000000000000, 1.000000000000000000 ) ) ;
#12642=EDGE_CURVE ( 'NONE', #27103, #15924, #28535, .T. ) ;
#12647=CARTESIAN_POINT ( 'NONE',  ( 110.2274383572228942, 17.36892446252421962, -4.612695725900422872 ) ) ;
#12660=CARTESIAN_POINT ( 'NONE',  ( 107.5345041083672584, 18.40851707499601631, 5.126370027289036457 ) ) ;
#12674=ORIENTED_EDGE ( 'NONE', *, *, #15755, .F. ) ;
#12679=DIRECTION ( 'NONE',  ( 0.4999999999999978906, 0.8660254037844397068, 9.233562054644581322E-18 ) ) ;
#12680=CARTESIAN_POINT ( 'NONE',  ( 107.6243858517459699, 18.92535819529473073, 5.093136976256313453 ) ) ;
#12690=LINE ( 'NONE', #23063, #16515 ) ;
#12693=LINE ( 'NONE', #22897, #8625 ) ;
#12708=EDGE_CURVE ( 'NONE', #32155, #11936, #16672, .T. ) ;
#12710=ORIENTED_EDGE ( 'NONE', *, *, #18975, .T. ) ;
#12718=PLANE ( 'NONE',  #10818 ) ;
#12739=ADVANCED_FACE ( 'NONE', ( #6654 ), #11823, .T. ) ;
#12740=VERTEX_POINT ( 'NONE', #27193 ) ;
#12745=DIRECTION ( 'NONE',  ( -1.000000000000000000, 0.000000000000000000, 0.000000000000000000 ) ) ;
#12751=DIRECTION ( 'NONE',  ( -0.000000000000000000, 0.000000000000000000, 1.000000000000000000 ) ) ;
#12760=DIRECTION ( 'NONE',  ( -1.000000000000000000, -5.361488761196502513E-16, 0.000000000000000000 ) ) ;
#12774=AXIS2_PLACEMENT_3D ( 'NONE', #29997, #7089, #17294 ) ;
#12779=ORIENTED_EDGE ( 'NONE', *, *, #23951, .T. ) ;
#12791=ORIENTED_EDGE ( 'NONE', *, *, #16475, .F. ) ;
#12801=AXIS2_PLACEMENT_3D ( 'NONE', #32896, #23189, #12636 ) ;
#12808=CARTESIAN_POINT ( 'NONE',  ( 107.9955289544189725, 18.15326337889181829, 5.055346619445248102 ) ) ;
#12832=VECTOR ( 'NONE', #13144, 1000.000000000000000 ) ;
#12839=ORIENTED_EDGE ( 'NONE', *, *, #12642, .T. ) ;
#12840=ORIENTED_EDGE ( 'NONE', *, *, #22432, .F. ) ;
#12844=CIRCLE ( 'NONE', #4843, 302.4235430809786749 ) ;
#12845=EDGE_CURVE ( 'NONE', #8184, #12626, #30703, .T. ) ;
#12847=AXIS2_PLACEMENT_3D ( 'NONE', #29072, #6159, #16491 ) ;
#12853=EDGE_CURVE ( 'NONE', #28913, #11008, #13054, .T. ) ;
#12868=AXIS2_PLACEMENT_3D ( 'NONE', #17459, #7111, #27507 ) ;
#12869=ORIENTED_EDGE ( 'NONE', *, *, #28566, .F. ) ;
#12878=DIRECTION ( 'NONE',  ( -0.4999999999999982236, -0.8660254037844398178, 0.000000000000000000 ) ) ;
#12888=DIRECTION ( 'NONE',  ( 0.4999999999999977796, 0.8660254037844398178, 0.000000000000000000 ) ) ;
#12893=EDGE_CURVE ( 'NONE', #18598, #293, #27474, .T. ) ;
#12895=FACE_OUTER_BOUND ( 'NONE', #25322, .T. ) ;
#12896=CARTESIAN_POINT ( 'NONE',  ( -0.2059365608663963898, 0.000000000000000000, 1.000000000000000000 ) ) ;
#12900=CARTESIAN_POINT ( 'NONE',  ( -60.22964952008683781, -5.531562813905956055, 2.028141679950118625 ) ) ;
#12902=ORIENTED_EDGE ( 'NONE', *, *, #23807, .F. ) ;
#12911=ORIENTED_EDGE ( 'NONE', *, *, #16167, .T. ) ;
#12918=ORIENTED_EDGE ( 'NONE', *, *, #3257, .T. ) ;
#12925=ORIENTED_EDGE ( 'NONE', *, *, #24125, .T. ) ;
#12940=FACE_OUTER_BOUND ( 'NONE', #16426, .T. ) ;
#12941=AXIS2_PLACEMENT_3D ( 'NONE', #27597, #4699, #12373 ) ;
#12949=EDGE_CURVE ( 'NONE', #18415, #429, #24747, .T. ) ;
#12952=VERTEX_POINT ( 'NONE', #28697 ) ;
#12984=AXIS2_PLACEMENT_3D ( 'NONE', #3355, #13679, #3667 ) ;
#12989=AXIS2_PLACEMENT_3D ( 'NONE', #11790, #11978, #21994 ) ;
#12992=AXIS2_PLACEMENT_3D ( 'NONE', #18254, #5579, #28629 ) ;
#12996=CARTESIAN_POINT ( 'NONE',  ( -56.32565245118806274, 0.3500057972172317955, -1.478456117012219462 ) ) ;
#12997=CARTESIAN_POINT ( 'NONE',  ( -1.152183934781129714E-14, 21.49000000000002331, -1.050000000000000044 ) ) ;
#13008=( BOUNDED_CURVE ( )  B_SPLINE_CURVE ( 3, ( #7614, #30869, #7789, #17982 ),
 .UNSPECIFIED., .F., .F. ) 
 B_SPLINE_CURVE_WITH_KNOTS ( ( 4, 4 ),
 ( 0.6009777071450013164, 1.570796326794896558 ),
 .UNSPECIFIED. ) 
 CURVE ( )  GEOMETRIC_REPRESENTATION_ITEM ( )  RATIONAL_B_SPLINE_CURVE ( ( 1.000000000000000000, 0.9231448173254019895, 0.9231448173254019895, 1.000000000000000000 ) ) 
 REPRESENTATION_ITEM ( '' )  );
#13031=CARTESIAN_POINT ( 'NONE',  ( -31.80940264096946635, 0.000000000000000000, 1.000000000000000000 ) ) ;
#13034=ORIENTED_EDGE ( 'NONE', *, *, #13268, .T. ) ;
#13040=EDGE_CURVE ( 'NONE', #21301, #7656, #11455, .T. ) ;
#13054=CIRCLE ( 'NONE', #29604, 0.9999999999999991118 ) ;
#13057=CARTESIAN_POINT ( 'NONE',  ( -19.06947354093846059, 16.57130634721221440, 1.818690743637907836 ) ) ;
#13059=ORIENTED_EDGE ( 'NONE', *, *, #23899, .T. ) ;
#13065=CARTESIAN_POINT ( 'NONE',  ( -47.55999999999999517, -10.96999999999998643, 5.700000000000000178 ) ) ;
#13067=CARTESIAN_POINT ( 'NONE',  ( 14.23800746264082839, 22.11259878822725966, 1.508259000770582059 ) ) ;
#13068=CARTESIAN_POINT ( 'NONE',  ( 23.59981322687704264, 18.33325850388178324, 1.500000000000000000 ) ) ;
#13072=CARTESIAN_POINT ( 'NONE',  ( -42.46793790805479318, 24.51887538314362658, 1.500000000000000000 ) ) ;
#13074=ORIENTED_EDGE ( 'NONE', *, *, #29017, .F. ) ;
#13075=ADVANCED_FACE ( 'NONE', ( #3619 ), #28164, .T. ) ;
#13077=CARTESIAN_POINT ( 'NONE',  ( -0.2059365608663963898, 0.5000000000000000000, 1.000000000000000000 ) ) ;
#13081=DIRECTION ( 'NONE',  ( -1.000000000000000000, 0.000000000000000000, 0.000000000000000000 ) ) ;
#13084=EDGE_LOOP ( 'NONE', ( #12710, #32350, #17522, #437, #17689, #3847 ) ) ;
#13095=CARTESIAN_POINT ( 'NONE',  ( -40.70363404372887572, -12.74270274920393575, 5.547394276430027027 ) ) ;
#13106=CARTESIAN_POINT ( 'NONE',  ( -31.80959807272226669, -0.0003384977252881313063, 1.500000000000000000 ) ) ;
#13111=SPHERICAL_SURFACE ( 'NONE', #18336, 0.4500000000000000111 ) ;
#13117=DIRECTION ( 'NONE',  ( -0.000000000000000000, -0.3746065934159164001, 0.9271838545667856479 ) ) ;
#13130=ORIENTED_EDGE ( 'NONE', *, *, #16167, .F. ) ;
#13143=VERTEX_POINT ( 'NONE', #22163 ) ;
#13144=DIRECTION ( 'NONE',  ( -0.09975574163943222439, 0.1727820128662104771, -0.9798954883250904357 ) ) ;
#13150=LINE ( 'NONE', #10484, #138 ) ;
#13156=CARTESIAN_POINT ( 'NONE',  ( 108.0732232521118590, 18.58589588515538082, 4.641033904584911163 ) ) ;
#13166=EDGE_CURVE ( 'NONE', #25302, #10864, #21812, .T. ) ;
#13168=CARTESIAN_POINT ( 'NONE',  ( 9.282537329959909655, 0.2172754300399127037, 1.041239158277186938 ) ) ;
#13175=CARTESIAN_POINT ( 'NONE',  ( 9.286001645569189833, 0.2223290027121335721, -1.044355983488527873 ) ) ;
#13194=CARTESIAN_POINT ( 'NONE',  ( -31.80940264096946635, 0.000000000000000000, 1.000000000000000000 ) ) ;
#13195=EDGE_LOOP ( 'NONE', ( #29088, #30425, #6717, #22858, #25962, #12925, #2287 ) ) ;
#13198=CARTESIAN_POINT ( 'NONE',  ( -16.91521474802581437, 10.78976942541848594, 1.963924860182840515 ) ) ;
#13209=LINE ( 'NONE', #13362, #31126 ) ;
#13211=( BOUNDED_SURFACE ( )  B_SPLINE_SURFACE ( 1, 3, ( 
 ( #29687, #19649, #22811, #25644 ),
 ( #4759, #15117, #5104, #22477 ) ),
 .UNSPECIFIED., .F., .F., .F. ) 
 B_SPLINE_SURFACE_WITH_KNOTS ( ( 2, 2 ),
 ( 4, 4 ),
 ( 0.000000000000000000, 1.000000000000000000 ),
 ( 0.000000000000000000, 1.000000000000000000 ),
 .UNSPECIFIED. ) 
 GEOMETRIC_REPRESENTATION_ITEM ( )  RATIONAL_B_SPLINE_SURFACE ( (
 ( 1.000000000000000000, 0.9917560313531952332, 0.9917560313531952332, 1.000000000000000000),
 ( 1.000000000000000000, 0.9917560313531952332, 0.9917560313531952332, 1.000000000000000000) ) ) 
 REPRESENTATION_ITEM ( '' )  SURFACE ( )  );
#13218=CARTESIAN_POINT ( 'NONE',  ( 8.870145747188287189, 0.000000000000000000, 4.148259000770580407 ) ) ;
#13220=CARTESIAN_POINT ( 'NONE',  ( -29.98627798296288915, 13.02091040240743602, 1.906846592315978528 ) ) ;
#13243=ORIENTED_EDGE ( 'NONE', *, *, #20269, .F. ) ;
#13247=CARTESIAN_POINT ( 'NONE',  ( 17.32050807568873552, 10.00000000000002309, -1.491740999229418829 ) ) ;
#13255=ADVANCED_FACE ( 'NONE', ( #30516 ), #30018, .T. ) ;
#13258=FACE_BOUND ( 'NONE', #29786, .T. ) ;
#13268=EDGE_CURVE ( 'NONE', #3200, #8276, #6922, .T. ) ;
#13269=CARTESIAN_POINT ( 'NONE',  ( 0.6708088701982989344, 0.000000000000000000, -4.612695725900422872 ) ) ;
#13270=ORIENTED_EDGE ( 'NONE', *, *, #28255, .T. ) ;
#13279=CYLINDRICAL_SURFACE ( 'NONE', #2778, 0.4499999999999996225 ) ;
#13280=ORIENTED_EDGE ( 'NONE', *, *, #25627, .T. ) ;
#13283=ORIENTED_EDGE ( 'NONE', *, *, #23114, .T. ) ;
#13285=CARTESIAN_POINT ( 'NONE',  ( -42.46793790805478608, 24.51887538314362658, -1.500000000000000000 ) ) ;
#13301=ADVANCED_FACE ( 'NONE', ( #12940 ), #18465, .T. ) ;
#13307=EDGE_LOOP ( 'NONE', ( #2640, #21163, #26723, #2393 ) ) ;
#13317=ADVANCED_FACE ( 'NONE', ( #13258, #80 ), #10273, .T. ) ;
#13327=ORIENTED_EDGE ( 'NONE', *, *, #20135, .F. ) ;
#13331=DIRECTION ( 'NONE',  ( -0.000000000000000000, -0.000000000000000000, -1.000000000000000000 ) ) ;
#13344=AXIS2_PLACEMENT_3D ( 'NONE', #30340, #27810, #15605 ) ;
#13362=CARTESIAN_POINT ( 'NONE',  ( -41.86373177837819526, -16.13513036599590222, 5.128141679950118714 ) ) ;
#13363=CARTESIAN_POINT ( 'NONE',  ( 16.54275606305774460, 11.79585867046270486, 1.050000000000000044 ) ) ;
#13367=DIRECTION ( 'NONE',  ( 0.000000000000000000, -0.9271838545667856479, -0.3746065934159162891 ) ) ;
#13372=DIRECTION ( 'NONE',  ( 0.000000000000000000, 0.000000000000000000, 1.000000000000000000 ) ) ;
#13374=CARTESIAN_POINT ( 'NONE',  ( -19.95676506897142843, 4.491141813158487928, 1.500000000000000000 ) ) ;
#13383=CIRCLE ( 'NONE', #6978, 299.4192503346018270 ) ;
#13391=VERTEX_POINT ( 'NONE', #30706 ) ;
#13392=( BOUNDED_CURVE ( )  B_SPLINE_CURVE ( 3, ( #13585, #903, #31820, #11081 ),
 .UNSPECIFIED., .F., .F. ) 
 B_SPLINE_CURVE_WITH_KNOTS ( ( 4, 4 ),
 ( 3.901433257974888047, 5.290220370840431841 ),
 .UNSPECIFIED. ) 
 CURVE ( )  GEOMETRIC_REPRESENTATION_ITEM ( )  RATIONAL_B_SPLINE_CURVE ( ( 1.000000000000000000, 0.8456279454424026065, 0.8456279454424026065, 1.000000000000000000 ) ) 
 REPRESENTATION_ITEM ( '' )  );
#13397=ORIENTED_EDGE ( 'NONE', *, *, #32526, .F. ) ;
#13400=FACE_OUTER_BOUND ( 'NONE', #3422, .T. ) ;
#13413=CARTESIAN_POINT ( 'NONE',  ( 17.32050807568873552, 10.00000000000002309, 1.500000000000000000 ) ) ;
#13414=EDGE_CURVE ( 'NONE', #5412, #15980, #30859, .T. ) ;
#13421=CARTESIAN_POINT ( 'NONE',  ( 108.0068349480237373, 18.21621961241920573, 4.414771370926589000 ) ) ;
#13424=EDGE_LOOP ( 'NONE', ( #12573, #7914, #13902, #6511 ) ) ;
#13426=CIRCLE ( 'NONE', #19850, 12.49867430706171767 ) ;
#13429=CARTESIAN_POINT ( 'NONE',  ( -50.81000000000000227, -10.96999999999998643, 1.499999999999999556 ) ) ;
#13433=EDGE_CURVE ( 'NONE', #12626, #8184, #21083, .T. ) ;
#13451=CARTESIAN_POINT ( 'NONE',  ( 17.80111248010111424, 13.30892117176750666, 1.049999999999999822 ) ) ;
#13456=DIRECTION ( 'NONE',  ( 1.000000000000000000, 0.000000000000000000, 0.000000000000000000 ) ) ;
#13480=CARTESIAN_POINT ( 'NONE',  ( 13.04731869766886554, 19.33256796700939262, -5.396302277755719246 ) ) ;
#13484=VERTEX_POINT ( 'NONE', #21288 ) ;
#13503=CARTESIAN_POINT ( 'NONE',  ( 108.1834173863008886, 19.19950030484896786, -3.592082168559364241 ) ) ;
#13515=CARTESIAN_POINT ( 'NONE',  ( -30.51827900900860158, 4.402097243136377180, 5.049999999999999822 ) ) ;
#13518=CARTESIAN_POINT ( 'NONE',  ( -59.40911793129208007, -5.269765563131745267, 5.315798354995362018 ) ) ;
#13519=AXIS2_PLACEMENT_3D ( 'NONE', #17405, #24208, #21215 ) ;
#13523=ORIENTED_EDGE ( 'NONE', *, *, #21609, .F. ) ;
#13528=ORIENTED_EDGE ( 'NONE', *, *, #16885, .T. ) ;
#13536=ORIENTED_EDGE ( 'NONE', *, *, #12269, .F. ) ;
#13539=EDGE_CURVE ( 'NONE', #429, #18469, #6385, .T. ) ;
#13546=CARTESIAN_POINT ( 'NONE',  ( 14.99916604845051360, 9.584522669134234008, 1.500000000000000000 ) ) ;
#13547=ADVANCED_FACE ( 'NONE', ( #14089, #6234 ), #16581, .T. ) ;
#13558=CARTESIAN_POINT ( 'NONE',  ( 110.2274383572228942, 17.36892446252421962, 4.629213727441584325 ) ) ;
#13570=DIRECTION ( 'NONE',  ( -0.7849335118354594520, -0.6195800045172962234, -0.000000000000000000 ) ) ;
#13583=ORIENTED_EDGE ( 'NONE', *, *, #29897, .F. ) ;
#13584=CARTESIAN_POINT ( 'NONE',  ( 13.48264087563610580, 7.964219514463561467, -1.500000000000000000 ) ) ;
#13585=CARTESIAN_POINT ( 'NONE',  ( -3.064492245890347188, 0.000000000000000000, -1.000000000000000222 ) ) ;
#13609=ORIENTED_EDGE ( 'NONE', *, *, #32581, .T. ) ;
#13614=ORIENTED_EDGE ( 'NONE', *, *, #18107, .F. ) ;
#13616=EDGE_CURVE ( 'NONE', #32155, #30480, #29971, .T. ) ;
#13617=B_SPLINE_CURVE_WITH_KNOTS ( 'NONE', 3,
 ( #11488, #4286, #1802, #31739, #19517, #32395, #9456, #29713, #16478, #16331, #19673, #21684, #1463, #11639, #6793, #6149, #8815, #21834, #32047, #19020 ),
 .UNSPECIFIED., .F., .F.,
 ( 4, 2, 2, 2, 2, 2, 2, 2, 2, 4 ),
 ( 0.0002980439675631849604, 0.003522811531434848643, 0.006747579095306512759, 0.009972346659178177308, 0.01319711422304984012, 0.01642188178692150294, 0.01964664935079316749, 0.02125903313272899456, 0.02287141691466482163, 0.02609618447853648271 ),
 .UNSPECIFIED. ) ;
#13629=FACE_OUTER_BOUND ( 'NONE', #24484, .T. ) ;
#13651=EDGE_CURVE ( 'NONE', #10864, #18045, #6042, .T. ) ;
#13653=EDGE_CURVE ( 'NONE', #28345, #28296, #26594, .T. ) ;
#13654=CARTESIAN_POINT ( 'NONE',  ( 8.930755659321954809, 0.4999999999534671113, 1.500000000000000000 ) ) ;
#13665=CARTESIAN_POINT ( 'NONE',  ( 108.1834172094735749, 19.19949932020479366, 3.608602272731602500 ) ) ;
#13667=ORIENTED_EDGE ( 'NONE', *, *, #25378, .T. ) ;
#13669=ADVANCED_FACE ( 'NONE', ( #12046 ), #27496, .T. ) ;
#13679=DIRECTION ( 'NONE',  ( -0.4999999999999960032, -0.8660254037844409281, -0.000000000000000000 ) ) ;
#13686=EDGE_CURVE ( 'NONE', #3747, #2818, #22153, .T. ) ;
#13699=CARTESIAN_POINT ( 'NONE',  ( -23.54713438637982748, 8.434582260019382716, 8.205946861809124471 ) ) ;
#13702=CARTESIAN_POINT ( 'NONE',  ( 18.72918216980634298, 14.91508072752954739, 1.500000000000000222 ) ) ;
#13703=B_SPLINE_CURVE_WITH_KNOTS ( 'NONE', 3,
 ( #3020, #23534, #13175, #18193, #26221, #23376, #10663 ),
 .UNSPECIFIED., .F., .F.,
 ( 4, 3, 4 ),
 ( 0.000000000000000000, 1.028838076071613430E-05, 3.621257616738532545E-05 ),
 .UNSPECIFIED. ) ;
#13711=CARTESIAN_POINT ( 'NONE',  ( -17.84619894073314583, 6.485688093852441050, 1.500000000000000000 ) ) ;
#13718=ORIENTED_EDGE ( 'NONE', *, *, #1799, .F. ) ;
#13726=CARTESIAN_POINT ( 'NONE',  ( 26.08945412691625521, 19.05746434167071612, 1.050000000000000044 ) ) ;
#13734=CARTESIAN_POINT ( 'NONE',  ( 107.8265053079015559, 17.21207302154092389, 2.264765925274638825 ) ) ;
#13736=FACE_OUTER_BOUND ( 'NONE', #28305, .T. ) ;
#13737=CARTESIAN_POINT ( 'NONE',  ( -56.28351068136514357, 0.000000000000000000, -1.000000000000000000 ) ) ;
#13747=CARTESIAN_POINT ( 'NONE',  ( -41.77414131929176477, -16.18685544166627821, 1.500000000000000000 ) ) ;
#13749=CARTESIAN_POINT ( 'NONE',  ( 13.62547635268492385, 21.94000000000003681, -1.081064828084696394 ) ) ;
#13759=VERTEX_POINT ( 'NONE', #22394 ) ;
#13765=DIRECTION ( 'NONE',  ( 0.000000000000000000, -0.000000000000000000, -1.000000000000000000 ) ) ;
#13780=DIRECTION ( 'NONE',  ( 0.000000000000000000, -0.9271838545667854259, -0.3746065934159166777 ) ) ;
#13786=ORIENTED_EDGE ( 'NONE', *, *, #2673, .F. ) ;
#13788=FACE_OUTER_BOUND ( 'NONE', #18761, .T. ) ;
#13792=CARTESIAN_POINT ( 'NONE',  ( -59.84585868070823267, -5.753144558333701752, 1.500000000000000000 ) ) ;
#13814=CARTESIAN_POINT ( 'NONE',  ( -56.28351068137280322, 0.000000000000000000, 4.148259000770580407 ) ) ;
#13823=LINE ( 'NONE', #6483, #11857 ) ;
#13825=CARTESIAN_POINT ( 'NONE',  ( -42.85764933975779201, 24.74387538314362800, 1.050000000000000044 ) ) ;
#13838=DIRECTION ( 'NONE',  ( -0.000000000000000000, -0.000000000000000000, -1.000000000000000000 ) ) ;
#13850=CARTESIAN_POINT ( 'NONE',  ( 19.54096706358707181, 15.62796595325201920, 1.500000000000000222 ) ) ;
#13862=DIRECTION ( 'NONE',  ( -0.000000000000000000, -0.000000000000000000, -1.000000000000000000 ) ) ;
#13869=VECTOR ( 'NONE', #15892, 1000.000000000000227 ) ;
#13886=CARTESIAN_POINT ( 'NONE',  ( -2.558315521542159132, 0.4094970184090410137, -1.491740999229417941 ) ) ;
#13889=CIRCLE ( 'NONE', #27248, 0.4500000000000006772 ) ;
#13891=CARTESIAN_POINT ( 'NONE',  ( -23.54713438637982748, 10.71031731502107576, 2.573304945315896042 ) ) ;
#13892=CIRCLE ( 'NONE', #19794, 6.035938585833444670 ) ;
#13902=ORIENTED_EDGE ( 'NONE', *, *, #28245, .T. ) ;
#13906=CARTESIAN_POINT ( 'NONE',  ( 8.886976913778035225, 2.271465516421274549E-16, -1.168311665897499463 ) ) ;
#13912=CARTESIAN_POINT ( 'NONE',  ( 47.40009415622113664, 24.02318594975524491, -5.396302277755718357 ) ) ;
#13919=CARTESIAN_POINT ( 'NONE',  ( 8.007433738499996068, 15.00000000000000000, 5.412820279296878923 ) ) ;
#13921=ORIENTED_EDGE ( 'NONE', *, *, #26018, .F. ) ;
#13942=CONICAL_SURFACE ( 'NONE', #18241, 2.524999999999999911, 0.7853981633974627119 ) ;
#13954=CARTESIAN_POINT ( 'NONE',  ( 108.1721831928535806, 19.13694388309671623, 4.863130064418045961 ) ) ;
#13974=EDGE_CURVE ( 'NONE', #10113, #22357, #1921, .T. ) ;
#13976=CARTESIAN_POINT ( 'NONE',  ( 9.031711214211203043, 0.01997115109544704906, 1.016156546702292829 ) ) ;
#13977=CARTESIAN_POINT ( 'NONE',  ( 107.6567828190203215, 16.56237727417163796, 1.453690251525116217 ) ) ;
#14002=CARTESIAN_POINT ( 'NONE',  ( 2.619288827430985567, 0.4094970184090461762, -1.491740999229418829 ) ) ;
#14023=ORIENTED_EDGE ( 'NONE', *, *, #12194, .F. ) ;
#14030=ORIENTED_EDGE ( 'NONE', *, *, #2240, .T. ) ;
#14032=CARTESIAN_POINT ( 'NONE',  ( 107.7704431822035076, 16.89989698459580225, -1.579319589807283819 ) ) ;
#14037=CARTESIAN_POINT ( 'NONE',  ( -59.84585868070823267, -5.753144558333704417, 1.949999999999999734 ) ) ;
#14042=ADVANCED_FACE ( 'NONE', ( #22188 ), #19675, .T. ) ;
#14047=CARTESIAN_POINT ( 'NONE',  ( -27.13750370379022314, 17.93667199020026715, 1.500000000000000000 ) ) ;
#14056=EDGE_CURVE ( 'NONE', #31304, #6067, #20664, .T. ) ;
#14063=( BOUNDED_SURFACE ( )  B_SPLINE_SURFACE ( 3, 3, ( 
 ( #23512, #21190, #31728, #26200 ),
 ( #8463, #23992, #13480, #5653 ),
 ( #18660, #31542, #20851, #3487 ),
 ( #8804, #1299, #8152, #26043 ) ),
 .UNSPECIFIED., .F., .F., .F. ) 
 B_SPLINE_SURFACE_WITH_KNOTS ( ( 4, 4 ),
 ( 4, 4 ),
 ( 0.000000000000000000, 1.000000000000000000 ),
 ( 0.000000000000000000, 1.000000000000000000 ),
 .UNSPECIFIED. ) 
 GEOMETRIC_REPRESENTATION_ITEM ( )  RATIONAL_B_SPLINE_SURFACE ( (
 ( 1.000000000000000000, 0.9321687722090974404, 0.9321687722090974404, 1.000000000000000000),
 ( 0.6539698177806696489, 0.6096102421024139906, 0.6096102421024139906, 0.6539698177806696489),
 ( 0.6539698177806696489, 0.6096102421024139906, 0.6096102421024139906, 0.6539698177806696489),
 ( 1.000000000000000000, 0.9321687722090974404, 0.9321687722090974404, 1.000000000000000000) ) ) 
 REPRESENTATION_ITEM ( '' )  SURFACE ( )  );
#14084=EDGE_CURVE ( 'NONE', #32977, #30284, #10185, .T. ) ;
#14087=LINE ( 'NONE', #19107, #2903 ) ;
#14089=FACE_OUTER_BOUND ( 'NONE', #32386, .T. ) ;
#14097=FACE_OUTER_BOUND ( 'NONE', #15142, .T. ) ;
#14110=ORIENTED_EDGE ( 'NONE', *, *, #7221, .F. ) ;
#14118=CARTESIAN_POINT ( 'NONE',  ( 17.32050807568873552, 10.00000000000002309, -4.612695725900422872 ) ) ;
#14124=DIRECTION ( 'NONE',  ( 0.000000000000000000, 0.000000000000000000, 1.000000000000000000 ) ) ;
#14146=EDGE_CURVE ( 'NONE', #14600, #29447, #14189, .T. ) ;
#14164=DIRECTION ( 'NONE',  ( 0.000000000000000000, 0.000000000000000000, -1.000000000000000000 ) ) ;
#14172=CARTESIAN_POINT ( 'NONE',  ( -59.40973711574257976, -5.237753430259554754, 5.221982333003774457 ) ) ;
#14178=CARTESIAN_POINT ( 'NONE',  ( 107.8403069887453967, 17.28892622633358656, -3.570939384223136059 ) ) ;
#14189=LINE ( 'NONE', #6682, #4880 ) ;
#14193=CARTESIAN_POINT ( 'NONE',  ( 10.07279555557439998, 2.216694168388106068, -1.500000000000000222 ) ) ;
#14205=B_SPLINE_CURVE_WITH_KNOTS ( 'NONE', 3,
 ( #5259, #32693, #9935, #12609, #20652, #9773, #2759 ),
 .UNSPECIFIED., .F., .F.,
 ( 4, 3, 4 ),
 ( 1.015220885719448636E-17, 0.002676966304866045410, 0.003456443485869430642 ),
 .UNSPECIFIED. ) ;
#14206=CARTESIAN_POINT ( 'NONE',  ( -38.14293509397969473, 10.97000000000000419, 1.500000000000000000 ) ) ;
#14207=DIRECTION ( 'NONE',  ( 0.000000000000000000, -0.9271838545667856479, -0.3746065934159164001 ) ) ;
#14212=VERTEX_POINT ( 'NONE', #24894 ) ;
#14225=ADVANCED_FACE ( 'NONE', ( #19894 ), #30109, .T. ) ;
#14230=VERTEX_POINT ( 'NONE', #6505 ) ;
#14231=CARTESIAN_POINT ( 'NONE',  ( 12.22604216692669254, 4.899348761096485205, -1.499999999999763300 ) ) ;
#14232=CARTESIAN_POINT ( 'NONE',  ( 8.870145747188287189, 0.000000000000000000, -1.000000000000000222 ) ) ;
#14241=CARTESIAN_POINT ( 'NONE',  ( 8.585585455345263739, 0.000000000000000000, -1.000000000000000000 ) ) ;
#14246=EDGE_CURVE ( 'NONE', #18415, #5412, #15197, .T. ) ;
#14249=CARTESIAN_POINT ( 'NONE',  ( 0.6708088701982984903, 0.000000000000000000, -4.612695725900422872 ) ) ;
#14254=CARTESIAN_POINT ( 'NONE',  ( 108.1960732670207079, 19.26997324246909926, 4.630839363390458985 ) ) ;
#14260=ORIENTED_EDGE ( 'NONE', *, *, #4736, .F. ) ;
#14269=CARTESIAN_POINT ( 'NONE',  ( -56.77852586542613267, 0.3797334620625366086, -1.050000000000000044 ) ) ;
#14272=( BOUNDED_SURFACE ( )  B_SPLINE_SURFACE ( 1, 3, ( 
 ( #15210, #7505, #27920, #15524 ),
 ( #32949, #30782, #5032, #25738 ) ),
 .UNSPECIFIED., .F., .F., .F. ) 
 B_SPLINE_SURFACE_WITH_KNOTS ( ( 2, 2 ),
 ( 4, 4 ),
 ( 0.000000000000000000, 1.000000000000000000 ),
 ( 0.000000000000000000, 1.000000000000000000 ),
 .UNSPECIFIED. ) 
 GEOMETRIC_REPRESENTATION_ITEM ( )  RATIONAL_B_SPLINE_SURFACE ( (
 ( 1.000000000000000000, 0.9321687722090974404, 0.9321687722090974404, 1.000000000000000000),
 ( 1.000000000000000000, 0.9321687722090974404, 0.9321687722090974404, 1.000000000000000000) ) ) 
 REPRESENTATION_ITEM ( '' )  SURFACE ( )  );
#14284=ORIENTED_EDGE ( 'NONE', *, *, #11205, .T. ) ;
#14290=ORIENTED_EDGE ( 'NONE', *, *, #2889, .T. ) ;
#14310=LINE ( 'NONE', #4143, #20421 ) ;
#14311=CARTESIAN_POINT ( 'NONE',  ( 26.07786135537692473, 19.05625643470508024, 1.113327811892661501 ) ) ;
#14319=DIRECTION ( 'NONE',  ( 1.000000000000000000, 2.650271977186794621E-15, 0.000000000000000000 ) ) ;
#14325=CYLINDRICAL_SURFACE ( 'NONE', #5541, 0.5000000000000004441 ) ;
#14344=DIRECTION ( 'NONE',  ( -1.067350013832299672E-17, 0.4539904997395510788, -0.8910065241883655673 ) ) ;
#14347=DIRECTION ( 'NONE',  ( 0.8660254037844427044, -0.4999999999999931721, 0.000000000000000000 ) ) ;
#14356=DIRECTION ( 'NONE',  ( 0.000000000000000000, -0.9271838545667855369, -0.3746065934159163446 ) ) ;
#14362=AXIS2_PLACEMENT_3D ( 'NONE', #14558, #10146, #7668 ) ;
#14369=EDGE_LOOP ( 'NONE', ( #30944, #2222, #14532, #28254, #32631 ) ) ;
#14379=CARTESIAN_POINT ( 'NONE',  ( 21.53922796474764567, 16.55061608779757520, -1.500000000000000000 ) ) ;
#14387=TOROIDAL_SURFACE ( 'NONE', #11211, 10.43371088333261731, 0.4500000000000000111 ) ;
#14393=VECTOR ( 'NONE', #30960, 1000.000000000000000 ) ;
#14397=CARTESIAN_POINT ( 'NONE',  ( -23.54713438637982748, 5.934235225036485595, 7.654118351624816796 ) ) ;
#14404=ORIENTED_EDGE ( 'NONE', *, *, #774, .F. ) ;
#14406=AXIS2_PLACEMENT_3D ( 'NONE', #10928, #31180, #18280 ) ;
#14408=CARTESIAN_POINT ( 'NONE',  ( 13.62547635268498780, 21.94000000000002970, 1.500000000000000000 ) ) ;
#14418=AXIS2_PLACEMENT_3D ( 'NONE', #18645, #450, #28357 ) ;
#14439=AXIS2_PLACEMENT_3D ( 'NONE', #14842, #9347, #25041 ) ;
#14465=CARTESIAN_POINT ( 'NONE',  ( -23.54713438637982748, 10.22246055240786333, 9.386673846173426483 ) ) ;
#14474=CIRCLE ( 'NONE', #8615, 0.4500000000000000111 ) ;
#14475=CIRCLE ( 'NONE', #18768, 0.4500000000000013989 ) ;
#14481=CARTESIAN_POINT ( 'NONE',  ( 26.02102126874770249, 19.05032542655294137, 1.189564967197544343 ) ) ;
#14488=ORIENTED_EDGE ( 'NONE', *, *, #14246, .T. ) ;
#14493=EDGE_CURVE ( 'NONE', #28865, #18809, #2769, .T. ) ;
#14500=CARTESIAN_POINT ( 'NONE',  ( 108.0946672814455525, 20.79497283818417230, 1.508486338784366998 ) ) ;
#14503=CARTESIAN_POINT ( 'NONE',  ( -58.12441765334286004, -3.826327783517069481, 5.759795199666357668 ) ) ;
#14512=VERTEX_POINT ( 'NONE', #18866 ) ;
#14521=AXIS2_PLACEMENT_3D ( 'NONE', #12997, #617, #23687 ) ;
#14532=ORIENTED_EDGE ( 'NONE', *, *, #21315, .T. ) ;
#14536=CARTESIAN_POINT ( 'NONE',  ( 107.3062245775731895, 17.12232141698407517, 3.051466462891762266 ) ) ;
#14539=EDGE_CURVE ( 'NONE', #5929, #25797, #24627, .T. ) ;
#14540=CARTESIAN_POINT ( 'NONE',  ( -27.92832289637407328, 17.36640870223426347, 1.500000000000000000 ) ) ;
#14547=AXIS2_PLACEMENT_3D ( 'NONE', #6972, #1642, #14319 ) ;
#14555=LINE ( 'NONE', #32314, #3333 ) ;
#14556=CIRCLE ( 'NONE', #25237, 0.4500000000000007327 ) ;
#14558=CARTESIAN_POINT ( 'NONE',  ( 56.97280603064898941, -277.2763395528616002, 1.508259000770582059 ) ) ;
#14565=ORIENTED_EDGE ( 'NONE', *, *, #14721, .F. ) ;
#14570=ORIENTED_EDGE ( 'NONE', *, *, #4084, .F. ) ;
#14575=AXIS2_PLACEMENT_3D ( 'NONE', #2854, #11005, #10842 ) ;
#14576=CARTESIAN_POINT ( 'NONE',  ( 19.52627448105246444, 15.61656174521109364, -1.500000000000000000 ) ) ;
#14590=FACE_OUTER_BOUND ( 'NONE', #29837, .T. ) ;
#14598=CARTESIAN_POINT ( 'NONE',  ( 8.911384905465473238, 0.2172754300402908179, -1.412391582771881371 ) ) ;
#14600=VERTEX_POINT ( 'NONE', #11328 ) ;
#14604=CIRCLE ( 'NONE', #1813, 5.100000000000000533 ) ;
#14609=CARTESIAN_POINT ( 'NONE',  ( -59.84585868070823267, -5.753144558333701752, 1.949999999999999956 ) ) ;
#14614=ORIENTED_EDGE ( 'NONE', *, *, #23158, .T. ) ;
#14618=CARTESIAN_POINT ( 'NONE',  ( -56.48155856471830560, 0.04209818965781165351, -1.019622293805160007 ) ) ;
#14627=EDGE_CURVE ( 'NONE', #30284, #21159, #11086, .T. ) ;
#14633=DIRECTION ( 'NONE',  ( 1.000000000000000000, 0.000000000000000000, 0.000000000000000000 ) ) ;
#14638=DIRECTION ( 'NONE',  ( 0.000000000000000000, -1.000000000000000000, 0.000000000000000000 ) ) ;
#14642=EDGE_CURVE ( 'NONE', #29668, #23825, #18236, .T. ) ;
#14647=MECHANICAL_CONTEXT ( 'NONE', #19317, 'mechanical' ) ;
#14650=VERTEX_POINT ( 'NONE', #11814 ) ;
#14662=ORIENTED_EDGE ( 'NONE', *, *, #822, .F. ) ;
#14663=CARTESIAN_POINT ( 'NONE',  ( 108.1033629032233847, 18.75372535508294902, -4.515627687203030760 ) ) ;
#14666=EDGE_CURVE ( 'NONE', #18809, #4208, #32137, .T. ) ;
#14667=DIRECTION ( 'NONE',  ( -0.000000000000000000, -0.000000000000000000, -1.000000000000000000 ) ) ;
#14670=VECTOR ( 'NONE', #26452, 1000.000000000000000 ) ;
#14699=CARTESIAN_POINT ( 'NONE',  ( 107.5137442065068996, 18.28919312501354710, 5.093186791727767115 ) ) ;
#14703=CARTESIAN_POINT ( 'NONE',  ( -57.40374817251313999, -2.616512360834426953, 5.500000000000000000 ) ) ;
#14704=PLANE ( 'NONE',  #12463 ) ;
#14711=CARTESIAN_POINT ( 'NONE',  ( -16.91347898512169934, 12.16064947808539998, 1.928605623396539404 ) ) ;
#14712=DIRECTION ( 'NONE',  ( -0.000000000000000000, -0.000000000000000000, -1.000000000000000000 ) ) ;
#14721=EDGE_CURVE ( 'NONE', #2170, #6161, #10750, .T. ) ;
#14738=CARTESIAN_POINT ( 'NONE',  ( 21.53922796458296318, 16.55061608804989604, -1.050000000000000044 ) ) ;
#14739=CARTESIAN_POINT ( 'NONE',  ( 9.236821176939058020, 0.1505923090604457948, -1.036667534179769756 ) ) ;
#14748=CARTESIAN_POINT ( 'NONE',  ( 108.2917183403186812, 19.80256275033599778, -2.304437341803263095 ) ) ;
#14761=CARTESIAN_POINT ( 'NONE',  ( 107.6996442589674103, 19.35565155597527109, 4.629213727441584325 ) ) ;
#14764=B_SPLINE_CURVE_WITH_KNOTS ( 'NONE', 3,
 ( #10143, #14500, #20202, #14989, #20364, #30398 ),
 .UNSPECIFIED., .F., .F.,
 ( 4, 2, 4 ),
 ( 0.000000000000000000, 0.0003973515176470922890, 0.0007947030352941845781 ),
 .UNSPECIFIED. ) ;
#14768=VERTEX_POINT ( 'NONE', #410 ) ;
#14779=DIRECTION ( 'NONE',  ( -0.000000000000000000, -0.000000000000000000, 1.000000000000000000 ) ) ;
#14783=CARTESIAN_POINT ( 'NONE',  ( -1.152183934781129714E-14, 21.49000000000002331, 1.050000000000000044 ) ) ;
#14792=CARTESIAN_POINT ( 'NONE',  ( 107.2582456157670805, 16.85513498755496542, -2.462483528952394529 ) ) ;
#14796=CARTESIAN_POINT ( 'NONE',  ( 0.000000000000000000, 0.000000000000000000, 0.000000000000000000 ) ) ;
#14798=DIRECTION ( 'NONE',  ( -0.000000000000000000, 0.000000000000000000, 1.000000000000000000 ) ) ;
#14805=CARTESIAN_POINT ( 'NONE',  ( 9.256647899302816285, 0.1794474037904786601, -1.452724983837345718 ) ) ;
#14807=CARTESIAN_POINT ( 'NONE',  ( -23.54713438637982748, 8.429255322705477838, 8.219131494323725917 ) ) ;
#14820=CARTESIAN_POINT ( 'NONE',  ( -56.29156811815547456, 0.01555455218834706291, -1.127217129886184832 ) ) ;
#14821=DIRECTION ( 'NONE',  ( 1.000000000000000000, -5.637851296924461498E-14, 0.000000000000000000 ) ) ;
#14836=CARTESIAN_POINT ( 'NONE',  ( -56.30345176035514498, 0.06347132377568256989, -1.252366240086452365 ) ) ;
#14842=CARTESIAN_POINT ( 'NONE',  ( -41.30970132048468457, -16.45499999999997343, 0.000000000000000000 ) ) ;
#14846=EDGE_LOOP ( 'NONE', ( #23400, #3575, #22288, #32180 ) ) ;
#14856=CARTESIAN_POINT ( 'NONE',  ( 17.32050807568873552, 10.00000000000002309, 1.508259000770582059 ) ) ;
#14860=CARTESIAN_POINT ( 'NONE',  ( -21.68109753780534632, 18.70748839123718454, 1.500000000000000000 ) ) ;
#14864=( BOUNDED_SURFACE ( )  B_SPLINE_SURFACE ( 3, 2, ( 
 ( #31974, #29140, #23938 ),
 ( #21766, #18771, #3423 ),
 ( #9223, #24101, #24428 ),
 ( #9042, #6227, #21615 ),
 ( #4065, #14231, #28976 ),
 ( #19451, #29644, #6562 ),
 ( #13584, #16080, #26619 ),
 ( #3723, #16761, #23790 ),
 ( #902, #19101, #11080 ),
 ( #3576, #21279, #26962 ),
 ( #16571, #1227, #26783 ),
 ( #11420, #31478, #31819 ),
 ( #8891, #6076, #29289 ),
 ( #6375, #26477, #3900 ),
 ( #14576, #1717, #2394 ),
 ( #11915, #2206, #22611 ),
 ( #17063, #14379, #14738 ),
 ( #19755, #25090, #4563 ),
 ( #22771, #27461, #12392 ),
 ( #4393, #32822, #24590 ),
 ( #27275, #29961, #24780 ),
 ( #32978, #10046, #24935 ),
 ( #6725, #9542, #25277 ),
 ( #32331, #12566, #12075 ) ),
 .UNSPECIFIED., .F., .F., .F. ) 
 B_SPLINE_SURFACE_WITH_KNOTS ( ( 4, 2, 2, 2, 2, 2, 2, 2, 2, 2, 2, 4 ),
 ( 3, 3 ),
 ( 0.009504881860343756053, 0.01278571900407518211, 0.01606655614780660990, 0.01934739329153803422, 0.02098781186340374638, 0.02262823043526946201, 0.02590906757900088980, 0.02918990472273231412, 0.03083032329459802975, 0.03247074186646374538, 0.03411116043832945754, 0.03575157901019516971 ),
 ( 0.000000000000000000, 1.000000000000000000 ),
 .UNSPECIFIED. ) 
 GEOMETRIC_REPRESENTATION_ITEM ( )  RATIONAL_B_SPLINE_SURFACE ( (
 ( 1.000000000000000000, 0.7071067811865475727, 1.000000000000000000),
 ( 1.000000000000000000, 0.7071067811865475727, 1.000000000000000000),
 ( 1.000000000000000000, 0.7071067811865475727, 1.000000000000000000),
 ( 1.000000000000000000, 0.7071067811865475727, 1.000000000000000000),
 ( 1.000000000000000000, 0.7071067811865471286, 1.000000000000000000),
 ( 1.000000000000000000, 0.7071067811865471286, 1.000000000000000000),
 ( 1.000000000000000000, 0.7071067811865475727, 1.000000000000000000),
 ( 1.000000000000000000, 0.7071067811865475727, 1.000000000000000000),
 ( 1.000000000000000000, 0.7071067811865486830, 1.000000000000000000),
 ( 1.000000000000000000, 0.7071067811865486830, 1.000000000000000000),
 ( 1.000000000000000000, 0.7071067811865475727, 1.000000000000000000),
 ( 1.000000000000000000, 0.7071067811865475727, 1.000000000000000000),
 ( 1.000000000000000000, 0.7071067811865475727, 1.000000000000000000),
 ( 1.000000000000000000, 0.7071067811865475727, 1.000000000000000000),
 ( 1.000000000000000000, 0.7071067811865475727, 1.000000000000000000),
 ( 1.000000000000000000, 0.7071067811865475727, 1.000000000000000000),
 ( 1.000000000000000000, 0.7071067811865475727, 1.000000000000000000),
 ( 1.000000000000000000, 0.7071067811865475727, 1.000000000000000000),
 ( 1.000000000000000000, 0.7071067811865475727, 1.000000000000000000),
 ( 1.000000000000000000, 0.7071067811865475727, 1.000000000000000000),
 ( 1.000000000000000000, 0.7071067811865475727, 1.000000000000000000),
 ( 1.000000000000000000, 0.7071067811865475727, 1.000000000000000000),
 ( 1.000000000000000000, 0.7071067811865475727, 1.000000000000000000),
 ( 1.000000000000000000, 0.7071067811865475727, 1.000000000000000000) ) ) 
 REPRESENTATION_ITEM ( '' )  SURFACE ( )  );
#14876=CARTESIAN_POINT ( 'NONE',  ( 108.0381478102898853, 18.39058198498274876, -4.599267682029278603 ) ) ;
#14897=CARTESIAN_POINT ( 'NONE',  ( 108.2036592059122171, 19.31221474348546607, -3.351118779959896266 ) ) ;
#14901=DIRECTION ( 'NONE',  ( -0.000000000000000000, -0.000000000000000000, -1.000000000000000000 ) ) ;
#14906=CIRCLE ( 'NONE', #31492, 0.5000000000000000000 ) ;
#14925=EDGE_LOOP ( 'NONE', ( #8588, #30540, #3794, #19749 ) ) ;
#14932=DIRECTION ( 'NONE',  ( -0.000000000000000000, 0.000000000000000000, 1.000000000000000000 ) ) ;
#14940=VECTOR ( 'NONE', #32431, 1000.000000000000114 ) ;
#14959=EDGE_CURVE ( 'NONE', #32661, #536, #89, .T. ) ;
#14964=DIRECTION ( 'NONE',  ( 8.326672684688674053E-17, 0.3746065934159164001, -0.9271838545667857590 ) ) ;
#14975=DIRECTION ( 'NONE',  ( -0.000000000000000000, -0.3746065934159164001, 0.9271838545667856479 ) ) ;
#14978=CARTESIAN_POINT ( 'NONE',  ( -56.32770133515839461, 0.5000000000000000000, -1.500000000000000000 ) ) ;
#14987=AXIS2_PLACEMENT_3D ( 'NONE', #3372, #26437, #28753 ) ;
#14989=CARTESIAN_POINT ( 'NONE',  ( 108.3631457176462618, 20.50192626814461860, 1.454023645857057678 ) ) ;
#14995=EDGE_LOOP ( 'NONE', ( #14110, #32382, #7190, #27134 ) ) ;
#15002=AXIS2_PLACEMENT_3D ( 'NONE', #20142, #9927, #30337 ) ;
#15018=ORIENTED_EDGE ( 'NONE', *, *, #15727, .T. ) ;
#15021=AXIS2_PLACEMENT_3D ( 'NONE', #9474, #22528, #30076 ) ;
#15042=ORIENTED_EDGE ( 'NONE', *, *, #20840, .T. ) ;
#15044=CARTESIAN_POINT ( 'NONE',  ( 108.0553047662118331, 18.48611868536735514, -4.631814065063916352 ) ) ;
#15045=CIRCLE ( 'NONE', #24640, 0.5000000000000004441 ) ;
#15047=CARTESIAN_POINT ( 'NONE',  ( -17.06946722187133147, 9.668269422107719890, 1.993141146079933312 ) ) ;
#15051=VERTEX_POINT ( 'NONE', #1719 ) ;
#15056=VECTOR ( 'NONE', #18482, 1000.000000000000227 ) ;
#15102=EDGE_LOOP ( 'NONE', ( #26135, #27563, #18025, #32518, #31885 ) ) ;
#15117=CARTESIAN_POINT ( 'NONE',  ( 45.78962651942645579, 26.61627915917710041, -1.491740999229417941 ) ) ;
#15129=EDGE_CURVE ( 'NONE', #18014, #23780, #25841, .T. ) ;
#15137=CARTESIAN_POINT ( 'NONE',  ( -40.71733131760397129, -12.43974741078717372, 5.871858320049880398 ) ) ;
#15142=EDGE_LOOP ( 'NONE', ( #2387, #22137, #20644, #12791, #20356 ) ) ;
#15151=( BOUNDED_SURFACE ( )  B_SPLINE_SURFACE ( 3, 2, ( 
 ( #14978, #7309, #7654 ),
 ( #17500, #27696, #4800 ),
 ( #7162, #2318, #5302 ),
 ( #12996, #27548, #32751 ),
 ( #30077, #4988, #30748 ),
 ( #17853, #9639, #30567 ),
 ( #9828, #25375, #2484 ),
 ( #10324, #22709, #25694 ),
 ( #7819, #32911, #20044 ),
 ( #25019, #17356, #18012 ),
 ( #2132, #9981, #20191 ),
 ( #30388, #10130, #4645 ),
 ( #14820, #28201, #2815 ),
 ( #12313, #22529, #7460 ),
 ( #30238, #15480, #25529 ),
 ( #17661, #28051, #27870 ) ),
 .UNSPECIFIED., .F., .F., .F. ) 
 B_SPLINE_SURFACE_WITH_KNOTS ( ( 4, 2, 2, 2, 2, 2, 2, 4 ),
 ( 3, 3 ),
 ( 0.0003684723101340264297, 0.0003800852853942607453, 0.0003916982606544950609, 0.0004033112359147293766, 0.0004149242111749636922, 0.0004381501616954323235, 0.0004497631369556666934, 0.0004613761122159010090 ),
 ( 0.000000000000000000, 1.000000000000000000 ),
 .UNSPECIFIED. ) 
 GEOMETRIC_REPRESENTATION_ITEM ( )  RATIONAL_B_SPLINE_SURFACE ( (
 ( 1.000000000000000000, 0.7071067811865529018, 1.000000000000000000),
 ( 1.000000000000000000, 0.7069009979025784318, 1.000000000000000000),
 ( 1.000000000000000000, 0.7132090502674284238, 1.000000000000000000),
 ( 1.000000000000000000, 0.7358066242641170263, 1.000000000000000000),
 ( 1.000000000000000000, 0.7518633517842446823, 1.000000000000000000),
 ( 1.000000000000000000, 0.7874886208250170272, 1.000000000000000000),
 ( 1.000000000000000000, 0.8071925469186636004, 1.000000000000000000),
 ( 1.000000000000000000, 0.8453094253659971802, 1.000000000000000000),
 ( 1.000000000000000000, 0.8640810776869900511, 1.000000000000000000),
 ( 1.000000000000000000, 0.9164353439694726822, 1.000000000000000000),
 ( 1.000000000000000000, 0.9447016862624076916, 1.000000000000000000),
 ( 1.000000000000000000, 0.9748905170909382134, 1.000000000000000000),
 ( 1.000000000000000000, 0.9828855915604548521, 1.000000000000000000),
 ( 1.000000000000000000, 0.9943518368180752631, 1.000000000000000000),
 ( 1.000000000000000000, 0.9980588531602458957, 1.000000000000000000),
 ( 1.000000000000000000, 0.9983060766582193546, 1.000000000000000000) ) ) 
 REPRESENTATION_ITEM ( '' )  SURFACE ( )  );
#15166=CARTESIAN_POINT ( 'NONE',  ( -38.14293509397970183, 21.49000000000000199, 1.500000000000000000 ) ) ;
#15197=LINE ( 'NONE', #15701, #16042 ) ;
#15210=CARTESIAN_POINT ( 'NONE',  ( 11.04311965146447427, 15.00000000000002132, -1.491740999229419273 ) ) ;
#15215=CARTESIAN_POINT ( 'NONE',  ( -24.41293782978024041, 3.998227953278250535, 2.146185852361514268 ) ) ;
#15220=ORIENTED_EDGE ( 'NONE', *, *, #3636, .T. ) ;
#15225=CARTESIAN_POINT ( 'NONE',  ( 107.5866720633429878, 18.70855422806117474, -5.131518431764148680 ) ) ;
#15227=CARTESIAN_POINT ( 'NONE',  ( -23.08853323649765343, 18.46223496596753932, 1.773004750130224627 ) ) ;
#15237=DIRECTION ( 'NONE',  ( -0.000000000000000000, -0.000000000000000000, -1.000000000000000000 ) ) ;
#15246=CYLINDRICAL_SURFACE ( 'NONE', #10268, 0.5000000000000000000 ) ;
#15263=CARTESIAN_POINT ( 'NONE',  ( -41.86373177837820236, -16.13513036599589867, 5.128141679950118714 ) ) ;
#15266=DIRECTION ( 'NONE',  ( -0.000000000000000000, 0.000000000000000000, 1.000000000000000000 ) ) ;
#15270=CARTESIAN_POINT ( 'NONE',  ( -23.85705198072715660, 13.77387538314364335, 1.500000000000000000 ) ) ;
#15290=ADVANCED_FACE ( 'NONE', ( #22386 ), #8634, .T. ) ;
#15320=EDGE_CURVE ( 'NONE', #7656, #6904, #20939, .T. ) ;
#15321=EDGE_CURVE ( 'NONE', #21704, #4740, #18658, .T. ) ;
#15324=FACE_OUTER_BOUND ( 'NONE', #16446, .T. ) ;
#15325=CARTESIAN_POINT ( 'NONE',  ( -1.176310634206514104E-14, 21.94000000000002260, -1.050000000000000044 ) ) ;
#15331=CARTESIAN_POINT ( 'NONE',  ( 107.4927781683577734, 18.16905313753168016, 5.010584227462816287 ) ) ;
#15348=DIRECTION ( 'NONE',  ( 0.4999999999999977796, 0.8660254037844398178, 0.000000000000000000 ) ) ;
#15362=CARTESIAN_POINT ( 'NONE',  ( -28.64263641446437347, 5.485000000000014531, 1.500000000000000000 ) ) ;
#15367=CARTESIAN_POINT ( 'NONE',  ( 8.911384905465473238, 0.2172754300402719996, 1.412391582771868492 ) ) ;
#15373=ORIENTED_EDGE ( 'NONE', *, *, #29310, .T. ) ;
#15375=ORIENTED_EDGE ( 'NONE', *, *, #17467, .F. ) ;
#15376=CARTESIAN_POINT ( 'NONE',  ( -22.41343429466623149, 4.100545212957339203, 2.143340414843532660 ) ) ;
#15387=ORIENTED_EDGE ( 'NONE', *, *, #13433, .F. ) ;
#15394=VERTEX_POINT ( 'NONE', #12532 ) ;
#15395=LINE ( 'NONE', #13218, #17834 ) ;
#15396=CARTESIAN_POINT ( 'NONE',  ( -27.70590053552606591, 16.86946294693127157, 1.811428998031433535 ) ) ;
#15398=DIRECTION ( 'NONE',  ( -0.4999999999999981681, -0.8660254037844395958, 0.000000000000000000 ) ) ;
#15419=DIRECTION ( 'NONE',  ( -0.9895623637898895986, 0.1441052676711233327, 0.000000000000000000 ) ) ;
#15446=EDGE_CURVE ( 'NONE', #18474, #32515, #21790, .T. ) ;
#15452=EDGE_CURVE ( 'NONE', #25811, #13759, #23465, .T. ) ;
#15455=DIRECTION ( 'NONE',  ( 0.2951703194034057121, -0.3797261271633443069, -0.8767454310646958238 ) ) ;
#15467=CARTESIAN_POINT ( 'NONE',  ( 22.28390758787569581, 17.05912403623761975, 1.049999999999999822 ) ) ;
#15470=FACE_OUTER_BOUND ( 'NONE', #30885, .T. ) ;
#15475=FACE_OUTER_BOUND ( 'NONE', #16258, .T. ) ;
#15480=CARTESIAN_POINT ( 'NONE',  ( -56.31169168320045770, 1.934928713445239489E-05, -1.021773151746335095 ) ) ;
#15488=CARTESIAN_POINT ( 'NONE',  ( 108.1273057862948974, 18.88704877543205640, 5.058538142693402406 ) ) ;
#15494=EDGE_LOOP ( 'NONE', ( #23674, #4241, #29166, #24762 ) ) ;
#15507=VECTOR ( 'NONE', #301, 1000.000000000000000 ) ;
#15514=CARTESIAN_POINT ( 'NONE',  ( 108.1608273670511267, 19.07371016407039122, -3.860697231985633415 ) ) ;
#15521=VERTEX_POINT ( 'NONE', #19031 ) ;
#15522=EDGE_CURVE ( 'NONE', #26215, #22604, #15045, .T. ) ;
#15524=CARTESIAN_POINT ( 'NONE',  ( 17.41559371906258136, 18.02474698348859050, -1.491740999229419273 ) ) ;
#15527=AXIS2_PLACEMENT_3D ( 'NONE', #30302, #7881, #2706 ) ;
#15533=FACE_OUTER_BOUND ( 'NONE', #32442, .T. ) ;
#15543=EDGE_LOOP ( 'NONE', ( #25699, #27488 ) ) ;
#15545=ORIENTED_EDGE ( 'NONE', *, *, #8473, .F. ) ;
#15546=CARTESIAN_POINT ( 'NONE',  ( -17.11424327971897696, 13.04685258179087626, 1.906190955135662168 ) ) ;
#15565=DIRECTION ( 'NONE',  ( -0.000000000000000000, -0.000000000000000000, -1.000000000000000000 ) ) ;
#15569=VECTOR ( 'NONE', #2072, 1000.000000000000000 ) ;
#15573=CARTESIAN_POINT ( 'NONE',  ( -26.39604612056346511, 17.76592253751580586, 1.789727549128061757 ) ) ;
#15577=CARTESIAN_POINT ( 'NONE',  ( -56.27770248097862549, 0.4996615022747108448, 1.500000000000000000 ) ) ;
#15585=AXIS2_PLACEMENT_3D ( 'NONE', #18082, #2717, #28461 ) ;
#15597=CARTESIAN_POINT ( 'NONE',  ( -41.86373177837820236, -16.13513036599589867, 5.128141679950118714 ) ) ;
#15605=DIRECTION ( 'NONE',  ( -0.8896831085035101783, 0.4565785435645562940, 0.000000000000000000 ) ) ;
#15629=CARTESIAN_POINT ( 'NONE',  ( 13.58267262069031922, 21.92668125727452733, -1.161744080134329726 ) ) ;
#15641=CONICAL_SURFACE ( 'NONE', #6017, 5.999999999999999112, 0.08726646259971666819 ) ;
#15664=DIRECTION ( 'NONE',  ( 0.1767573132311699713, 0.9842544651762054064, 0.000000000000000000 ) ) ;
#15666=AXIS2_PLACEMENT_3D ( 'NONE', #24837, #32536, #14638 ) ;
#15673=FACE_OUTER_BOUND ( 'NONE', #3107, .T. ) ;
#15680=EDGE_CURVE ( 'NONE', #10104, #1079, #5474, .T. ) ;
#15686=CIRCLE ( 'NONE', #5559, 9.713116299512234875 ) ;
#15701=CARTESIAN_POINT ( 'NONE',  ( 2.382865613620175349, 0.000000000000000000, -1.491740999229418829 ) ) ;
#15706=EDGE_CURVE ( 'NONE', #11079, #15980, #9739, .T. ) ;
#15707=CARTESIAN_POINT ( 'NONE',  ( -53.96180052795275373, 5.510921350264005092, 1.087562001069957152 ) ) ;
#15714=EDGE_CURVE ( 'NONE', #13391, #7656, #4413, .T. ) ;
#15720=CARTESIAN_POINT ( 'NONE',  ( 8.901867736793459329, 0.07845480144339982143, 1.317219896051721406 ) ) ;
#15725=DIRECTION ( 'NONE',  ( 0.2880220749472559572, 0.1662896225033555220, -0.9430753128943462071 ) ) ;
#15727=EDGE_CURVE ( 'NONE', #32925, #23049, #14310, .T. ) ;
#15733=ORIENTED_EDGE ( 'NONE', *, *, #24002, .T. ) ;
#15743=CARTESIAN_POINT ( 'NONE',  ( 13.32340444471394569, 6.787188996462521828, 1.050000000000000044 ) ) ;
#15752=CARTESIAN_POINT ( 'NONE',  ( -28.19744467622691175, 16.39278089773672420, 1.823048619078819765 ) ) ;
#15755=EDGE_CURVE ( 'NONE', #24602, #25095, #1206, .T. ) ;
#15759=ORIENTED_EDGE ( 'NONE', *, *, #618, .T. ) ;
#15760=CARTESIAN_POINT ( 'NONE',  ( -1.082681991931091270, 0.000000000000000000, 4.629213727441584325 ) ) ;
#15772=ORIENTED_EDGE ( 'NONE', *, *, #28151, .F. ) ;
#15773=( BOUNDED_CURVE ( )  B_SPLINE_CURVE ( 3, ( #27283, #4400, #19458, #1723 ),
 .UNSPECIFIED., .F., .F. ) 
 B_SPLINE_CURVE_WITH_KNOTS ( ( 4, 4 ),
 ( 3.141592653589793560, 4.712388980384691450 ),
 .UNSPECIFIED. ) 
 CURVE ( )  GEOMETRIC_REPRESENTATION_ITEM ( )  RATIONAL_B_SPLINE_CURVE ( ( 1.000000000000000000, 0.8047378541243646044, 0.8047378541243646044, 1.000000000000000000 ) ) 
 REPRESENTATION_ITEM ( '' )  );
#15777=ORIENTED_EDGE ( 'NONE', *, *, #17978, .T. ) ;
#15780=CARTESIAN_POINT ( 'NONE',  ( -2.523601663466349176, 0.4696231843230803671, -1.500000000000000000 ) ) ;
#15785=LINE ( 'NONE', #3097, #4808 ) ;
#15793=ORIENTED_EDGE ( 'NONE', *, *, #27611, .F. ) ;
#15802=ADVANCED_FACE ( 'NONE', ( #16993 ), #25014, .T. ) ;
#15803=ORIENTED_EDGE ( 'NONE', *, *, #3773, .F. ) ;
#15808=ORIENTED_EDGE ( 'NONE', *, *, #13616, .F. ) ;
#15810=ORIENTED_EDGE ( 'NONE', *, *, #11205, .F. ) ;
#15815=CYLINDRICAL_SURFACE ( 'NONE', #9635, 2.099999999999994316 ) ;
#15821=EDGE_CURVE ( 'NONE', #293, #18598, #18730, .T. ) ;
#15825=CARTESIAN_POINT ( 'NONE',  ( 2.619288827430985567, 0.4094970184090461762, -1.491740999229418829 ) ) ;
#15833=CARTESIAN_POINT ( 'NONE',  ( 107.6764431011533816, 19.22343047903795465, 4.860991410050878869 ) ) ;
#15838=ORIENTED_EDGE ( 'NONE', *, *, #15879, .F. ) ;
#15843=CARTESIAN_POINT ( 'NONE',  ( 8.924010941014284271, 0.4014965238409368142, 1.499999999990832666 ) ) ;
#15851=ORIENTED_EDGE ( 'NONE', *, *, #1519, .T. ) ;
#15854=CARTESIAN_POINT ( 'NONE',  ( 108.3527734911110088, 20.14254192115948072, 1.595847809240644288 ) ) ;
#15856=ORIENTED_EDGE ( 'NONE', *, *, #24520, .F. ) ;
#15863=CARTESIAN_POINT ( 'NONE',  ( 56.97280603064898941, -277.2763395528616002, -1.491740999229417941 ) ) ;
#15867=EDGE_CURVE ( 'NONE', #3662, #23049, #30561, .T. ) ;
#15869=EDGE_CURVE ( 'NONE', #32554, #30955, #9848, .T. ) ;
#15879=EDGE_CURVE ( 'NONE', #30480, #2170, #3008, .T. ) ;
#15885=CARTESIAN_POINT ( 'NONE',  ( 16.36487458112951643, 19.37645981759113312, -4.612695725900422872 ) ) ;
#15888=CARTESIAN_POINT ( 'NONE',  ( 16.87315779138724992, 12.21951710860944473, 1.050000000000000044 ) ) ;
#15892=DIRECTION ( 'NONE',  ( -0.4999999999999981126, -0.8660254037844395958, 0.000000000000000000 ) ) ;
#15899=CARTESIAN_POINT ( 'NONE',  ( -20.21556244645115541, 4.906976360849258256, 2.121007814587539286 ) ) ;
#15913=EDGE_LOOP ( 'NONE', ( #12840, #31362, #20167, #3513 ) ) ;
#15915=DIRECTION ( 'NONE',  ( 1.000000000000000000, 0.000000000000000000, 7.709882115452493155E-15 ) ) ;
#15924=VERTEX_POINT ( 'NONE', #2808 ) ;
#15927=CARTESIAN_POINT ( 'NONE',  ( -53.62634062816648139, 4.812476404579010492, 5.128141679950119602 ) ) ;
#15932=DIRECTION ( 'NONE',  ( -0.000000000000000000, -0.000000000000000000, -1.000000000000000000 ) ) ;
#15939=CARTESIAN_POINT ( 'NONE',  ( 13.61463604683894069, 21.93665163297713150, -1.110659530650990323 ) ) ;
#15972=CARTESIAN_POINT ( 'NONE',  ( -27.61335648245702501, 5.440830098941747295, 2.106297401565270011 ) ) ;
#15974=VERTEX_POINT ( 'NONE', #31526 ) ;
#15980=VERTEX_POINT ( 'NONE', #21178 ) ;
#15982=ADVANCED_FACE ( 'NONE', ( #13629 ), #31635, .T. ) ;
#15985=CARTESIAN_POINT ( 'NONE',  ( -29.86426557179348507, 4.845260731991870351, 5.128141679950118714 ) ) ;
#15991=ORIENTED_EDGE ( 'NONE', *, *, #15522, .F. ) ;
#15993=CARTESIAN_POINT ( 'NONE',  ( 25.39414263582314746, 18.98424558132892770, -1.448744400657052234 ) ) ;
#16007=DIRECTION ( 'NONE',  ( 0.8247831655431905329, -0.5654491399202531410, 0.000000000000000000 ) ) ;
#16018=ORIENTED_EDGE ( 'NONE', *, *, #15522, .T. ) ;
#16026=ORIENTED_EDGE ( 'NONE', *, *, #24585, .F. ) ;
#16034=CARTESIAN_POINT ( 'NONE',  ( 11.66870695124253743, 3.948484734076533442, 1.499999999999881650 ) ) ;
#16038=LINE ( 'NONE', #13072, #13869 ) ;
#16042=VECTOR ( 'NONE', #15348, 1000.000000000000114 ) ;
#16043=CARTESIAN_POINT ( 'NONE',  ( -25.33717935682962619, 4.262548611904803053, 2.138841724730499827 ) ) ;
#16045=CARTESIAN_POINT ( 'NONE',  ( -18.33450643518137113, 6.805598625771001942, 1.500000000000411893 ) ) ;
#16048=AXIS2_PLACEMENT_3D ( 'NONE', #31282, #25930, #28746 ) ;
#16051=CARTESIAN_POINT ( 'NONE',  ( 9.296291922083815606, 0.2373464012013740410, 1.049642900790956901 ) ) ;
#16060=CARTESIAN_POINT ( 'NONE',  ( -42.46793790805478608, 24.51887538314362658, -1.050000000000000044 ) ) ;
#16073=VERTEX_POINT ( 'NONE', #22161 ) ;
#16080=CARTESIAN_POINT ( 'NONE',  ( 13.87075382807543988, 7.736340727907119685, -1.499999999999170441 ) ) ;
#16098=ADVANCED_FACE ( 'NONE', ( #17116 ), #13211, .T. ) ;
#16100=CARTESIAN_POINT ( 'NONE',  ( 107.7451628514262723, 16.75912612768599885, 1.294109110054813661 ) ) ;
#16103=ORIENTED_EDGE ( 'NONE', *, *, #21010, .T. ) ;
#16116=B_SPLINE_SURFACE_WITH_KNOTS ( 'NONE', 3, 1, ( 
 ( #13726, #6214 ),
 ( #20948, #31809 ),
 ( #18446, #8253 ),
 ( #31167, #5589 ) ),
 .UNSPECIFIED., .F., .F., .F.,
 ( 4, 4 ),
 ( 2, 2 ),
 ( 0.000000000000000000, 0.9914900096613892266 ),
 ( 0.000000000000000000, 1.000000000000000000 ),
 .UNSPECIFIED. ) ;
#16136=TOROIDAL_SURFACE ( 'NONE', #20431, 10.51999999999999957, 0.4500000000000000111 ) ;
#16142=EDGE_CURVE ( 'NONE', #21273, #685, #14205, .T. ) ;
#16149=ADVANCED_FACE ( 'NONE', ( #7415 ), #28954, .T. ) ;
#16157=CARTESIAN_POINT ( 'NONE',  ( 108.1033190409114155, 18.75348111242300320, 4.532405430181406736 ) ) ;
#16160=ORIENTED_EDGE ( 'NONE', *, *, #15452, .T. ) ;
#16163=VERTEX_POINT ( 'NONE', #10088 ) ;
#16167=EDGE_CURVE ( 'NONE', #4208, #18809, #32636, .T. ) ;
#16168=B_SPLINE_CURVE_WITH_KNOTS ( 'NONE', 3,
 ( #9868, #30276, #7199, #19727, #29925, #27736, #2364, #22083, #9187, #29613, #19570, #17538, #22242, #19414, #25245, #6695, #32792, #17393 ),
 .UNSPECIFIED., .F., .F.,
 ( 4, 2, 2, 2, 2, 2, 2, 2, 4 ),
 ( 0.0006071315980451493302, 0.003701157179670942245, 0.006795182761296735159, 0.009889208342922527206, 0.01298323392454832012, 0.01607725950617410957, 0.01917128508779990248, 0.02226531066942568846, 0.02535933625105148137 ),
 .UNSPECIFIED. ) ;
#16169=CARTESIAN_POINT ( 'NONE',  ( 9.302055952158307051, 0.2457637072682087309, 1.499999999976339371 ) ) ;
#16173=AXIS2_PLACEMENT_3D ( 'NONE', #17364, #17185, #3832 ) ;
#16177=DIRECTION ( 'NONE',  ( 1.224646799147353207E-16, 1.000000000000000000, -0.000000000000000000 ) ) ;
#16185=CARTESIAN_POINT ( 'NONE',  ( 108.2963978243841296, 19.82861996404848881, 2.265613416507222144 ) ) ;
#16188=ORIENTED_EDGE ( 'NONE', *, *, #8449, .T. ) ;
#16219=LINE ( 'NONE', #26255, #24162 ) ;
#16226=AXIS2_PLACEMENT_3D ( 'NONE', #24694, #9472, #19532 ) ;
#16237=LINE ( 'NONE', #18921, #22003 ) ;
#16240=CARTESIAN_POINT ( 'NONE',  ( -21.81615113095794101, 4.185543752813694063, 2.140960162089520669 ) ) ;
#16243=CARTESIAN_POINT ( 'NONE',  ( 14.23800746264082839, 22.11259878822726321, -1.491740999229417941 ) ) ;
#16246=ORIENTED_EDGE ( 'NONE', *, *, #14493, .T. ) ;
#16256=CARTESIAN_POINT ( 'NONE',  ( 108.3926549169586764, 20.36461743673850577, -1.408140718819804738 ) ) ;
#16258=EDGE_LOOP ( 'NONE', ( #6712, #10383, #11975, #30527, #16103, #12599, #4274, #5115 ) ) ;
#16262=CARTESIAN_POINT ( 'NONE',  ( 107.8715728503188842, 17.46302688052359287, 2.802307197317986720 ) ) ;
#16264=CARTESIAN_POINT ( 'NONE',  ( -2.096054051514731231, 1.210157370878028882, 1.500000000000000000 ) ) ;
#16292=CARTESIAN_POINT ( 'NONE',  ( 0.2409471776115470198, 0.000000000000000000, 5.412820279296879811 ) ) ;
#16311=EDGE_CURVE ( 'NONE', #3200, #17057, #26322, .T. ) ;
#16331=CARTESIAN_POINT ( 'NONE',  ( 16.73992168104834377, 12.07607160919255840, -1.050000000000000266 ) ) ;
#16389=CARTESIAN_POINT ( 'NONE',  ( 9.301477900249441433, 0.2449194893134349904, 1.049999999999945643 ) ) ;
#16391=ORIENTED_EDGE ( 'NONE', *, *, #10247, .T. ) ;
#16394=CARTESIAN_POINT ( 'NONE',  ( -1.082681991931091270, 0.000000000000000000, 4.629213727441584325 ) ) ;
#16396=EDGE_CURVE ( 'NONE', #11936, #15394, #18294, .T. ) ;
#16398=EDGE_CURVE ( 'NONE', #7325, #19201, #16168, .T. ) ;
#16399=( BOUNDED_SURFACE ( )  B_SPLINE_SURFACE ( 3, 2, ( 
 ( #28897, #5826, #11351 ),
 ( #6170, #16504, #29084 ),
 ( #18888, #989, #11170 ),
 ( #26420, #26712, #844 ),
 ( #31582, #3522, #24371 ),
 ( #4005, #11021, #3353 ),
 ( #13518, #6316, #14172 ),
 ( #24027, #1488, #11664 ) ),
 .UNSPECIFIED., .F., .F., .F. ) 
 B_SPLINE_SURFACE_WITH_KNOTS ( ( 4, 2, 2, 4 ),
 ( 3, 3 ),
 ( 0.000000000000000000, 0.001031706651898130385, 0.002063413303796260770, 0.004126826607592521540 ),
 ( 0.000000000000000000, 1.000000000000000000 ),
 .UNSPECIFIED. ) 
 GEOMETRIC_REPRESENTATION_ITEM ( )  RATIONAL_B_SPLINE_SURFACE ( (
 ( 1.000000000000000000, 0.7660444431189777914, 1.000000000000000000),
 ( 1.000000000000000000, 0.8085210103976964158, 1.000000000000000000),
 ( 1.000000000000000000, 0.8435318601836696573, 1.000000000000000000),
 ( 1.000000000000000000, 0.9022997401206489521, 1.000000000000000000),
 ( 1.000000000000000000, 0.9260936007027089634, 1.000000000000000000),
 ( 1.000000000000000000, 0.9823303353968980689, 1.000000000000000000),
 ( 1.000000000000000000, 0.9997933690882994107, 1.000000000000000000),
 ( 1.000000000000000000, 1.000000000000000000, 1.000000000000000000) ) ) 
 REPRESENTATION_ITEM ( '' )  SURFACE ( )  );
#16403=EDGE_CURVE ( 'NONE', #3662, #10864, #11805, .T. ) ;
#16409=CARTESIAN_POINT ( 'NONE',  ( 107.8039775135429750, 17.08662937350926825, 1.995979254009180082 ) ) ;
#16411=DIRECTION ( 'NONE',  ( -0.8660254037844399289, 0.4999999999999978906, 0.000000000000000000 ) ) ;
#16419=DIRECTION ( 'NONE',  ( 0.000000000000000000, -0.9271838545667856479, -0.3746065934159163446 ) ) ;
#16424=LINE ( 'NONE', #13747, #7061 ) ;
#16426=EDGE_LOOP ( 'NONE', ( #19846, #4627, #6320, #8433 ) ) ;
#16428=CARTESIAN_POINT ( 'NONE',  ( 78.40736801748178664, 24.56822898102832653, -4.612695725900423760 ) ) ;
#16446=EDGE_LOOP ( 'NONE', ( #4432, #7444, #19298, #30684 ) ) ;
#16449=CARTESIAN_POINT ( 'NONE',  ( -56.77604778592783674, 0.4588835684945939963, 1.891358768140224633 ) ) ;
#16450=CARTESIAN_POINT ( 'NONE',  ( -50.81000000000000227, -10.96999999999998643, 8.628141679950115162 ) ) ;
#16457=CARTESIAN_POINT ( 'NONE',  ( 107.9638161812112003, 20.82655351785253472, -1.472934137033776736 ) ) ;
#16475=EDGE_CURVE ( 'NONE', #32977, #23825, #25785, .T. ) ;
#16478=CARTESIAN_POINT ( 'NONE',  ( 15.47903418055154390, 10.33214376877492846, -1.050000000000000044 ) ) ;
#16486=CARTESIAN_POINT ( 'NONE',  ( 15.82680059085170221, 20.06867288585792863, 4.148259000770580407 ) ) ;
#16489=ORIENTED_EDGE ( 'NONE', *, *, #12893, .F. ) ;
#16491=DIRECTION ( 'NONE',  ( 1.000000000000000000, 0.000000000000000000, 0.000000000000000000 ) ) ;
#16504=CARTESIAN_POINT ( 'NONE',  ( -57.39838859230419388, -3.103981716530615387, 5.547394276431782956 ) ) ;
#16515=VECTOR ( 'NONE', #20576, 1000.000000000000227 ) ;
#16525=ADVANCED_FACE ( 'NONE', ( #5525 ), #14272, .T. ) ;
#16534=DIRECTION ( 'NONE',  ( -1.000000000000000000, 0.000000000000000000, -0.000000000000000000 ) ) ;
#16538=CARTESIAN_POINT ( 'NONE',  ( 15.28872660057389155, 20.76088595412472415, 4.629213727441584325 ) ) ;
#16542=CARTESIAN_POINT ( 'NONE',  ( -29.24806983202759625, 15.94212570950531038, 1.500000000000000000 ) ) ;
#16549=CARTESIAN_POINT ( 'NONE',  ( -56.27770248097862549, -0.0003384977252891612984, 1.500000000000000000 ) ) ;
#16570=ORIENTED_EDGE ( 'NONE', *, *, #16396, .F. ) ;
#16571=CARTESIAN_POINT ( 'NONE',  ( 15.54097886440126963, 11.19125261692687268, -1.500000000000000000 ) ) ;
#16581=PLANE ( 'NONE',  #24816 ) ;
#16610=CARTESIAN_POINT ( 'NONE',  ( 14.89337309020629085, 18.05463290658611442, 1.508259000770581837 ) ) ;
#16612=DIRECTION ( 'NONE',  ( -1.348670067729972350E-16, 0.9848077530122080203, 0.1736481776669307198 ) ) ;
#16620=CIRCLE ( 'NONE', #26768, 0.5000000000000004441 ) ;
#16621=B_SPLINE_CURVE_WITH_KNOTS ( 'NONE', 3,
 ( #19331, #17323, #19154, #4118, #27517, #14792, #11478, #16639, #11627, #1956 ),
 .UNSPECIFIED., .F., .F.,
 ( 4, 3, 3, 4 ),
 ( 2.562756726049955231E-17, 0.001785006303531573362, 0.002677509960260540146, 0.003454325209724627699 ),
 .UNSPECIFIED. ) ;
#16623=( BOUNDED_SURFACE ( )  B_SPLINE_SURFACE ( 3, 3, ( 
 ( #21201, #4133, #31398, #24005 ),
 ( #8644, #3803, #8475, #21687 ),
 ( #21349, #18673, #28874, #19170 ),
 ( #31892, #29362, #3985, #9459 ) ),
 .UNSPECIFIED., .F., .F., .F. ) 
 B_SPLINE_SURFACE_WITH_KNOTS ( ( 4, 4 ),
 ( 4, 4 ),
 ( 0.000000000000000000, 1.000000000000000000 ),
 ( 0.000000000000000000, 1.000000000000000000 ),
 .UNSPECIFIED. ) 
 GEOMETRIC_REPRESENTATION_ITEM ( )  RATIONAL_B_SPLINE_SURFACE ( (
 ( 1.000000000000000000, 0.9321687722090974404, 0.9321687722090974404, 1.000000000000000000),
 ( 0.6539698177806696489, 0.6096102421024139906, 0.6096102421024139906, 0.6539698177806696489),
 ( 0.6539698177806696489, 0.6096102421024139906, 0.6096102421024139906, 0.6539698177806696489),
 ( 1.000000000000000000, 0.9321687722090974404, 0.9321687722090974404, 1.000000000000000000) ) ) 
 REPRESENTATION_ITEM ( '' )  SURFACE ( )  );
#16629=EDGE_CURVE ( 'NONE', #13759, #25811, #17709, .T. ) ;
#16637=ORIENTED_EDGE ( 'NONE', *, *, #7936, .T. ) ;
#16639=CARTESIAN_POINT ( 'NONE',  ( 107.2161092216380212, 16.62048478722980960, -1.959702381427974149 ) ) ;
#16659=ORIENTED_EDGE ( 'NONE', *, *, #3269, .F. ) ;
#16660=CARTESIAN_POINT ( 'NONE',  ( 8.906813281368062718, 0.1505923090604537329, 1.366675429750776161 ) ) ;
#16670=CARTESIAN_POINT ( 'NONE',  ( -53.35155202832373078, 4.402097243136373628, 5.049999999999999822 ) ) ;
#16672=LINE ( 'NONE', #26885, #8756 ) ;
#16675=CARTESIAN_POINT ( 'NONE',  ( -47.55999999999999517, -10.96999999999998643, 9.000000000000000000 ) ) ;
#16679=VECTOR ( 'NONE', #28264, 1000.000000000000000 ) ;
#16687=DIRECTION ( 'NONE',  ( 0.4999999999999978351, 0.8660254037844398178, 0.000000000000000000 ) ) ;
#16705=CARTESIAN_POINT ( 'NONE',  ( 107.7536796087345294, 16.80655079293032017, 0.4463807625373348298 ) ) ;
#16716=FACE_OUTER_BOUND ( 'NONE', #27644, .T. ) ;
#16720=ORIENTED_EDGE ( 'NONE', *, *, #26232, .T. ) ;
#16731=CARTESIAN_POINT ( 'NONE',  ( -17.84619894073145119, 15.94212570950478636, 1.500000000000000000 ) ) ;
#16761=CARTESIAN_POINT ( 'NONE',  ( 14.71918161885289855, 9.125819088444179883, -1.500000000000414557 ) ) ;
#16775=AXIS2_PLACEMENT_3D ( 'NONE', #13413, #25995, #22965 ) ;
#16798=CARTESIAN_POINT ( 'NONE',  ( 12.61464622672343516, 16.97301654637829671, 1.508259000770581837 ) ) ;
#16804=CARTESIAN_POINT ( 'NONE',  ( -56.49561586466536056, 0.04964621674521208644, 1.500000000000000000 ) ) ;
#16819=CARTESIAN_POINT ( 'NONE',  ( -41.86373177837819526, -16.13513036599590222, 5.128141679950119602 ) ) ;
#16844=CARTESIAN_POINT ( 'NONE',  ( 25.94779144751832334, 19.04267035867732361, 1.250701234898322411 ) ) ;
#16847=FACE_OUTER_BOUND ( 'NONE', #25910, .T. ) ;
#16853=ORIENTED_EDGE ( 'NONE', *, *, #1389, .F. ) ;
#16859=ORIENTED_EDGE ( 'NONE', *, *, #23847, .F. ) ;
#16871=DIRECTION ( 'NONE',  ( 1.000000000000000000, -0.000000000000000000, 0.000000000000000000 ) ) ;
#16885=EDGE_CURVE ( 'NONE', #14212, #13759, #25172, .T. ) ;
#16886=CARTESIAN_POINT ( 'NONE',  ( -23.54713438637984169, 18.60133783399175655, 1.500000000000000000 ) ) ;
#16887=CARTESIAN_POINT ( 'NONE',  ( -25.28731355807216374, 18.27315738579029158, 1.777518634818306742 ) ) ;
#16904=CARTESIAN_POINT ( 'NONE',  ( -53.45715098423449518, 5.485000000000009202, 1.500000000000000000 ) ) ;
#16909=EDGE_LOOP ( 'NONE', ( #11762, #2294 ) ) ;
#16912=PLANE ( 'NONE',  #3320 ) ;
#16932=ORIENTED_EDGE ( 'NONE', *, *, #21044, .T. ) ;
#16933=CARTESIAN_POINT ( 'NONE',  ( 8.923856355840481314, 0.3992388782433658467, -1.500000000000000000 ) ) ;
#16938=ADVANCED_FACE ( 'NONE', ( #16847 ), #27044, .F. ) ;
#16950=DIRECTION ( 'NONE',  ( 0.000000000000000000, -0.1736481776669307198, 0.9848077530122080203 ) ) ;
#16951=ORIENTED_EDGE ( 'NONE', *, *, #20985, .T. ) ;
#16958=CARTESIAN_POINT ( 'NONE',  ( 48.53640747082131668, 22.19355195243385026, 1.508259000770581393 ) ) ;
#16965=EDGE_LOOP ( 'NONE', ( #9209, #3435, #32358, #1453 ) ) ;
#16967=DIRECTION ( 'NONE',  ( -0.9563911903463312436, 0.000000000000000000, -0.2920888409849436429 ) ) ;
#16970=CARTESIAN_POINT ( 'NONE',  ( -2.794738735352966685, 0.000000000000000000, -1.491740999229417941 ) ) ;
#16974=ORIENTED_EDGE ( 'NONE', *, *, #30645, .T. ) ;
#16985=CARTESIAN_POINT ( 'NONE',  ( 8.960941058736731080, 0.001013528757994727400, 1.090795311548445667 ) ) ;
#16987=DIRECTION ( 'NONE',  ( 0.000000000000000000, 0.000000000000000000, -1.000000000000000000 ) ) ;
#16991=CARTESIAN_POINT ( 'NONE',  ( 107.6996442589674956, 19.35565155597525688, -4.612695725900422872 ) ) ;
#16993=FACE_OUTER_BOUND ( 'NONE', #2606, .T. ) ;
#16994=CARTESIAN_POINT ( 'NONE',  ( 25.22852577301904020, 18.96657818733213574, 1.477421824444246967 ) ) ;
#17001=ORIENTED_EDGE ( 'NONE', *, *, #22071, .T. ) ;
#17023=EDGE_LOOP ( 'NONE', ( #32851, #8258, #13074, #13327, #27460 ) ) ;
#17036=CARTESIAN_POINT ( 'NONE',  ( -27.63096596336819744, 17.00757181511110971, 1.808020238517759282 ) ) ;
#17037=CYLINDRICAL_SURFACE ( 'NONE', #25260, 0.5000000000000004441 ) ;
#17046=DIRECTION ( 'NONE',  ( -0.000000000000000000, -0.000000000000000000, -1.000000000000000000 ) ) ;
#17052=DIRECTION ( 'NONE',  ( -0.000000000000000000, -0.000000000000000000, -1.000000000000000000 ) ) ;
#17055=DIRECTION ( 'NONE',  ( 0.4999999999999977240, 0.8660254037844398178, 0.000000000000000000 ) ) ;
#17057=VERTEX_POINT ( 'NONE', #12500 ) ;
#17063=CARTESIAN_POINT ( 'NONE',  ( 21.28505181527162904, 16.92208734359699562, -1.500000000000000000 ) ) ;
#17087=CARTESIAN_POINT ( 'NONE',  ( 8.930755659325139817, 0.4999999999999980571, -1.500000000000000000 ) ) ;
#17093=ORIENTED_EDGE ( 'NONE', *, *, #25627, .F. ) ;
#17102=ORIENTED_EDGE ( 'NONE', *, *, #5669, .F. ) ;
#17106=AXIS2_PLACEMENT_3D ( 'NONE', #1037, #13570, #10918 ) ;
#17116=FACE_OUTER_BOUND ( 'NONE', #23638, .T. ) ;
#17118=CARTESIAN_POINT ( 'NONE',  ( -2.096054051514731231, 1.210157370878028882, -1.500000000000000000 ) ) ;
#17156=FACE_OUTER_BOUND ( 'NONE', #21857, .T. ) ;
#17164=CARTESIAN_POINT ( 'NONE',  ( 108.1960732670208216, 19.26997324246910992, -4.614321361849309966 ) ) ;
#17165=CARTESIAN_POINT ( 'NONE',  ( 17.41559371906258136, 18.02474698348857274, 1.500000000000000000 ) ) ;
#17166=DIRECTION ( 'NONE',  ( 0.000000000000000000, -1.000000000000000000, -5.782411586589358822E-15 ) ) ;
#17167=CARTESIAN_POINT ( 'NONE',  ( -0.2059365608663963898, 0.000000000000000000, 4.148259000770580407 ) ) ;
#17185=DIRECTION ( 'NONE',  ( -0.000000000000000000, -0.3746065934159164001, 0.9271838545667856479 ) ) ;
#17189=CARTESIAN_POINT ( 'NONE',  ( -23.54713438637982748, 12.65740340961132304, 3.359978791489319772 ) ) ;
#17201=B_SPLINE_CURVE_WITH_KNOTS ( 'NONE', 3,
 ( #10404, #2914, #30666, #3210, #10224, #28272, #20446, #15573, #25956, #7740, #3065, #18431, #15396, #23588, #15752, #23110, #25788, #23278, #10554, #30966, #13220, #23420, #527, #19536, #23910, #22206, #27386, #4313, #5857, #24514, #1019, #11052, #8708, #32261, #31450, #9322, #12010, #19691, #23761, #16043, #22040, #8527, #1828, #11203 ),
 .UNSPECIFIED., .F., .F.,
 ( 4, 2, 2, 2, 2, 2, 2, 2, 2, 2, 2, 2, 2, 2, 2, 2, 2, 2, 2, 2, 2, 4 ),
 ( 0.000000000000000000, 0.0006857049238397940321, 0.001371409847679588064, 0.002742819695359173960, 0.003428524619198961704, 0.004114229543038749014, 0.004799934466878537191, 0.005485639390718325369, 0.006857049238397909530, 0.008228459086077491089, 0.009599868933757074382, 0.01028557385759686950, 0.01097127878143666288, 0.01234268862911625485, 0.01371409847679585028, 0.01508550832447544225, 0.01645691817215503422, 0.01782832801983462792, 0.01919973786751422162, 0.01988544279135401674, 0.02057114771519381533, 0.02194255756287339515 ),
 .UNSPECIFIED. ) ;
#17218=CARTESIAN_POINT ( 'NONE',  ( -59.75626822162180218, -5.804869634004078627, 5.128141679950119602 ) ) ;
#17220=TOROIDAL_SURFACE ( 'NONE', #148, 5.587650971692158741, 0.4500000000000000111 ) ;
#17223=EDGE_LOOP ( 'NONE', ( #20143, #28509, #5461, #3094 ) ) ;
#17224=CIRCLE ( 'NONE', #4966, 0.5000000000000000000 ) ;
#17226=DIRECTION ( 'NONE',  ( -0.000000000000000000, -0.000000000000000000, -1.000000000000000000 ) ) ;
#17227=CARTESIAN_POINT ( 'NONE',  ( -17.08382165986120071, 13.10789634492833855, 1.904575337205325125 ) ) ;
#17229=DIRECTION ( 'NONE',  ( -1.000000000000000000, 0.000000000000000000, 0.000000000000000000 ) ) ;
#17232=DIRECTION ( 'NONE',  ( -0.000000000000000000, -0.3746065934159164001, 0.9271838545667856479 ) ) ;
#17248=DIRECTION ( 'NONE',  ( 0.000000000000000000, 0.000000000000000000, -1.000000000000000000 ) ) ;
#17259=ORIENTED_EDGE ( 'NONE', *, *, #5503, .T. ) ;
#17264=CIRCLE ( 'NONE', #16173, 2.099999999999990319 ) ;
#17266=VECTOR ( 'NONE', #27166, 1000.000000000000000 ) ;
#17271=VECTOR ( 'NONE', #9792, 1000.000000000000227 ) ;
#17272=CONICAL_SURFACE ( 'NONE', #32219, 2.099999999999997868, 1.029744258676653423 ) ;
#17276=CARTESIAN_POINT ( 'NONE',  ( 107.7876430002164909, 19.84562591318736224, -3.565951703812070495 ) ) ;
#17294=DIRECTION ( 'NONE',  ( -0.1327696077594705815, 0.9911469271785068313, 0.000000000000000000 ) ) ;
#17296=ORIENTED_EDGE ( 'NONE', *, *, #15320, .F. ) ;
#17307=( BOUNDED_SURFACE ( )  B_SPLINE_SURFACE ( 3, 2, ( 
 ( #9906, #1104, #7066 ),
 ( #17276, #4573, #14897 ),
 ( #25101, #8794, #14748 ),
 ( #16457, #30165, #7238 ) ),
 .UNSPECIFIED., .F., .F., .F. ) 
 B_SPLINE_SURFACE_WITH_KNOTS ( ( 4, 4 ),
 ( 3, 3 ),
 ( -1.734723475976807094E-18, 0.003477590727840301505 ),
 ( 0.000000000000000000, 1.000000000000000000 ),
 .UNSPECIFIED. ) 
 GEOMETRIC_REPRESENTATION_ITEM ( )  RATIONAL_B_SPLINE_SURFACE ( (
 ( 1.000000000000000000, 0.7044453589051415943, 1.000000000000000000),
 ( 1.000000000000000000, 0.7044500455794215910, 1.000000000000000000),
 ( 1.000000000000000000, 0.7044547099241695864, 1.000000000000000000),
 ( 1.000000000000000000, 0.7044593522111741724, 1.000000000000000000) ) ) 
 REPRESENTATION_ITEM ( '' )  SURFACE ( )  );
#17312=DIRECTION ( 'NONE',  ( 1.000000000000000000, 0.000000000000000000, -0.000000000000000000 ) ) ;
#17313=CYLINDRICAL_SURFACE ( 'NONE', #5423, 0.4499999999999990119 ) ;
#17323=CARTESIAN_POINT ( 'NONE',  ( 107.3934749906246111, 17.60820349277802421, -4.075198509582265594 ) ) ;
#17338=CARTESIAN_POINT ( 'NONE',  ( 9.302055952181044418, 0.2457637073014158069, -1.500000000000004219 ) ) ;
#17340=LINE ( 'NONE', #14465, #4306 ) ;
#17356=CARTESIAN_POINT ( 'NONE',  ( -56.46106707970686500, 0.01431647023326164565, -1.180353684121977276 ) ) ;
#17358=ORIENTED_EDGE ( 'NONE', *, *, #12537, .T. ) ;
#17364=CARTESIAN_POINT ( 'NONE',  ( -23.54713438637982748, 8.434582260019382716, 8.205946861809124471 ) ) ;
#17385=CARTESIAN_POINT ( 'NONE',  ( 108.0068349480237515, 18.21621961241920573, -4.398253369385427547 ) ) ;
#17390=ORIENTED_EDGE ( 'NONE', *, *, #29832, .F. ) ;
#17393=CARTESIAN_POINT ( 'NONE',  ( 24.72695737054825926, 18.91229966141139229, 1.500000000000000000 ) ) ;
#17395=CARTESIAN_POINT ( 'NONE',  ( -18.13299741701835188, 15.72250979567403206, 1.500000000000000222 ) ) ;
#17396=CARTESIAN_POINT ( 'NONE',  ( -30.49072021768049012, 9.200062826706727037, 1.500000000000000000 ) ) ;
#17401=ORIENTED_EDGE ( 'NONE', *, *, #15321, .T. ) ;
#17405=CARTESIAN_POINT ( 'NONE',  ( -61.24371088333262492, -10.96999999999998643, 1.949999999999999956 ) ) ;
#17410=EDGE_LOOP ( 'NONE', ( #20297, #29464, #14488, #12304 ) ) ;
#17424=VERTEX_POINT ( 'NONE', #22816 ) ;
#17431=CARTESIAN_POINT ( 'NONE',  ( 17.32050807568873552, 10.00000000000002309, 1.500000000000000000 ) ) ;
#17435=ORIENTED_EDGE ( 'NONE', *, *, #6396, .F. ) ;
#17438=DIRECTION ( 'NONE',  ( -1.000000000000000000, 0.000000000000000000, 0.000000000000000000 ) ) ;
#17459=CARTESIAN_POINT ( 'NONE',  ( -23.54713438637982748, 10.71031731502107576, 2.573304945315896042 ) ) ;
#17467=EDGE_CURVE ( 'NONE', #8185, #1782, #7596, .T. ) ;
#17475=ORIENTED_EDGE ( 'NONE', *, *, #18924, .T. ) ;
#17484=CARTESIAN_POINT ( 'NONE',  ( 9.282537329959810180, 0.2172754300396264326, -1.041239158277639021 ) ) ;
#17489=CARTESIAN_POINT ( 'NONE',  ( 17.41559371906258136, 18.02474698348859405, -1.491740999229418829 ) ) ;
#17500=CARTESIAN_POINT ( 'NONE',  ( -56.32772727923107681, 0.4611123337040696213, -1.500000000000000000 ) ) ;
#17509=CARTESIAN_POINT ( 'NONE',  ( 107.5052154967213482, 18.24033990947258133, 5.057122841292876814 ) ) ;
#17514=EDGE_LOOP ( 'NONE', ( #8288, #31277, #10534, #22860 ) ) ;
#17522=ORIENTED_EDGE ( 'NONE', *, *, #20438, .T. ) ;
#17531=CARTESIAN_POINT ( 'NONE',  ( -50.81000000000000227, -10.96999999999998643, 9.000000000000000000 ) ) ;
#17532=ADVANCED_FACE ( 'NONE', ( #29796 ), #24424, .F. ) ;
#17533=CARTESIAN_POINT ( 'NONE',  ( -53.92460539084177640, 5.494498998130930900, 1.240130434009519833 ) ) ;
#17538=CARTESIAN_POINT ( 'NONE',  ( 18.03711215731073736, 14.23863779149164621, 1.500000000000000222 ) ) ;
#17543=CARTESIAN_POINT ( 'NONE',  ( -27.92832289637516041, 5.061405101124985428, 1.500000000000000000 ) ) ;
#17578=DIRECTION ( 'NONE',  ( 0.5649695393302013313, 0.8251117619019986416, 2.783162557147745187E-15 ) ) ;
#17582=DIRECTION ( 'NONE',  ( 0.000000000000000000, 0.000000000000000000, -1.000000000000000000 ) ) ;
#17585=ADVANCED_FACE ( 'NONE', ( #24584 ), #20105, .F. ) ;
#17603=ORIENTED_EDGE ( 'NONE', *, *, #1389, .T. ) ;
#17607=CIRCLE ( 'NONE', #24536, 8.025310301077736241 ) ;
#17641=CARTESIAN_POINT ( 'NONE',  ( 24.81047430030741552, 18.92139209076561457, -1.500000000000001776 ) ) ;
#17658=AXIS2_PLACEMENT_3D ( 'NONE', #27446, #7363, #25263 ) ;
#17661=CARTESIAN_POINT ( 'NONE',  ( -56.28351068141993352, -3.534499082302744455E-14, -1.000000000037517767 ) ) ;
#17670=CARTESIAN_POINT ( 'NONE',  ( 108.0329321482101648, 18.36153912052067128, 4.597321217600237375 ) ) ;
#17689=ORIENTED_EDGE ( 'NONE', *, *, #19595, .F. ) ;
#17699=CARTESIAN_POINT ( 'NONE',  ( -53.94245116308378130, 5.494009027683203428, 1.203691125345451196 ) ) ;
#17709=( BOUNDED_CURVE ( )  B_SPLINE_CURVE ( 3, ( #18878, #1331, #5995, #21367 ),
 .UNSPECIFIED., .F., .F. ) 
 B_SPLINE_CURVE_WITH_KNOTS ( ( 4, 4 ),
 ( 0.000000000000000000, 3.141592653589793116 ),
 .UNSPECIFIED. ) 
 CURVE ( )  GEOMETRIC_REPRESENTATION_ITEM ( )  RATIONAL_B_SPLINE_CURVE ( ( 1.000000000000000000, 0.3333333333333333703, 0.3333333333333333703, 1.000000000000000000 ) ) 
 REPRESENTATION_ITEM ( '' )  );
#17714=CARTESIAN_POINT ( 'NONE',  ( -30.00126220292998624, 9.321674377478409212, 2.002134007589322806 ) ) ;
#17717=CARTESIAN_POINT ( 'NONE',  ( -23.54713438637982748, 10.71031731502107576, 2.573304945315896042 ) ) ;
#17721=VERTEX_POINT ( 'NONE', #31009 ) ;
#17732=VERTEX_POINT ( 'NONE', #19614 ) ;
#17733=CARTESIAN_POINT ( 'NONE',  ( -21.33422931780647502, 18.05240604713923958, 1.782833241104217592 ) ) ;
#17745=ORIENTED_EDGE ( 'NONE', *, *, #14642, .T. ) ;
#17766=DIRECTION ( 'NONE',  ( -0.4999999999999981681, -0.8660254037844395958, 0.000000000000000000 ) ) ;
#17773=LINE ( 'NONE', #32997, #9691 ) ;
#17778=CARTESIAN_POINT ( 'NONE',  ( -41.57389320450581494, -15.56693736020740637, 5.315798355015693311 ) ) ;
#17789=AXIS2_PLACEMENT_3D ( 'NONE', #12128, #2280, #22679 ) ;
#17809=DIRECTION ( 'NONE',  ( -0.000000000000000000, -0.3746065934159164001, 0.9271838545667856479 ) ) ;
#17814=EDGE_LOOP ( 'NONE', ( #12918, #1483, #26591, #3594, #21434, #12208 ) ) ;
#17818=DIRECTION ( 'NONE',  ( -0.000000000000000000, 0.000000000000000000, 1.000000000000000000 ) ) ;
#17819=DIRECTION ( 'NONE',  ( 0.000000000000000000, 0.000000000000000000, -1.000000000000000000 ) ) ;
#17832=VERTEX_POINT ( 'NONE', #24601 ) ;
#17834=VECTOR ( 'NONE', #34, 1000.000000000000000 ) ;
#17838=CARTESIAN_POINT ( 'NONE',  ( 16.75741909111353678, 12.07361620705510497, 1.049999999999999600 ) ) ;
#17843=VERTEX_POINT ( 'NONE', #31832 ) ;
#17853=CARTESIAN_POINT ( 'NONE',  ( -56.32142235783205564, 0.2514572592548188212, -1.435292253568081655 ) ) ;
#17855=ORIENTED_EDGE ( 'NONE', *, *, #8073, .F. ) ;
#17857=VERTEX_POINT ( 'NONE', #29300 ) ;
#17862=CARTESIAN_POINT ( 'NONE',  ( 107.9372080783385286, 17.82850972856275362, 4.742639206112238881 ) ) ;
#17865=ORIENTED_EDGE ( 'NONE', *, *, #9343, .T. ) ;
#17870=CARTESIAN_POINT ( 'NONE',  ( -53.56955650739543273, 4.402097243136370963, 5.500000000000000000 ) ) ;
#17891=VERTEX_POINT ( 'NONE', #20121 ) ;
#17897=CARTESIAN_POINT ( 'NONE',  ( -26.78358164153306120, 5.033963319885375043, 1.499999999999090949 ) ) ;
#17912=CARTESIAN_POINT ( 'NONE',  ( -19.05749829221029401, 5.903777093689171807, 2.093710349196163278 ) ) ;
#17920=DIRECTION ( 'NONE',  ( 0.8660254037844409281, -0.4999999999999960587, 0.000000000000000000 ) ) ;
#17922=CARTESIAN_POINT ( 'NONE',  ( 7.437041877750292684, 18.60036511249582958, 1.508259000770582059 ) ) ;
#17923=CARTESIAN_POINT ( 'NONE',  ( 25.05611271041078680, 19.07770844178882186, 1.500000000000000000 ) ) ;
#17924=( BOUNDED_SURFACE ( )  B_SPLINE_SURFACE ( 3, 2, ( 
 ( #398, #60, #25121 ),
 ( #10421, #13095, #33001 ),
 ( #20285, #20633, #5406 ),
 ( #20470, #10574, #30493 ),
 ( #25810, #7906, #7578 ),
 ( #8066, #20781, #18097 ),
 ( #2244, #18271, #17778 ),
 ( #15263, #15597, #28482 ) ),
 .UNSPECIFIED., .F., .F., .F. ) 
 B_SPLINE_SURFACE_WITH_KNOTS ( ( 4, 2, 2, 4 ),
 ( 3, 3 ),
 ( 0.000000000000000000, 0.001031706651898124964, 0.002063413303796249928, 0.004126826607592499856 ),
 ( 0.000000000000000000, 1.000000000000000000 ),
 .UNSPECIFIED. ) 
 GEOMETRIC_REPRESENTATION_ITEM ( )  RATIONAL_B_SPLINE_SURFACE ( (
 ( 1.000000000000000000, 0.7660444431189785686, 1.000000000000000000),
 ( 1.000000000000000000, 0.8085210103973671236, 1.000000000000000000),
 ( 1.000000000000000000, 0.8435318601841085284, 1.000000000000000000),
 ( 1.000000000000000000, 0.9022997401202091927, 1.000000000000000000),
 ( 1.000000000000000000, 0.9260936007027841255, 1.000000000000000000),
 ( 1.000000000000000000, 0.9823303353967430818, 1.000000000000000000),
 ( 1.000000000000000000, 0.9997933690884138747, 1.000000000000000000),
 ( 1.000000000000000000, 1.000000000000000000, 1.000000000000000000) ) ) 
 REPRESENTATION_ITEM ( '' )  SURFACE ( )  );
#17935=CARTESIAN_POINT ( 'NONE',  ( 56.97280603064898941, -277.2763395528616002, 0.000000000000000000 ) ) ;
#17937=ADVANCED_FACE ( 'NONE', ( #4730 ), #24948, .T. ) ;
#17938=ORIENTED_EDGE ( 'NONE', *, *, #3257, .F. ) ;
#17939=CARTESIAN_POINT ( 'NONE',  ( -38.14293509397970183, 21.49000000000000199, -1.500000000000000000 ) ) ;
#17959=VERTEX_POINT ( 'NONE', #2722 ) ;
#17960=CARTESIAN_POINT ( 'NONE',  ( 2.671540748214986660, 0.5000000000000006661, -1.500000000000000000 ) ) ;
#17962=VERTEX_POINT ( 'NONE', #32494 ) ;
#17978=EDGE_CURVE ( 'NONE', #10298, #2361, #8175, .T. ) ;
#17982=CARTESIAN_POINT ( 'NONE',  ( 8.870145747188287189, 0.000000000000000000, -1.000000000000000000 ) ) ;
#17998=DIRECTION ( 'NONE',  ( -0.1356223135424326209, 0.9907606108790346644, 0.000000000000000000 ) ) ;
#18000=ORIENTED_EDGE ( 'NONE', *, *, #14146, .T. ) ;
#18006=FACE_OUTER_BOUND ( 'NONE', #8907, .T. ) ;
#18012=CARTESIAN_POINT ( 'NONE',  ( -56.56779778351672405, 0.08779471422964917060, -1.028538298015328145 ) ) ;
#18014=VERTEX_POINT ( 'NONE', #20932 ) ;
#18020=CARTESIAN_POINT ( 'NONE',  ( 108.0434313396344379, 18.42000276116402091, 5.147805806629488501 ) ) ;
#18021=CARTESIAN_POINT ( 'NONE',  ( -38.14293509397969473, 10.97000000000000419, 1.050000000000000044 ) ) ;
#18025=ORIENTED_EDGE ( 'NONE', *, *, #3484, .F. ) ;
#18038=CARTESIAN_POINT ( 'NONE',  ( 108.1156589233279135, 18.82219444680288234, -4.397958565568440115 ) ) ;
#18041=CARTESIAN_POINT ( 'NONE',  ( 107.8490366731511898, 17.33753655370295377, -2.517018891476558995 ) ) ;
#18045=VERTEX_POINT ( 'NONE', #3215 ) ;
#18052=DIRECTION ( 'NONE',  ( -0.8660254037844399289, 0.4999999999999978351, 0.000000000000000000 ) ) ;
#18056=EDGE_LOOP ( 'NONE', ( #19465, #2427, #26123, #19982 ) ) ;
#18057=CARTESIAN_POINT ( 'NONE',  ( -23.54713438638086842, 3.998227953278294944, 2.146185852361370383 ) ) ;
#18060=CARTESIAN_POINT ( 'NONE',  ( 108.0793717420579014, 18.62013310325329840, -5.132089558057739254 ) ) ;
#18062=CARTESIAN_POINT ( 'NONE',  ( -18.45273447307403814, 6.578304958228390120, 2.075379730733474926 ) ) ;
#18073=CARTESIAN_POINT ( 'NONE',  ( 24.28956136227655094, 18.19040579222011900, 1.500000000000650147 ) ) ;
#18081=EDGE_CURVE ( 'NONE', #23780, #17891, #21110, .T. ) ;
#18082=CARTESIAN_POINT ( 'NONE',  ( -56.27770248097862549, 0.4996615022747108448, 0.000000000000000000 ) ) ;
#18097=CARTESIAN_POINT ( 'NONE',  ( -41.33570690803944814, -14.97572508516781120, 5.493143919433947531 ) ) ;
#18098=ORIENTED_EDGE ( 'NONE', *, *, #21003, .F. ) ;
#18107=EDGE_CURVE ( 'NONE', #17857, #7402, #10409, .T. ) ;
#18124=ADVANCED_FACE ( 'NONE', ( #7893 ), #5388, .T. ) ;
#18130=ADVANCED_FACE ( 'NONE', ( #32118 ), #17037, .T. ) ;
#18131=LINE ( 'NONE', #13269, #27432 ) ;
#18137=ADVANCED_FACE ( 'NONE', ( #6700 ), #1025, .F. ) ;
#18149=ADVANCED_FACE ( 'NONE', ( #21744 ), #15641, .T. ) ;
#18156=CARTESIAN_POINT ( 'NONE',  ( 15.82680059085170221, 20.06867288585792863, -4.131740999229418954 ) ) ;
#18159=DIRECTION ( 'NONE',  ( 1.000000000000000000, 0.000000000000000000, -0.000000000000000000 ) ) ;
#18168=TOROIDAL_SURFACE ( 'NONE', #11246, 10.64228691119592796, 0.4500000000000000111 ) ;
#18181=CARTESIAN_POINT ( 'NONE',  ( 9.302055952177829212, 0.2457637072967208403, 1.050000000000000044 ) ) ;
#18182=VECTOR ( 'NONE', #8221, 1000.000000000000000 ) ;
#18193=CARTESIAN_POINT ( 'NONE',  ( 9.287819511157117347, 0.2249814976390548393, -1.045547970484144829 ) ) ;
#18199=EDGE_LOOP ( 'NONE', ( #25467, #8362, #13528, #9564 ) ) ;
#18202=TOROIDAL_SURFACE ( 'NONE', #3793, 10.64228691119592796, 0.4500000000000000111 ) ;
#18223=CARTESIAN_POINT ( 'NONE',  ( -19.56543409745250273, 5.443045001481024769, 2.106299155096469367 ) ) ;
#18234=CARTESIAN_POINT ( 'NONE',  ( 23.79966985373406985, 18.45386651007853729, -1.499999999999999778 ) ) ;
#18236=CIRCLE ( 'NONE', #7014, 299.4192503346018270 ) ;
#18240=DIRECTION ( 'NONE',  ( 0.000000000000000000, 0.000000000000000000, 1.000000000000000000 ) ) ;
#18241=AXIS2_PLACEMENT_3D ( 'NONE', #4062, #8887, #24425 ) ;
#18246=CIRCLE ( 'NONE', #3837, 12.49867430706168570 ) ;
#18254=CARTESIAN_POINT ( 'NONE',  ( -56.32100375116784363, 0.5246615022747117552, -1.050000000000000044 ) ) ;
#18255=AXIS2_PLACEMENT_3D ( 'NONE', #26753, #14712, #17229 ) ;
#18268=ORIENTED_EDGE ( 'NONE', *, *, #24125, .F. ) ;
#18271=CARTESIAN_POINT ( 'NONE',  ( -41.55992208616379457, -15.55928713972474675, 5.268872846871810900 ) ) ;
#18280=DIRECTION ( 'NONE',  ( -0.7821988420038089584, 0.6230288689682847991, 0.000000000000000000 ) ) ;
#18283=ORIENTED_EDGE ( 'NONE', *, *, #27453, .F. ) ;
#18294=LINE ( 'NONE', #28503, #1151 ) ;
#18309=( BOUNDED_SURFACE ( )  B_SPLINE_SURFACE ( 1, 3, ( 
 ( #31137, #17922, #3055, #13067 ),
 ( #23269, #10545, #5211, #25440 ) ),
 .UNSPECIFIED., .F., .F., .F. ) 
 B_SPLINE_SURFACE_WITH_KNOTS ( ( 2, 2 ),
 ( 4, 4 ),
 ( 0.000000000000000000, 1.000000000000000000 ),
 ( 0.000000000000000000, 1.000000000000000000 ),
 .UNSPECIFIED. ) 
 GEOMETRIC_REPRESENTATION_ITEM ( )  RATIONAL_B_SPLINE_SURFACE ( (
 ( 1.000000000000000000, 0.9321687722090974404, 0.9321687722090974404, 1.000000000000000000),
 ( 1.000000000000000000, 0.9321687722090974404, 0.9321687722090974404, 1.000000000000000000) ) ) 
 REPRESENTATION_ITEM ( '' )  SURFACE ( )  );
#18327=DIRECTION ( 'NONE',  ( -0.000000000000000000, -0.000000000000000000, -1.000000000000000000 ) ) ;
#18336=AXIS2_PLACEMENT_3D ( 'NONE', #8084, #30702, #28155 ) ;
#18340=CARTESIAN_POINT ( 'NONE',  ( 8.930755659325139817, 0.4999999999999997780, 1.050000000000000044 ) ) ;
#18343=DIRECTION ( 'NONE',  ( 0.7895257206258718963, 0.6137174728408810731, 0.000000000000000000 ) ) ;
#18345=EDGE_CURVE ( 'NONE', #18014, #20999, #9203, .T. ) ;
#18353=CIRCLE ( 'NONE', #8205, 0.5000000000000000000 ) ;
#18364=EDGE_CURVE ( 'NONE', #9701, #32393, #190, .T. ) ;
#18382=ORIENTED_EDGE ( 'NONE', *, *, #14627, .F. ) ;
#18384=CARTESIAN_POINT ( 'NONE',  ( 108.2286009897290597, 19.45110043733557958, 3.071383935681160970 ) ) ;
#18387=VERTEX_POINT ( 'NONE', #31916 ) ;
#18394=CARTESIAN_POINT ( 'NONE',  ( -23.54713438637982748, 2.712271330416904380, 6.352360439504502132 ) ) ;
#18401=FACE_OUTER_BOUND ( 'NONE', #23491, .T. ) ;
#18409=AXIS2_PLACEMENT_3D ( 'NONE', #7110, #7601, #17312 ) ;
#18415=VERTEX_POINT ( 'NONE', #14002 ) ;
#18424=CARTESIAN_POINT ( 'NONE',  ( 17.92222975117456230, 13.44085466222674619, 1.500000000000000000 ) ) ;
#18431=CARTESIAN_POINT ( 'NONE',  ( -27.53304292598423331, 17.01599196463006436, 1.807868844288452070 ) ) ;
#18435=CARTESIAN_POINT ( 'NONE',  ( 78.40736801748178664, 24.56822898102832653, 4.629213727441585213 ) ) ;
#18443=CARTESIAN_POINT ( 'NONE',  ( 108.0849451456563628, 18.65116801364982990, -4.602065642979003890 ) ) ;
#18445=ORIENTED_EDGE ( 'NONE', *, *, #13651, .T. ) ;
#18446=CARTESIAN_POINT ( 'NONE',  ( 15.05218482013242820, 8.633077639384330482, 1.050000000000000044 ) ) ;
#18461=DIRECTION ( 'NONE',  ( -0.000000000000000000, -0.000000000000000000, -1.000000000000000000 ) ) ;
#18465=CYLINDRICAL_SURFACE ( 'NONE', #16775, 8.025310301077734465 ) ;
#18469=VERTEX_POINT ( 'NONE', #6315 ) ;
#18471=ADVANCED_FACE ( 'NONE', ( #24215 ), #24370, .F. ) ;
#18474=VERTEX_POINT ( 'NONE', #6664 ) ;
#18482=DIRECTION ( 'NONE',  ( 0.4999999999999978351, 0.8660254037844399289, 0.000000000000000000 ) ) ;
#18501=CARTESIAN_POINT ( 'NONE',  ( 2.501106528969298193, 0.1614173311939657851, -1.446082916213565106 ) ) ;
#18510=ORIENTED_EDGE ( 'NONE', *, *, #27453, .T. ) ;
#18527=CARTESIAN_POINT ( 'NONE',  ( 17.41559371906258136, 18.02474698348857274, -1.500000000000000000 ) ) ;
#18543=CARTESIAN_POINT ( 'NONE',  ( 8.911384905465473238, 0.4717275430040264173, 1.041239158277188048 ) ) ;
#18568=CARTESIAN_POINT ( 'NONE',  ( 15.21374380700450146, 10.74503379549556037, 1.500000000000000000 ) ) ;
#18574=EDGE_LOOP ( 'NONE', ( #3971, #9931, #8099, #23298 ) ) ;
#18593=LINE ( 'NONE', #28963, #31541 ) ;
#18594=EDGE_LOOP ( 'NONE', ( #26562, #19209, #28053, #3898 ) ) ;
#18598=VERTEX_POINT ( 'NONE', #9698 ) ;
#18602=CARTESIAN_POINT ( 'NONE',  ( 107.9842833620133149, 18.09064348308214321, 4.146048564489902333 ) ) ;
#18616=CARTESIAN_POINT ( 'NONE',  ( -23.54713438637982748, 6.328288363227374980, 7.813326153826580800 ) ) ;
#18617=CARTESIAN_POINT ( 'NONE',  ( 107.8323272165537929, 17.24449170613202753, 2.334489955268165939 ) ) ;
#18625=ORIENTED_EDGE ( 'NONE', *, *, #29954, .F. ) ;
#18633=DIRECTION ( 'NONE',  ( 1.000000000000000000, 0.000000000000000000, 0.000000000000000000 ) ) ;
#18643=DIRECTION ( 'NONE',  ( -0.000000000000000000, 0.000000000000000000, 1.000000000000000000 ) ) ;
#18645=CARTESIAN_POINT ( 'NONE',  ( -56.28351068137280322, 0.4500000000000000111, 1.500000000000000000 ) ) ;
#18649=CYLINDRICAL_SURFACE ( 'NONE', #23021, 2.099999999999994316 ) ;
#18658=B_SPLINE_CURVE_WITH_KNOTS ( 'NONE', 3,
 ( #17218, #6841, #9180, #11690, #21888, #14703 ),
 .UNSPECIFIED., .F., .F.,
 ( 4, 2, 4 ),
 ( -2.095334690189621038E-05, 0.001971868223395999934, 0.003964689793693895736 ),
 .UNSPECIFIED. ) ;
#18660=CARTESIAN_POINT ( 'NONE',  ( 8.007433738499960540, 15.00000000000002132, -5.396302277755718357 ) ) ;
#18665=AXIS2_PLACEMENT_3D ( 'NONE', #10969, #21654, #26653 ) ;
#18673=CARTESIAN_POINT ( 'NONE',  ( 10.47272779071480819, 17.64623289522323191, 5.412820279296879811 ) ) ;
#18675=DIRECTION ( 'NONE',  ( 1.000000000000000000, 0.000000000000000000, 0.000000000000000000 ) ) ;
#18690=DIRECTION ( 'NONE',  ( -0.1385137909583552540, 0.9903605049245174374, 0.000000000000000000 ) ) ;
#18694=DIRECTION ( 'NONE',  ( -1.000000000000000000, 0.000000000000000000, 0.000000000000000000 ) ) ;
#18704=AXIS2_PLACEMENT_3D ( 'NONE', #13247, #23447, #5598 ) ;
#18714=ORIENTED_EDGE ( 'NONE', *, *, #20269, .T. ) ;
#18722=CARTESIAN_POINT ( 'NONE',  ( 9.302055952181040865, 0.2457637073014105056, 1.050000000000000044 ) ) ;
#18730=CIRCLE ( 'NONE', #19902, 5.100000000000000533 ) ;
#18748=DIRECTION ( 'NONE',  ( -0.8660254037844409281, 0.4999999999999960587, 0.000000000000000000 ) ) ;
#18752=ORIENTED_EDGE ( 'NONE', *, *, #13686, .T. ) ;
#18761=EDGE_LOOP ( 'NONE', ( #26394, #351, #11074, #24623 ) ) ;
#18762=ORIENTED_EDGE ( 'NONE', *, *, #3822, .F. ) ;
#18768=AXIS2_PLACEMENT_3D ( 'NONE', #5245, #12436, #15419 ) ;
#18771=CARTESIAN_POINT ( 'NONE',  ( 9.924500721667349978, 1.154815372884564928, -1.500000000000000000 ) ) ;
#18776=CARTESIAN_POINT ( 'NONE',  ( -1.152183934781129714E-14, 21.49000000000002331, -1.500000000000000000 ) ) ;
#18788=DIRECTION ( 'NONE',  ( -0.4999999999999978906, -0.8660254037844399289, 0.000000000000000000 ) ) ;
#18791=ORIENTED_EDGE ( 'NONE', *, *, #20734, .T. ) ;
#18792=VECTOR ( 'NONE', #25315, 1000.000000000000000 ) ;
#18800=ADVANCED_FACE ( 'NONE', ( #4159 ), #14325, .T. ) ;
#18808=CARTESIAN_POINT ( 'NONE',  ( 7.577572045913244736, 15.00000000000000178, 4.629213727441584325 ) ) ;
#18809=VERTEX_POINT ( 'NONE', #3833 ) ;
#18823=VECTOR ( 'NONE', #21076, 1000.000000000000000 ) ;
#18829=DIRECTION ( 'NONE',  ( -1.000000000000000000, 0.000000000000000000, 0.000000000000000000 ) ) ;
#18857=CARTESIAN_POINT ( 'NONE',  ( 108.1156589233279419, 18.82219444680297116, 4.414476567109417715 ) ) ;
#18866=CARTESIAN_POINT ( 'NONE',  ( -47.64323377349501243, 16.45499999999998408, -1.050000000000000044 ) ) ;
#18878=CARTESIAN_POINT ( 'NONE',  ( -23.54713438637982748, 18.90773822806172433, 1.500000000000000000 ) ) ;
#18881=B_SPLINE_CURVE_WITH_KNOTS ( 'NONE', 3,
 ( #523, #6693, #26929, #4032, #32448, #6344, #9010, #24555, #27425, #4532, #1677, #4179 ),
 .UNSPECIFIED., .F., .F.,
 ( 4, 2, 2, 2, 2, 4 ),
 ( 0.000000000000000000, 0.0007208007047092903361, 0.001081201057063939461, 0.001261401233241265379, 0.001351501321329926387, 0.001441601409418587394 ),
 .UNSPECIFIED. ) ;
#18888=CARTESIAN_POINT ( 'NONE',  ( -57.64077562173743985, -3.382820725347776225, 5.845255965757654160 ) ) ;
#18900=DIRECTION ( 'NONE',  ( 0.9563911903463302444, 0.000000000000000000, 0.2920888409849467515 ) ) ;
#18910=CARTESIAN_POINT ( 'NONE',  ( 18.74139243898558149, 14.92200307055332509, -1.499999999999999556 ) ) ;
#18913=CIRCLE ( 'NONE', #29054, 10.64228691119593151 ) ;
#18920=EDGE_CURVE ( 'NONE', #17843, #536, #22544, .T. ) ;
#18921=CARTESIAN_POINT ( 'NONE',  ( -59.37247738224319704, -6.026451378431820771, 5.500000000000000000 ) ) ;
#18924=EDGE_CURVE ( 'NONE', #2818, #14512, #12020, .T. ) ;
#18933=AXIS2_PLACEMENT_3D ( 'NONE', #32908, #14975, #4981 ) ;
#18947=CARTESIAN_POINT ( 'NONE',  ( 8.911384905465473238, 0.2172754300402719996, 1.412391582771868492 ) ) ;
#18975=EDGE_CURVE ( 'NONE', #685, #10104, #14764, .T. ) ;
#18979=VERTEX_POINT ( 'NONE', #22865 ) ;
#18982=ADVANCED_FACE ( 'NONE', ( #28062 ), #30089, .T. ) ;
#18987=ORIENTED_EDGE ( 'NONE', *, *, #19034, .T. ) ;
#18990=CARTESIAN_POINT ( 'NONE',  ( -56.72341663440466419, 0.2675318231349337328, 1.614498169334199984 ) ) ;
#18996=CARTESIAN_POINT ( 'NONE',  ( 14.23800746264082839, 22.11259878822726321, 1.508259000770582059 ) ) ;
#19003=DIRECTION ( 'NONE',  ( 0.000000000000000000, 0.000000000000000000, 1.000000000000000000 ) ) ;
#19013=EDGE_CURVE ( 'NONE', #28345, #15521, #27927, .T. ) ;
#19020=CARTESIAN_POINT ( 'NONE',  ( 26.08945412691624099, 19.05746434167065928, -1.050000000000000044 ) ) ;
#19024=EDGE_LOOP ( 'NONE', ( #15018, #28637, #14404, #11553 ) ) ;
#19026=CARTESIAN_POINT ( 'NONE',  ( -60.07995281065674931, -10.96999999999998465, 8.549999999999998934 ) ) ;
#19031=CARTESIAN_POINT ( 'NONE',  ( -40.71733131760397129, -12.43974741078717372, 5.871858320049880398 ) ) ;
#19034=EDGE_CURVE ( 'NONE', #11008, #15051, #19507, .T. ) ;
#19054=VERTEX_POINT ( 'NONE', #4772 ) ;
#19055=CARTESIAN_POINT ( 'NONE',  ( 8.454317476977939450, 15.00000000000000178, -4.131740999229418954 ) ) ;
#19101=CARTESIAN_POINT ( 'NONE',  ( 15.00732532868866542, 9.584243418233409528, -1.499999999999998446 ) ) ;
#19105=CARTESIAN_POINT ( 'NONE',  ( -50.81000000000000227, -10.96999999999998643, 5.871858320049875957 ) ) ;
#19107=CARTESIAN_POINT ( 'NONE',  ( 2.382865613620175349, 0.000000000000000000, 1.508259000770581615 ) ) ;
#19119=DIRECTION ( 'NONE',  ( -0.000000000000000000, -0.000000000000000000, -1.000000000000000000 ) ) ;
#19121=ADVANCED_FACE ( 'NONE', ( #25159 ), #1957, .T. ) ;
#19122=ORIENTED_EDGE ( 'NONE', *, *, #23713, .F. ) ;
#19126=EDGE_LOOP ( 'NONE', ( #21644, #21031, #32487, #14614 ) ) ;
#19154=CARTESIAN_POINT ( 'NONE',  ( 107.3483866128421056, 17.35711432068121596, -3.537658942756404912 ) ) ;
#19166=EDGE_CURVE ( 'NONE', #28913, #4370, #18131, .T. ) ;
#19170=CARTESIAN_POINT ( 'NONE',  ( 16.10106094948406863, 19.71584668020014419, 5.412820279296879811 ) ) ;
#19180=DIRECTION ( 'NONE',  ( -0.8896831085035101783, 0.4565785435645562940, 0.000000000000000000 ) ) ;
#19187=AXIS2_PLACEMENT_3D ( 'NONE', #14609, #6407, #24810 ) ;
#19199=CARTESIAN_POINT ( 'NONE',  ( -57.64172636127213423, -3.383636359799072846, 5.845147464816284000 ) ) ;
#19201=VERTEX_POINT ( 'NONE', #7615 ) ;
#19203=EDGE_CURVE ( 'NONE', #17832, #8403, #14604, .T. ) ;
#19206=AXIS2_PLACEMENT_3D ( 'NONE', #30362, #32714, #4954 ) ;
#19209=ORIENTED_EDGE ( 'NONE', *, *, #20906, .T. ) ;
#19223=CARTESIAN_POINT ( 'NONE',  ( -38.14293509397969473, 10.97000000000000419, -1.050000000000000044 ) ) ;
#19228=ADVANCED_FACE ( 'NONE', ( #7941 ), #584, .T. ) ;
#19235=CARTESIAN_POINT ( 'NONE',  ( -30.67627260417763679, 12.22102706438213460, 1.500000000000000000 ) ) ;
#19256=AXIS2_PLACEMENT_3D ( 'NONE', #14037, #21891, #14347 ) ;
#19262=CARTESIAN_POINT ( 'NONE',  ( 9.127968561342507670, 0.03517121848167529402, -1.257822814154247126 ) ) ;
#19271=DIRECTION ( 'NONE',  ( 0.07591486983599084193, 0.4227239498239174220, 0.9030733053208088723 ) ) ;
#19274=CARTESIAN_POINT ( 'NONE',  ( -2.794738735352967574, 0.000000000000000000, 1.292893218813452538 ) ) ;
#19298=ORIENTED_EDGE ( 'NONE', *, *, #12396, .T. ) ;
#19303=DIRECTION ( 'NONE',  ( -0.4999999999999981126, -0.8660254037844395958, 0.000000000000000000 ) ) ;
#19309=CARTESIAN_POINT ( 'NONE',  ( -56.76951762135347224, 0.4049278075578381930, 1.763939777626597705 ) ) ;
#19315=CARTESIAN_POINT ( 'NONE',  ( 110.8079127523828618, 15.75827621748124940, 1.508259000770581615 ) ) ;
#19317=APPLICATION_CONTEXT ( 'configuration controlled 3d designs of mechanical parts and assemblies' ) ;
#19327=ORIENTED_EDGE ( 'NONE', *, *, #10481, .T. ) ;
#19331=CARTESIAN_POINT ( 'NONE',  ( 107.4385791398478602, 17.85938043952733878, -4.612695725900422872 ) ) ;
#19333=CARTESIAN_POINT ( 'NONE',  ( -40.76530497340966264, -12.76917967239650942, 5.871858320049882174 ) ) ;
#19354=CARTESIAN_POINT ( 'NONE',  ( 9.174708406371134828, 0.09531162291655140284, 1.030456265918283210 ) ) ;
#19374=ADVANCED_FACE ( 'NONE', ( #3744 ), #19648, .T. ) ;
#19399=ORIENTED_EDGE ( 'NONE', *, *, #14146, .F. ) ;
#19409=ORIENTED_EDGE ( 'NONE', *, *, #32089, .T. ) ;
#19414=CARTESIAN_POINT ( 'NONE',  ( 20.33529679551776681, 16.25852880933178213, 1.500000000000000444 ) ) ;
#19417=EDGE_CURVE ( 'NONE', #32515, #14230, #4585, .T. ) ;
#19421=CARTESIAN_POINT ( 'NONE',  ( -19.95676506897028091, 17.93667199019918357, 1.500000000000000000 ) ) ;
#19422=CIRCLE ( 'NONE', #26374, 300.9381170038701612 ) ;
#19446=AXIS2_PLACEMENT_3D ( 'NONE', #22494, #17818, #30530 ) ;
#19451=CARTESIAN_POINT ( 'NONE',  ( 12.93640105133131257, 7.016868255687757738, -1.500000000000000000 ) ) ;
#19458=CARTESIAN_POINT ( 'NONE',  ( 2.502438769489224502, 0.2071067811865478503, 1.500000000000000444 ) ) ;
#19465=ORIENTED_EDGE ( 'NONE', *, *, #6735, .T. ) ;
#19467=B_SPLINE_CURVE_WITH_KNOTS ( 'NONE', 3,
 ( #765, #13749, #15939, #15629, #31016, #10767, #25845, #578, #5619, #31496, #10451, #23469 ),
 .UNSPECIFIED., .F., .F.,
 ( 4, 2, 2, 2, 2, 4 ),
 ( 1.205172527016783068E-17, 9.147187684556683674E-05, 0.0001829437536911216388, 0.0003658875073822308093, 0.0007317750147644532703, 0.001463550029528898518 ),
 .UNSPECIFIED. ) ;
#19478=ORIENTED_EDGE ( 'NONE', *, *, #32087, .T. ) ;
#19486=FACE_OUTER_BOUND ( 'NONE', #17410, .T. ) ;
#19491=CARTESIAN_POINT ( 'NONE',  ( -56.45356511950618028, 0.03062438154691659795, -1.016704686750477649 ) ) ;
#19497=DIRECTION ( 'NONE',  ( 0.000000000000000000, 0.000000000000000000, 1.000000000000000000 ) ) ;
#19498=CARTESIAN_POINT ( 'NONE',  ( 108.3696618535068126, 20.23658298680886247, -1.378742097822665436 ) ) ;
#19505=DIRECTION ( 'NONE',  ( 0.2880220749472531261, 0.1662896225033516084, -0.9430753128943477614 ) ) ;
#19507=LINE ( 'NONE', #16970, #17271 ) ;
#19517=CARTESIAN_POINT ( 'NONE',  ( 12.16477365892661489, 4.794553353644049665, -1.050000000000000044 ) ) ;
#19524=CARTESIAN_POINT ( 'NONE',  ( 107.7536796087345294, 16.80655079293032017, 1.395761063491601783 ) ) ;
#19528=ORIENTED_EDGE ( 'NONE', *, *, #15129, .T. ) ;
#19532=DIRECTION ( 'NONE',  ( 0.000000000000000000, -0.9271838545667856479, -0.3746065934159163446 ) ) ;
#19536=CARTESIAN_POINT ( 'NONE',  ( -30.16981175037142293, 11.66754487082764236, 1.941331850688031491 ) ) ;
#19538=CARTESIAN_POINT ( 'NONE',  ( -56.32100375116784363, 0.5246615022747116441, -1.500000000000000000 ) ) ;
#19546=CARTESIAN_POINT ( 'NONE',  ( 108.0068349480237373, 18.21621961241920573, -4.398253369385428435 ) ) ;
#19566=FACE_BOUND ( 'NONE', #25264, .T. ) ;
#19570=CARTESIAN_POINT ( 'NONE',  ( 16.66046955005661800, 12.69976583513764012, 1.500000000000000000 ) ) ;
#19574=CARTESIAN_POINT ( 'NONE',  ( -25.33158220408985883, 18.40448632064655499, 1.499999999999999778 ) ) ;
#19576=FACE_OUTER_BOUND ( 'NONE', #9925, .T. ) ;
#19595=EDGE_CURVE ( 'NONE', #23529, #29856, #11555, .T. ) ;
#19614=CARTESIAN_POINT ( 'NONE',  ( 12.40148790557316794, 21.49000000000003041, 1.500000000000000000 ) ) ;
#19620=ADVANCED_FACE ( 'NONE', ( #5873 ), #31463, .T. ) ;
#19644=B_SPLINE_CURVE_WITH_KNOTS ( 'NONE', 3,
 ( #865, #18234, #28447, #6029, #31135, #18910, #23572, #5557, #3377, #11044, #21242, #31440, #26442, #3541, #23901, #14193, #4172, #21578 ),
 .UNSPECIFIED., .F., .F.,
 ( 4, 2, 2, 2, 2, 2, 2, 2, 4 ),
 ( 0.000000000000000000, 0.003093832034890393878, 0.006187664069780787757, 0.009281496104671181635, 0.01237532813956157551, 0.01546916017445196939, 0.01856299220934236327, 0.02165682424423275715, 0.02475065627912315103 ),
 .UNSPECIFIED. ) ;
#19648=( BOUNDED_SURFACE ( )  B_SPLINE_SURFACE ( 3, 3, ( 
 ( #8764, #6244, #4085, #3446 ),
 ( #11264, #13912, #21470, #26807 ),
 ( #26494, #24302, #3928, #11591 ),
 ( #769, #1254, #16428, #10952 ) ),
 .UNSPECIFIED., .F., .F., .F. ) 
 B_SPLINE_SURFACE_WITH_KNOTS ( ( 4, 4 ),
 ( 4, 4 ),
 ( 0.000000000000000000, 1.000000000000000000 ),
 ( 0.000000000000000000, 1.000000000000000000 ),
 .UNSPECIFIED. ) 
 GEOMETRIC_REPRESENTATION_ITEM ( )  RATIONAL_B_SPLINE_SURFACE ( (
 ( 1.000000000000000000, 0.9917560313531952332, 0.9917560313531952332, 1.000000000000000000),
 ( 0.6539698177806696489, 0.6485785111069292119, 0.6485785111069292119, 0.6539698177806696489),
 ( 0.6539698177806696489, 0.6485785111069292119, 0.6485785111069292119, 0.6539698177806696489),
 ( 1.000000000000000000, 0.9917560313531952332, 0.9917560313531952332, 1.000000000000000000) ) ) 
 REPRESENTATION_ITEM ( '' )  SURFACE ( )  );
#19649=CARTESIAN_POINT ( 'NONE',  ( 46.69789307159569347, 25.15383447853596621, -4.612695725900422872 ) ) ;
#19656=B_SPLINE_CURVE_WITH_KNOTS ( 'NONE', 3,
 ( #4909, #25310, #11065, #31318, #10730, #26294, #18443, #23923, #31162, #3404 ),
 .UNSPECIFIED., .F., .F.,
 ( 4, 2, 2, 2, 4 ),
 ( 0.000000000000000000, 0.0002027905827773804999, 0.0004055811655547609997, 0.0006083717483321414996, 0.0008111623311095219994 ),
 .UNSPECIFIED. ) ;
#19673=CARTESIAN_POINT ( 'NONE',  ( 17.41555300807529250, 12.90381744129215669, -1.050000000000000044 ) ) ;
#19675=PLANE ( 'NONE',  #24066 ) ;
#19680=LINE ( 'NONE', #30058, #10833 ) ;
#19687=DIRECTION ( 'NONE',  ( -0.000000000000000000, -0.000000000000000000, -1.000000000000000000 ) ) ;
#19691=CARTESIAN_POINT ( 'NONE',  ( -25.97738183003427537, 4.497411454590747759, 2.132333938606539636 ) ) ;
#19699=CARTESIAN_POINT ( 'NONE',  ( -47.64323377349501243, 16.45499999999998408, 1.500000000000000000 ) ) ;
#19700=ORIENTED_EDGE ( 'NONE', *, *, #23899, .F. ) ;
#19710=CARTESIAN_POINT ( 'NONE',  ( 107.1772993348646281, 16.40207914262226296, -1.491740999229418829 ) ) ;
#19721=DIRECTION ( 'NONE',  ( -0.1385137909583552540, 0.9903605049245174374, 0.000000000000000000 ) ) ;
#19727=CARTESIAN_POINT ( 'NONE',  ( 11.15780064305207908, 3.972637044352831381, 1.500000000000000222 ) ) ;
#19730=CARTESIAN_POINT ( 'NONE',  ( -29.44915099269499947, 14.89308641508704412, 1.500000000000740297 ) ) ;
#19743=ORIENTED_EDGE ( 'NONE', *, *, #19013, .F. ) ;
#19744=VECTOR ( 'NONE', #32864, 1000.000000000000227 ) ;
#19749=ORIENTED_EDGE ( 'NONE', *, *, #17978, .F. ) ;
#19755=CARTESIAN_POINT ( 'NONE',  ( 22.19886290009631580, 17.51851157713672436, -1.500000000000000000 ) ) ;
#19757=EDGE_CURVE ( 'NONE', #10864, #23529, #6383, .T. ) ;
#19767=CARTESIAN_POINT ( 'NONE',  ( 107.5966592983129289, 18.76599786124473468, -5.131640265752476893 ) ) ;
#19771=EDGE_LOOP ( 'NONE', ( #4122, #26271, #18762 ) ) ;
#19782=CARTESIAN_POINT ( 'NONE',  ( 108.1156589233279135, 18.82219444680288589, 4.414476567109600680 ) ) ;
#19794=AXIS2_PLACEMENT_3D ( 'NONE', #14807, #14964, #32240 ) ;
#19811=AXIS2_PLACEMENT_3D ( 'NONE', #31051, #28545, #15664 ) ;
#19846=ORIENTED_EDGE ( 'NONE', *, *, #21053, .T. ) ;
#19850=AXIS2_PLACEMENT_3D ( 'NONE', #8767, #19119, #29309 ) ;
#19866=CIRCLE ( 'NONE', #28403, 10.87687437218811581 ) ;
#19894=FACE_OUTER_BOUND ( 'NONE', #6290, .T. ) ;
#19902=AXIS2_PLACEMENT_3D ( 'NONE', #22524, #7453, #27864 ) ;
#19912=AXIS2_PLACEMENT_3D ( 'NONE', #19055, #31287, #29246 ) ;
#19913=CARTESIAN_POINT ( 'NONE',  ( 107.2415468212143992, 16.76214236186829254, 2.279906962690792849 ) ) ;
#19916=CARTESIAN_POINT ( 'NONE',  ( -16.99974336530646113, 13.10954151769649378, 1.499999999999779954 ) ) ;
#19917=CARTESIAN_POINT ( 'NONE',  ( -23.54713438637982748, 18.60133783399175655, 1.500000000000000000 ) ) ;
#19935=CARTESIAN_POINT ( 'NONE',  ( 108.0895495799427124, 18.67680732057917581, -4.580456116173253100 ) ) ;
#19947=CARTESIAN_POINT ( 'NONE',  ( 8.906813281368055613, 0.1505923090604610048, -1.366675429750782600 ) ) ;
#19966=CARTESIAN_POINT ( 'NONE',  ( 77.65715268217998357, 26.11770293189133341, 1.508259000770581837 ) ) ;
#19973=AXIS2_PLACEMENT_3D ( 'NONE', #32348, #29489, #9411 ) ;
#19974=ORIENTED_EDGE ( 'NONE', *, *, #19203, .T. ) ;
#19982=ORIENTED_EDGE ( 'NONE', *, *, #2988, .F. ) ;
#19998=CARTESIAN_POINT ( 'NONE',  ( -50.81000000000000227, -10.96999999999998643, 2.028141679950118625 ) ) ;
#20000=DIRECTION ( 'NONE',  ( -1.000000000000000000, -5.361488761196503499E-16, 0.000000000000000000 ) ) ;
#20009=ADVANCED_FACE ( 'NONE', ( #31213 ), #9378, .T. ) ;
#20017=VECTOR ( 'NONE', #19497, 1000.000000000000000 ) ;
#20036=ORIENTED_EDGE ( 'NONE', *, *, #11623, .F. ) ;
#20038=CARTESIAN_POINT ( 'NONE',  ( 107.7536796087345294, 16.80655079293032017, -1.379243061950440108 ) ) ;
#20039=CARTESIAN_POINT ( 'NONE',  ( 16.36487458112949511, 19.37645981759117575, -4.612695725900422872 ) ) ;
#20044=CARTESIAN_POINT ( 'NONE',  ( -56.63622713806018538, 0.1497937355729806186, -1.035521931139215868 ) ) ;
#20084=CARTESIAN_POINT ( 'NONE',  ( -29.41021809322157310, 5.485000000000014531, 1.500000000000000000 ) ) ;
#20085=ADVANCED_FACE ( 'NONE', ( #4430 ), #3937, .T. ) ;
#20086=CARTESIAN_POINT ( 'NONE',  ( -26.87870632630977852, 4.906976360849698793, 2.121007814587993590 ) ) ;
#20089=DIRECTION ( 'NONE',  ( 0.000000000000000000, 0.000000000000000000, 1.000000000000000000 ) ) ;
#20098=CARTESIAN_POINT ( 'NONE',  ( 108.0119426754549750, 18.24466145416912610, -4.459116668420948670 ) ) ;
#20104=ORIENTED_EDGE ( 'NONE', *, *, #1172, .F. ) ;
#20105=PLANE ( 'NONE',  #27349 ) ;
#20112=CARTESIAN_POINT ( 'NONE',  ( 9.038457413085614789, 1.187263343935664605E-16, 1.016831166589732938 ) ) ;
#20113=LINE ( 'NONE', #30306, #14393 ) ;
#20114=CARTESIAN_POINT ( 'NONE',  ( 9.282537329959909655, 0.2172754300399158400, -1.041239158277187160 ) ) ;
#20119=CARTESIAN_POINT ( 'NONE',  ( 107.5137997967071612, 18.28951216238115762, -5.076820443063085442 ) ) ;
#20121=CARTESIAN_POINT ( 'NONE',  ( 2.382865613620175349, 0.000000000000000000, 1.000000000000000222 ) ) ;
#20135=EDGE_CURVE ( 'NONE', #11370, #25797, #7434, .T. ) ;
#20142=CARTESIAN_POINT ( 'NONE',  ( -23.54713438637982748, 8.275374457817617824, 8.599999999999999645 ) ) ;
#20143=ORIENTED_EDGE ( 'NONE', *, *, #8715, .F. ) ;
#20152=CARTESIAN_POINT ( 'NONE',  ( -1.176310634206514104E-14, 21.94000000000002260, 1.500000000000000000 ) ) ;
#20155=DIRECTION ( 'NONE',  ( 0.000000000000000000, -0.9271838545667855369, -0.3746065934159163446 ) ) ;
#20167=ORIENTED_EDGE ( 'NONE', *, *, #2673, .T. ) ;
#20191=CARTESIAN_POINT ( 'NONE',  ( -56.51865391759180568, 0.05810651368888004181, -1.023525953523438226 ) ) ;
#20196=VERTEX_POINT ( 'NONE', #20636 ) ;
#20200=ADVANCED_FACE ( 'NONE', ( #4917 ), #14387, .T. ) ;
#20202=CARTESIAN_POINT ( 'NONE',  ( 108.2141344899977895, 20.71717987834380637, 1.495953707351421968 ) ) ;
#20223=CARTESIAN_POINT ( 'NONE',  ( -40.27879340802675046, -12.50360960397076404, 5.500000000000000000 ) ) ;
#20224=CARTESIAN_POINT ( 'NONE',  ( -23.54713438637982748, 18.90773822806172433, 1.500000000000000000 ) ) ;
#20230=CARTESIAN_POINT ( 'NONE',  ( 107.8323134827048619, 20.09434993960548965, -3.035090133884138286 ) ) ;
#20247=CARTESIAN_POINT ( 'NONE',  ( -20.50218941644604698, 17.67398915370758772, 1.791940890631988692 ) ) ;
#20249=ORIENTED_EDGE ( 'NONE', *, *, #11682, .T. ) ;
#20261=( BOUNDED_CURVE ( )  B_SPLINE_CURVE ( 3, ( #6239, #3741, #13906, #24121 ),
 .UNSPECIFIED., .F., .F. ) 
 B_SPLINE_CURVE_WITH_KNOTS ( ( 4, 4 ),
 ( 0.6009777071440908225, 1.570796326794896558 ),
 .UNSPECIFIED. ) 
 CURVE ( )  GEOMETRIC_REPRESENTATION_ITEM ( )  RATIONAL_B_SPLINE_CURVE ( ( 1.000000000000000000, 0.9231448173252605471, 0.9231448173252605471, 1.000000000000000000 ) ) 
 REPRESENTATION_ITEM ( '' )  );
#20269=EDGE_CURVE ( 'NONE', #2610, #25225, #17607, .T. ) ;
#20274=CARTESIAN_POINT ( 'NONE',  ( 46.69789307159569347, 25.15383447853596621, 4.629213727441585213 ) ) ;
#20285=CARTESIAN_POINT ( 'NONE',  ( -40.49578753310456136, -13.12325744026704832, 5.486698823786521295 ) ) ;
#20297=ORIENTED_EDGE ( 'NONE', *, *, #21315, .F. ) ;
#20304=CARTESIAN_POINT ( 'NONE',  ( -50.81000000000000227, -10.96999999999998643, 9.000000000000000000 ) ) ;
#20323=ORIENTED_EDGE ( 'NONE', *, *, #20985, .F. ) ;
#20332=CARTESIAN_POINT ( 'NONE',  ( -53.59739919106122841, 4.827917019894381490, 2.635056041638651703 ) ) ;
#20342=CIRCLE ( 'NONE', #19256, 0.4500000000000016764 ) ;
#20343=ADVANCED_FACE ( 'NONE', ( #28785 ), #29372, .T. ) ;
#20349=CARTESIAN_POINT ( 'NONE',  ( 11.04311965146451158, 15.00000000000000178, 1.508259000770581615 ) ) ;
#20353=DIRECTION ( 'NONE',  ( 0.000000000000000000, 0.000000000000000000, 1.000000000000000000 ) ) ;
#20356=ORIENTED_EDGE ( 'NONE', *, *, #14084, .T. ) ;
#20364=CARTESIAN_POINT ( 'NONE',  ( 108.3924980168111745, 20.36374375480692578, 1.424458110042542192 ) ) ;
#20375=AXIS2_PLACEMENT_3D ( 'NONE', #1069, #3746, #29005 ) ;
#20386=CARTESIAN_POINT ( 'NONE',  ( 107.6876975323875740, 19.28758966828627663, 4.774517761658953141 ) ) ;
#20389=CARTESIAN_POINT ( 'NONE',  ( 107.9391918483597550, 17.83955614279767588, -3.592051012467005755 ) ) ;
#20391=CARTESIAN_POINT ( 'NONE',  ( -53.96125734831202436, 5.502033201759978454, 1.127224778417299067 ) ) ;
#20400=CARTESIAN_POINT ( 'NONE',  ( -60.52311629951223892, -10.96999999999998820, 8.628141679950115162 ) ) ;
#20404=AXIS2_PLACEMENT_3D ( 'NONE', #31688, #3595, #21637 ) ;
#20405=CARTESIAN_POINT ( 'NONE',  ( -29.99064796452623582, 9.298459344133517490, 1.499999999996624700 ) ) ;
#20408=CARTESIAN_POINT ( 'NONE',  ( -23.54713438637982748, 8.429255322705477838, 8.219131494323725917 ) ) ;
#20420=CARTESIAN_POINT ( 'NONE',  ( 108.1273904054188080, 18.88751996810619715, -5.041740218227376502 ) ) ;
#20421=VECTOR ( 'NONE', #12152, 1000.000000000000114 ) ;
#20423=CARTESIAN_POINT ( 'NONE',  ( -23.08960572693444036, 4.011204475888708210, 2.145824749606468185 ) ) ;
#20431=AXIS2_PLACEMENT_3D ( 'NONE', #6367, #1216, #23928 ) ;
#20435=DIRECTION ( 'NONE',  ( 0.000000000000000000, 0.000000000000000000, -1.000000000000000000 ) ) ;
#20436=CARTESIAN_POINT ( 'NONE',  ( 25.73747082620503690, 18.89898602765365609, 1.050000000000000044 ) ) ;
#20438=EDGE_CURVE ( 'NONE', #7241, #18979, #12265, .T. ) ;
#20446=CARTESIAN_POINT ( 'NONE',  ( -25.77866645709989513, 18.05832575017197428, 1.782687067521398605 ) ) ;
#20462=EDGE_CURVE ( 'NONE', #20953, #7325, #2939, .T. ) ;
#20470=CARTESIAN_POINT ( 'NONE',  ( -40.73291413977247544, -13.73842845495894593, 5.444121653534940819 ) ) ;
#20476=EDGE_LOOP ( 'NONE', ( #6298, #7738, #16859, #9021, #9419, #28210 ) ) ;
#20478=CARTESIAN_POINT ( 'NONE',  ( 2.671540748214986660, 0.5000000000000006661, -1.500000000000000000 ) ) ;
#20496=AXIS2_PLACEMENT_3D ( 'NONE', #23342, #446, #10628 ) ;
#20505=ADVANCED_FACE ( 'NONE', ( #6066 ), #5592, .T. ) ;
#20522=CARTESIAN_POINT ( 'NONE',  ( -54.10469650629801919, 5.263418255572274163, 1.500000000000000000 ) ) ;
#20546=CARTESIAN_POINT ( 'NONE',  ( 108.0970801781586772, 18.71874066288092564, 5.127126610281505847 ) ) ;
#20556=ADVANCED_FACE ( 'NONE', ( #30221 ), #23060, .T. ) ;
#20576=DIRECTION ( 'NONE',  ( -0.2951703194034052125, 0.3797261271633437518, 0.8767454310646960458 ) ) ;
#20580=DIRECTION ( 'NONE',  ( 0.000000000000000000, 0.2923717047227409882, -0.9563047559630342143 ) ) ;
#20584=ORIENTED_EDGE ( 'NONE', *, *, #3636, .F. ) ;
#20593=CARTESIAN_POINT ( 'NONE',  ( -21.75451829708082840, 4.263352738049903223, 2.138819418443957066 ) ) ;
#20603=ORIENTED_EDGE ( 'NONE', *, *, #29017, .T. ) ;
#20604=DIRECTION ( 'NONE',  ( -1.000000000000000000, 0.000000000000000000, -0.000000000000000000 ) ) ;
#20605=FACE_OUTER_BOUND ( 'NONE', #11890, .T. ) ;
#20612=ORIENTED_EDGE ( 'NONE', *, *, #11623, .T. ) ;
#20619=CARTESIAN_POINT ( 'NONE',  ( 2.382865613620175349, 0.000000000000000000, 1.508259000770581615 ) ) ;
#20620=EDGE_LOOP ( 'NONE', ( #7846, #1215, #25427, #17390 ) ) ;
#20622=EDGE_CURVE ( 'NONE', #9701, #15924, #27220, .T. ) ;
#20628=EDGE_CURVE ( 'NONE', #25309, #18474, #21976, .T. ) ;
#20633=CARTESIAN_POINT ( 'NONE',  ( -40.76707995218932723, -13.06422702898852783, 5.564001359196309338 ) ) ;
#20636=CARTESIAN_POINT ( 'NONE',  ( -54.06000000000000227, -10.96999999999998643, 9.000000000000000000 ) ) ;
#20639=DIRECTION ( 'NONE',  ( -1.000000000000000000, 0.000000000000000000, 0.000000000000000000 ) ) ;
#20644=ORIENTED_EDGE ( 'NONE', *, *, #6221, .F. ) ;
#20652=CARTESIAN_POINT ( 'NONE',  ( 107.9227312540154458, 20.59779369625414347, 1.977410089419335826 ) ) ;
#20664=B_SPLINE_CURVE_WITH_KNOTS ( 'NONE', 3,
 ( #31037, #20829, #20683, #15467, #5289, #8299, #30886, #13451, #7636, #17838, #26177, #21008, #3283, #3129, #23492, #2983, #23339, #28685, #26023, #25675 ),
 .UNSPECIFIED., .F., .F.,
 ( 4, 2, 2, 2, 2, 2, 2, 2, 2, 4 ),
 ( -5.999999999908826955E-08, 0.003223665706961764427, 0.006447391413923528498, 0.009671117120885284330, 0.01128297997436616788, 0.01289484282784704797, 0.01611856853480881507, 0.01934229424177057524, 0.02256601994873234235, 0.02578974565569410252 ),
 .UNSPECIFIED. ) ;
#20665=CARTESIAN_POINT ( 'NONE',  ( -41.39035047991316674, -16.40843718609402302, 2.028141679950118625 ) ) ;
#20672=ORIENTED_EDGE ( 'NONE', *, *, #12537, .F. ) ;
#20682=ORIENTED_EDGE ( 'NONE', *, *, #4252, .T. ) ;
#20683=CARTESIAN_POINT ( 'NONE',  ( 24.14778831125731884, 18.13365127247671538, 1.049999999999999822 ) ) ;
#20684=LINE ( 'NONE', #13285, #22983 ) ;
#20698=ORIENTED_EDGE ( 'NONE', *, *, #4347, .F. ) ;
#20704=CARTESIAN_POINT ( 'NONE',  ( 107.6330232455594142, 18.97482909515709082, 5.056747795904239062 ) ) ;
#20708=CARTESIAN_POINT ( 'NONE',  ( -1.082681991931091492, 0.000000000000000000, 4.629213727441584325 ) ) ;
#20711=CARTESIAN_POINT ( 'NONE',  ( 107.9618353151786181, 20.81780380167319677, -1.491740999229417941 ) ) ;
#20714=FACE_OUTER_BOUND ( 'NONE', #22827, .T. ) ;
#20722=CARTESIAN_POINT ( 'NONE',  ( 108.3696618535068126, 20.23658298680886247, -1.378742097822665436 ) ) ;
#20729=( BOUNDED_SURFACE ( )  B_SPLINE_SURFACE ( 3, 2, ( 
 ( #1023, #9015, #23912 ),
 ( #713, #28626, #21589 ),
 ( #16240, #8711, #26453 ),
 ( #15899, #26108, #13374 ),
 ( #10903, #8384, #28769 ),
 ( #3552, #16045, #13711 ),
 ( #26277, #11206, #3393 ),
 ( #23764, #877, #6201 ),
 ( #27589, #9364, #4690 ),
 ( #14711, #30127, #29616 ),
 ( #17227, #19916, #26935 ),
 ( #11697, #4037, #9513 ),
 ( #7018, #17395, #16731 ),
 ( #7201, #25060, #27433 ),
 ( #4538, #9689, #19421 ),
 ( #12049, #24910, #14860 ),
 ( #12363, #22582, #2176 ),
 ( #6698, #16886, #21896 ) ),
 .UNSPECIFIED., .F., .F., .F. ) 
 B_SPLINE_SURFACE_WITH_KNOTS ( ( 4, 2, 2, 2, 2, 2, 2, 2, 4 ),
 ( 3, 3 ),
 ( 3.141592653589793116, 3.534291735288517255, 3.926990816987241395, 4.319689898685965090, 4.712388980384689674, 5.105088062083414258, 5.497787143782137953, 5.890486225480861648, 6.283185307179586232 ),
 ( 0.000000000000000000, 1.000000000000000000 ),
 .UNSPECIFIED. ) 
 GEOMETRIC_REPRESENTATION_ITEM ( )  RATIONAL_B_SPLINE_SURFACE ( (
 ( 1.000000000000000000, 0.5948227867513392608, 1.000000000000000000),
 ( 1.000000000000000000, 0.5947841457464595472, 1.000000000000000000),
 ( 1.000000000000000000, 0.5992555908982051260, 1.000000000000000000),
 ( 1.000000000000000000, 0.6156781713480670160, 1.000000000000000000),
 ( 1.000000000000000000, 0.6276164863437538877, 1.000000000000000000),
 ( 1.000000000000000000, 0.6558905360706541732, 1.000000000000000000),
 ( 1.000000000000000000, 0.6721825289739642439, 1.000000000000000000),
 ( 1.000000000000000000, 0.7057963334894752361, 1.000000000000000000),
 ( 1.000000000000000000, 0.7231030986475205369, 1.000000000000000000),
 ( 1.000000000000000000, 0.7560862040296049136, 1.000000000000000000),
 ( 1.000000000000000000, 0.7717639430041645099, 1.000000000000000000),
 ( 1.000000000000000000, 0.7996867613994225188, 1.000000000000000000),
 ( 1.000000000000000000, 0.8119378018739443759, 1.000000000000000000),
 ( 1.000000000000000000, 0.8319131657171122685, 1.000000000000000000),
 ( 1.000000000000000000, 0.8396427561410071405, 1.000000000000000000),
 ( 1.000000000000000000, 0.8500048284159551493, 1.000000000000000000),
 ( 1.000000000000000000, 0.8526458704374092479, 1.000000000000000000),
 ( 1.000000000000000000, 0.8526401643540935105, 1.000000000000000000) ) ) 
 REPRESENTATION_ITEM ( '' )  SURFACE ( )  );
#20734=EDGE_CURVE ( 'NONE', #4370, #21301, #2687, .T. ) ;
#20738=CARTESIAN_POINT ( 'NONE',  ( -47.55999999999999517, -10.96999999999998643, 9.000000000000000000 ) ) ;
#20749=ORIENTED_EDGE ( 'NONE', *, *, #7450, .T. ) ;
#20755=ORIENTED_EDGE ( 'NONE', *, *, #9153, .T. ) ;
#20757=CARTESIAN_POINT ( 'NONE',  ( 24.08142948293325247, 18.58944880476600048, 1.500000000000000000 ) ) ;
#20781=CARTESIAN_POINT ( 'NONE',  ( -41.30241497097880909, -14.93473732866679882, 5.402788590779837641 ) ) ;
#20788=CARTESIAN_POINT ( 'NONE',  ( 2.654002685506794634, 0.4696231843230830316, -1.499999999999999778 ) ) ;
#20789=CARTESIAN_POINT ( 'NONE',  ( 2.671540748214986660, 0.5000000000000006661, 1.500000000000000000 ) ) ;
#20795=CARTESIAN_POINT ( 'NONE',  ( 8.007433738499996068, 15.00000000000000000, -5.396302277755718357 ) ) ;
#20800=DIRECTION ( 'NONE',  ( 1.000000000000000000, 0.000000000000000000, 0.000000000000000000 ) ) ;
#20801=ADVANCED_FACE ( 'NONE', ( #9765 ), #30189, .T. ) ;
#20811=DIRECTION ( 'NONE',  ( 0.4999999999999977796, 0.8660254037844398178, 0.000000000000000000 ) ) ;
#20818=CARTESIAN_POINT ( 'NONE',  ( -38.14293509397970183, 21.94000000000000128, 1.050000000000000044 ) ) ;
#20826=CARTESIAN_POINT ( 'NONE',  ( 56.97280603064898941, -277.2763395528616002, -4.612695725900422872 ) ) ;
#20829=CARTESIAN_POINT ( 'NONE',  ( 25.10961529206432274, 18.61629793905443364, 1.050000000000000044 ) ) ;
#20831=CARTESIAN_POINT ( 'NONE',  ( 17.41559371906258136, 18.02474698348859405, 1.500000000000000000 ) ) ;
#20837=DIRECTION ( 'NONE',  ( 0.000000000000000000, 0.000000000000000000, -1.000000000000000000 ) ) ;
#20840=EDGE_CURVE ( 'NONE', #12952, #2157, #9630, .T. ) ;
#20851=CARTESIAN_POINT ( 'NONE',  ( 12.27700767694853390, 19.86581740147262209, -5.396302277755719246 ) ) ;
#20868=ORIENTED_EDGE ( 'NONE', *, *, #9373, .T. ) ;
#20871=EDGE_CURVE ( 'NONE', #23049, #18045, #28324, .T. ) ;
#20883=CIRCLE ( 'NONE', #14987, 5.587650971692158741 ) ;
#20893=LINE ( 'NONE', #23885, #18823 ) ;
#20901=CARTESIAN_POINT ( 'NONE',  ( -20.49373157874864759, 4.792442962972690346, 2.124178786190599855 ) ) ;
#20906=EDGE_CURVE ( 'NONE', #28296, #13484, #11237, .T. ) ;
#20917=FACE_OUTER_BOUND ( 'NONE', #16909, .T. ) ;
#20922=CARTESIAN_POINT ( 'NONE',  ( -2.506063600758156262, 0.4999999999999998890, -1.500000000000000000 ) ) ;
#20932=CARTESIAN_POINT ( 'NONE',  ( 9.282537329959909655, 0.2172754300399125094, 1.041239158277188048 ) ) ;
#20939=CIRCLE ( 'NONE', #1704, 300.9381170038701612 ) ;
#20948=CARTESIAN_POINT ( 'NONE',  ( 15.84732276226623604, 14.44600775457921493, 1.050000000000000044 ) ) ;
#20953=VERTEX_POINT ( 'NONE', #20789 ) ;
#20985=EDGE_CURVE ( 'NONE', #7402, #12740, #582, .T. ) ;
#20999=VERTEX_POINT ( 'NONE', #18947 ) ;
#21000=ORIENTED_EDGE ( 'NONE', *, *, #8888, .F. ) ;
#21003=EDGE_CURVE ( 'NONE', #18598, #17832, #26475, .T. ) ;
#21008=CARTESIAN_POINT ( 'NONE',  ( 15.48186204063833138, 10.33650625749590546, 1.049999999999999600 ) ) ;
#21010=EDGE_CURVE ( 'NONE', #4970, #21159, #24843, .T. ) ;
#21031=ORIENTED_EDGE ( 'NONE', *, *, #32458, .F. ) ;
#21044=EDGE_CURVE ( 'NONE', #24398, #3200, #420, .T. ) ;
#21053=EDGE_CURVE ( 'NONE', #5412, #11370, #32060, .T. ) ;
#21055=DIRECTION ( 'NONE',  ( -1.000000000000000000, 0.000000000000000000, 0.000000000000000000 ) ) ;
#21071=PLANE ( 'NONE',  #9232 ) ;
#21076=DIRECTION ( 'NONE',  ( 0.000000000000000000, 0.000000000000000000, -1.000000000000000000 ) ) ;
#21083=CIRCLE ( 'NONE', #6137, 2.524999999999999911 ) ;
#21097=CARTESIAN_POINT ( 'NONE',  ( 17.59176001116349752, 13.74650376811828423, 1.500000000000000222 ) ) ;
#21100=LINE ( 'NONE', #522, #25105 ) ;
#21101=CARTESIAN_POINT ( 'NONE',  ( -23.54713438637982748, 8.275374457817619600, 8.600000000000004974 ) ) ;
#21109=CARTESIAN_POINT ( 'NONE',  ( 78.98737618897432355, 23.37029618663415320, 5.412820279296879811 ) ) ;
#21110=LINE ( 'NONE', #12896, #32747 ) ;
#21114=EDGE_CURVE ( 'NONE', #16163, #8185, #13889, .T. ) ;
#21124=ORIENTED_EDGE ( 'NONE', *, *, #32526, .T. ) ;
#21144=ORIENTED_EDGE ( 'NONE', *, *, #6176, .T. ) ;
#21147=CARTESIAN_POINT ( 'NONE',  ( 107.2640681281281729, 16.88755960000358414, 2.548738122058122446 ) ) ;
#21159=VERTEX_POINT ( 'NONE', #6871 ) ;
#21163=ORIENTED_EDGE ( 'NONE', *, *, #26603, .T. ) ;
#21177=DIRECTION ( 'NONE',  ( -0.000000000000000000, -0.000000000000000000, -1.000000000000000000 ) ) ;
#21178=CARTESIAN_POINT ( 'NONE',  ( 11.04311965146451335, 15.00000000000000355, -1.500000000000000000 ) ) ;
#21188=ORIENTED_EDGE ( 'NONE', *, *, #18081, .T. ) ;
#21190=CARTESIAN_POINT ( 'NONE',  ( 10.90258948330155953, 17.51112508050605854, -4.612695725900421984 ) ) ;
#21193=ORIENTED_EDGE ( 'NONE', *, *, #28457, .T. ) ;
#21195=EDGE_LOOP ( 'NONE', ( #4576, #1017, #338, #11904 ) ) ;
#21201=CARTESIAN_POINT ( 'NONE',  ( 7.577572045913208321, 15.00000000000002132, 4.629213727441584325 ) ) ;
#21208=ORIENTED_EDGE ( 'NONE', *, *, #14493, .F. ) ;
#21210=ADVANCED_FACE ( 'NONE', ( #26 ), #5058, .T. ) ;
#21215=DIRECTION ( 'NONE',  ( 0.000000000000000000, 0.000000000000000000, -1.000000000000000000 ) ) ;
#21242=CARTESIAN_POINT ( 'NONE',  ( 14.29326447320846682, 9.302996554324566958, -1.500000000000000222 ) ) ;
#21245=CARTESIAN_POINT ( 'NONE',  ( 9.923352537767708981, 1.153138503616545796, 1.499999999999881650 ) ) ;
#21261=ORIENTED_EDGE ( 'NONE', *, *, #28255, .F. ) ;
#21272=CARTESIAN_POINT ( 'NONE',  ( 108.3696618535068126, 20.23658298680886247, -1.378742097822665436 ) ) ;
#21273=VERTEX_POINT ( 'NONE', #25275 ) ;
#21279=CARTESIAN_POINT ( 'NONE',  ( 15.60185111446442541, 10.48692277156955299, -1.499999999999998446 ) ) ;
#21282=CARTESIAN_POINT ( 'NONE',  ( 9.331062908042635939, 15.00000000000000178, -4.612695725900422872 ) ) ;
#21288=CARTESIAN_POINT ( 'NONE',  ( -41.77414131929176477, -16.18685544166627821, 1.500000000000000000 ) ) ;
#21301=VERTEX_POINT ( 'NONE', #15885 ) ;
#21312=ORIENTED_EDGE ( 'NONE', *, *, #25146, .F. ) ;
#21315=EDGE_CURVE ( 'NONE', #4711, #15980, #11193, .T. ) ;
#21321=EDGE_CURVE ( 'NONE', #25915, #17424, #5382, .T. ) ;
#21324=CARTESIAN_POINT ( 'NONE',  ( 17.41559371906256004, 18.02474698348863669, 1.508259000770581615 ) ) ;
#21338=CARTESIAN_POINT ( 'NONE',  ( -41.04966659693692321, -14.04895890769333811, 5.700525207345996215 ) ) ;
#21349=CARTESIAN_POINT ( 'NONE',  ( 8.901201215455847304, 15.00000000000002132, 5.412820279296879811 ) ) ;
#21357=CARTESIAN_POINT ( 'NONE',  ( 108.1382412073544685, 18.94794151480644118, -4.129322685383101543 ) ) ;
#21361=CARTESIAN_POINT ( 'NONE',  ( 108.3358872576213230, 20.04851271009933456, 1.796441256565045386 ) ) ;
#21367=CARTESIAN_POINT ( 'NONE',  ( -23.54713438637982748, 3.520075575296777171, 1.500000000000000000 ) ) ;
#21380=AXIS2_PLACEMENT_3D ( 'NONE', #21101, #6036, #13367 ) ;
#21381=AXIS2_PLACEMENT_3D ( 'NONE', #13699, #28611, #696 ) ;
#21382=ORIENTED_EDGE ( 'NONE', *, *, #24520, .T. ) ;
#21392=ORIENTED_EDGE ( 'NONE', *, *, #28457, .F. ) ;
#21393=VERTEX_POINT ( 'NONE', #13065 ) ;
#21402=CARTESIAN_POINT ( 'NONE',  ( 17.22494247561739300, 13.33946157486217032, 1.500000000000000000 ) ) ;
#21403=CIRCLE ( 'NONE', #15527, 5.100000000000000533 ) ;
#21404=EDGE_CURVE ( 'NONE', #24410, #2361, #19644, .T. ) ;
#21416=DIRECTION ( 'NONE',  ( -0.000000000000000000, 0.3746065934159164001, -0.9271838545667856479 ) ) ;
#21434=ORIENTED_EDGE ( 'NONE', *, *, #14056, .T. ) ;
#21442=CARTESIAN_POINT ( 'NONE',  ( 107.8490370924046857, 17.33753888827191147, 2.533541893723956662 ) ) ;
#21450=CARTESIAN_POINT ( 'NONE',  ( -50.81000000000000227, -10.96999999999998643, 5.700000000000000178 ) ) ;
#21459=ORIENTED_EDGE ( 'NONE', *, *, #11179, .T. ) ;
#21470=CARTESIAN_POINT ( 'NONE',  ( 78.98737618897432355, 23.37029618663415320, -5.396302277755718357 ) ) ;
#21490=DIRECTION ( 'NONE',  ( -0.8660254037844397068, 0.4999999999999981681, 0.000000000000000000 ) ) ;
#21497=CARTESIAN_POINT ( 'NONE',  ( 5.865515302491369098, 15.00000000000000000, 1.500000000000000000 ) ) ;
#21514=AXIS2_PLACEMENT_3D ( 'NONE', #17431, #14901, #4896 ) ;
#21537=CARTESIAN_POINT ( 'NONE',  ( 8.911384905465460804, 0.2172754300400931704, 1.412391582771745924 ) ) ;
#21544=CARTESIAN_POINT ( 'NONE',  ( 108.2511986533483110, 19.57693314497984360, 2.802790312710702558 ) ) ;
#21561=VECTOR ( 'NONE', #6058, 1000.000000000000000 ) ;
#21568=CARTESIAN_POINT ( 'NONE',  ( -2.794738735352966685, 0.000000000000000000, -1.491740999229417941 ) ) ;
#21573=MANIFOLD_SOLID_BREP ( 'Fillet6', #24296 ) ;
#21578=CARTESIAN_POINT ( 'NONE',  ( 8.930755659325139817, 0.4999999999999980571, -1.500000000000000000 ) ) ;
#21582=CARTESIAN_POINT ( 'NONE',  ( 19.82965097551559808, 15.28209255176019177, 1.499999999999766187 ) ) ;
#21584=CARTESIAN_POINT ( 'NONE',  ( -23.54713438637982748, 13.83847758521832993, 10.84763956049549805 ) ) ;
#21589=CARTESIAN_POINT ( 'NONE',  ( -22.61376412419543414, 3.520075575297991755, 1.500000000000000000 ) ) ;
#21593=CARTESIAN_POINT ( 'NONE',  ( 11.04311965146451158, 15.00000000000000178, 1.500000000000000000 ) ) ;
#21603=ORIENTED_EDGE ( 'NONE', *, *, #23394, .T. ) ;
#21609=EDGE_CURVE ( 'NONE', #23825, #21273, #11745, .T. ) ;
#21615=CARTESIAN_POINT ( 'NONE',  ( 11.67104222929842372, 3.952383228471274990, -1.050000000000000044 ) ) ;
#21633=ORIENTED_EDGE ( 'NONE', *, *, #27110, .T. ) ;
#21636=ORIENTED_EDGE ( 'NONE', *, *, #30110, .F. ) ;
#21637=DIRECTION ( 'NONE',  ( -0.9164966213036979115, 0.4000424266736042900, 0.000000000000000000 ) ) ;
#21644=ORIENTED_EDGE ( 'NONE', *, *, #12424, .T. ) ;
#21650=FACE_OUTER_BOUND ( 'NONE', #2455, .T. ) ;
#21654=DIRECTION ( 'NONE',  ( 1.000000000000000000, -0.000000000000000000, -0.000000000000000000 ) ) ;
#21660=CARTESIAN_POINT ( 'NONE',  ( 5.865515302491333571, 15.00000000000002132, -1.491740999229417941 ) ) ;
#21667=CARTESIAN_POINT ( 'NONE',  ( 108.0849250792287961, 18.65105627586314085, 4.618623753023407552 ) ) ;
#21675=EDGE_LOOP ( 'NONE', ( #20698, #11442, #19409 ) ) ;
#21684=CARTESIAN_POINT ( 'NONE',  ( 18.88504792851585279, 14.44361348414706647, -1.050000000000000266 ) ) ;
#21687=CARTESIAN_POINT ( 'NONE',  ( 15.55254023221933046, 20.42149909151570597, 5.412820279296878923 ) ) ;
#21690=DIRECTION ( 'NONE',  ( 0.000000000000000000, 0.000000000000000000, 1.000000000000000000 ) ) ;
#21691=CARTESIAN_POINT ( 'NONE',  ( -2.794738735352966685, 0.000000000000000000, -1.000000000000000000 ) ) ;
#21699=EDGE_CURVE ( 'NONE', #22155, #10298, #13703, .T. ) ;
#21700=CARTESIAN_POINT ( 'NONE',  ( -29.34654203815345141, 5.521763387534528889, 1.291504468647948212 ) ) ;
#21704=VERTEX_POINT ( 'NONE', #5333 ) ;
#21714=( BOUNDED_SURFACE ( )  B_SPLINE_SURFACE ( 3, 2, ( 
 ( #21845, #17164, #16991 ),
 ( #29565, #27374, #4489 ),
 ( #14663, #6650, #25078 ),
 ( #19935, #2536, #28249 ),
 ( #30142, #20420, #5199 ),
 ( #4861, #7218, #32965 ),
 ( #25581, #18060, #15225 ),
 ( #15044, #4707, #30800 ),
 ( #25265, #27604, #12379 ),
 ( #14876, #22600, #22757 ),
 ( #7868, #10034, #9883 ),
 ( #25760, #32812, #2382 ),
 ( #20098, #5359, #30447 ),
 ( #2693, #2192, #12554 ) ),
 .UNSPECIFIED., .F., .F., .F. ) 
 B_SPLINE_SURFACE_WITH_KNOTS ( ( 4, 2, 2, 2, 2, 2, 4 ),
 ( 3, 3 ),
 ( 8.673617379884035472E-19, 0.0002022161777894803118, 0.0003033242666842200612, 0.0004044323555789597563, 0.0005055404444736994515, 0.0006066485333684392550, 0.0008088647111579186453 ),
 ( 0.000000000000000000, 1.000000000000000000 ),
 .UNSPECIFIED. ) 
 GEOMETRIC_REPRESENTATION_ITEM ( )  RATIONAL_B_SPLINE_SURFACE ( (
 ( 1.000000000000000000, 0.7044453589051213882, 1.000000000000000000),
 ( 1.000000000000000000, 0.7046023864747805732, 1.000000000000000000),
 ( 1.000000000000000000, 0.7048235607688740911, 1.000000000000000000),
 ( 1.000000000000000000, 0.7054263556248401290, 1.000000000000000000),
 ( 1.000000000000000000, 0.7056784645812754775, 1.000000000000000000),
 ( 1.000000000000000000, 0.7063102947743578053, 1.000000000000000000),
 ( 1.000000000000000000, 0.7067030625551506962, 1.000000000000000000),
 ( 1.000000000000000000, 0.7074976564992083716, 1.000000000000000000),
 ( 1.000000000000000000, 0.7078925116172140042, 1.000000000000000000),
 ( 1.000000000000000000, 0.7085287470472093618, 1.000000000000000000),
 ( 1.000000000000000000, 0.7087824354666338866, 1.000000000000000000),
 ( 1.000000000000000000, 0.7093860731733975244, 1.000000000000000000),
 ( 1.000000000000000000, 0.7096079946502726887, 1.000000000000000000),
 ( 1.000000000000000000, 0.7097644798780707864, 1.000000000000000000) ) ) 
 REPRESENTATION_ITEM ( '' )  SURFACE ( )  );
#21718=EDGE_CURVE ( 'NONE', #21723, #7241, #4973, .T. ) ;
#21721=DIRECTION ( 'NONE',  ( 0.000000000000000000, 0.000000000000000000, -1.000000000000000000 ) ) ;
#21722=ORIENTED_EDGE ( 'NONE', *, *, #19203, .F. ) ;
#21723=VERTEX_POINT ( 'NONE', #7998 ) ;
#21731=CARTESIAN_POINT ( 'NONE',  ( 107.8265048288121051, 17.21207035378186845, -2.248242208486546989 ) ) ;
#21743=CARTESIAN_POINT ( 'NONE',  ( -30.49072021767876706, 13.22775097665176958, 1.500000000000000000 ) ) ;
#21744=FACE_OUTER_BOUND ( 'NONE', #5523, .T. ) ;
#21745=CARTESIAN_POINT ( 'NONE',  ( 56.97280603064898941, -277.2763395528616002, 1.508259000770581615 ) ) ;
#21747=CARTESIAN_POINT ( 'NONE',  ( 9.282537329959909655, 0.2172754300399125094, 1.041239158277188048 ) ) ;
#21766=CARTESIAN_POINT ( 'NONE',  ( 9.548498637265968370, 1.402184917482039994, -1.500000000000000000 ) ) ;
#21790=B_SPLINE_CURVE_WITH_KNOTS ( 'NONE', 3,
 ( #3023, #15707, #20391, #17699, #17533, #27913, #22739, #5338 ),
 .UNSPECIFIED., .F., .F.,
 ( 4, 2, 2, 4 ),
 ( 0.0001261938424379285015, 0.0002444035063406801295, 0.0003626131702434317846, 0.0005990324980489345526 ),
 .UNSPECIFIED. ) ;
#21812=LINE ( 'NONE', #18996, #20017 ) ;
#21817=CARTESIAN_POINT ( 'NONE',  ( 108.0731628266868540, 18.58555941254615007, 4.648189127559274603 ) ) ;
#21822=FACE_OUTER_BOUND ( 'NONE', #15102, .T. ) ;
#21834=CARTESIAN_POINT ( 'NONE',  ( 24.14622570346762842, 18.13272393406391814, -1.049999999999999822 ) ) ;
#21839=CARTESIAN_POINT ( 'NONE',  ( 9.065183082710460027, 0.01785380481418138293, 1.195037335522169730 ) ) ;
#21841=CARTESIAN_POINT ( 'NONE',  ( 107.7310687598602215, 16.68064466458321959, 1.424544220713904963 ) ) ;
#21845=CARTESIAN_POINT ( 'NONE',  ( 108.1156589233280272, 18.82219444680286458, -4.397958565568440115 ) ) ;
#21857=EDGE_LOOP ( 'NONE', ( #25165, #25135, #1641 ) ) ;
#21866=CARTESIAN_POINT ( 'NONE',  ( -59.39818691134999540, -5.278984095179490410, 5.312697832964588862 ) ) ;
#21888=CARTESIAN_POINT ( 'NONE',  ( -57.84278510284880781, -3.116935358302278747, 5.499999999999997335 ) ) ;
#21889=LINE ( 'NONE', #21584, #742 ) ;
#21891=DIRECTION ( 'NONE',  ( -0.4999999999999952816, -0.8660254037844413721, -0.000000000000000000 ) ) ;
#21896=CARTESIAN_POINT ( 'NONE',  ( -23.54713438637984169, 18.90773822806172433, 1.500000000000000000 ) ) ;
#21902=VECTOR ( 'NONE', #26133, 1000.000000000000000 ) ;
#21908=VECTOR ( 'NONE', #32742, 1000.000000000000114 ) ;
#21963=ORIENTED_EDGE ( 'NONE', *, *, #30021, .T. ) ;
#21976=( BOUNDED_CURVE ( )  B_SPLINE_CURVE ( 3, ( #20522, #22994, #12483, #33042 ),
 .UNSPECIFIED., .F., .F. ) 
 B_SPLINE_CURVE_WITH_KNOTS ( ( 4, 4 ),
 ( 3.159180468610128578, 3.757378358066267854 ),
 .UNSPECIFIED. ) 
 CURVE ( )  GEOMETRIC_REPRESENTATION_ITEM ( )  RATIONAL_B_SPLINE_CURVE ( ( 1.000000000000000000, 0.9704015875404256031, 0.9704015875404256031, 1.000000000000000000 ) ) 
 REPRESENTATION_ITEM ( '' )  );
#21980=CARTESIAN_POINT ( 'NONE',  ( 7.437041877750292684, 18.60036511249582958, -1.491740999229418385 ) ) ;
#21994=DIRECTION ( 'NONE',  ( 1.000000000000000000, 0.000000000000000000, 0.000000000000000000 ) ) ;
#22003=VECTOR ( 'NONE', #6041, 1000.000000000000114 ) ;
#22040=CARTESIAN_POINT ( 'NONE',  ( -25.11562363250528662, 4.199264901004248429, 2.140598393455739767 ) ) ;
#22045=VECTOR ( 'NONE', #21721, 1000.000000000000000 ) ;
#22053=FACE_OUTER_BOUND ( 'NONE', #15494, .T. ) ;
#22059=CIRCLE ( 'NONE', #14547, 0.4499999999999990119 ) ;
#22061=AXIS2_PLACEMENT_3D ( 'NONE', #21745, #6051, #29119 ) ;
#22071=EDGE_CURVE ( 'NONE', #28865, #28172, #25120, .T. ) ;
#22074=ORIENTED_EDGE ( 'NONE', *, *, #15446, .F. ) ;
#22081=EDGE_LOOP ( 'NONE', ( #17102, #15856, #24006, #7961 ) ) ;
#22083=CARTESIAN_POINT ( 'NONE',  ( 14.29722302835932624, 9.309426707029093251, 1.500000000000000222 ) ) ;
#22087=EDGE_CURVE ( 'NONE', #29681, #436, #32612, .T. ) ;
#22090=VECTOR ( 'NONE', #32105, 1000.000000000000000 ) ;
#22109=CARTESIAN_POINT ( 'NONE',  ( 8.917092964420161749, 0.3005351010058840977, 1.469472172318631920 ) ) ;
#22117=ORIENTED_EDGE ( 'NONE', *, *, #6106, .T. ) ;
#22129=CARTESIAN_POINT ( 'NONE',  ( -2.794738735352966685, 0.000000000000000000, 1.000000000000000000 ) ) ;
#22131=VECTOR ( 'NONE', #27331, 1000.000000000000000 ) ;
#22132=ORIENTED_EDGE ( 'NONE', *, *, #22372, .F. ) ;
#22137=ORIENTED_EDGE ( 'NONE', *, *, #21010, .F. ) ;
#22153=CIRCLE ( 'NONE', #4548, 0.4500000000000025646 ) ;
#22155=VERTEX_POINT ( 'NONE', #20114 ) ;
#22156=CARTESIAN_POINT ( 'NONE',  ( 14.23800746264082839, 22.11259878822726321, 1.508259000770582059 ) ) ;
#22160=CARTESIAN_POINT ( 'NONE',  ( -56.27770248097862549, -0.0003384977252891612984, 0.000000000000000000 ) ) ;
#22161=CARTESIAN_POINT ( 'NONE',  ( -2.794738735352966685, 0.000000000000000000, 1.000000000000000000 ) ) ;
#22163=CARTESIAN_POINT ( 'NONE',  ( -56.33578448492038859, 0.003046479527604620090, -1.000000000000000000 ) ) ;
#22188=FACE_OUTER_BOUND ( 'NONE', #10680, .T. ) ;
#22189=DIRECTION ( 'NONE',  ( -0.000000000000000000, -0.3746065934159164001, 0.9271838545667856479 ) ) ;
#22201=CARTESIAN_POINT ( 'NONE',  ( 24.97915472029188066, 18.93975620935289683, 1.499999999999998446 ) ) ;
#22206=CARTESIAN_POINT ( 'NONE',  ( -30.17749803717425294, 10.76421938935684075, 1.964586347758968232 ) ) ;
#22209=ORIENTED_EDGE ( 'NONE', *, *, #16398, .T. ) ;
#22216=DIRECTION ( 'NONE',  ( -1.000000000000000000, 0.000000000000000000, 0.000000000000000000 ) ) ;
#22232=ORIENTED_EDGE ( 'NONE', *, *, #30021, .F. ) ;
#22242=CARTESIAN_POINT ( 'NONE',  ( 18.77228938565977145, 14.95012848542240746, 1.500000000000000666 ) ) ;
#22246=CARTESIAN_POINT ( 'NONE',  ( -28.96127135574216638, 15.72250979567477636, 1.500000000000000000 ) ) ;
#22255=LINE ( 'NONE', #25072, #9248 ) ;
#22258=CARTESIAN_POINT ( 'NONE',  ( -41.54004718934325524, -10.96999999999998643, 9.000000000000000000 ) ) ;
#22271=CARTESIAN_POINT ( 'NONE',  ( 9.174708406371143710, 0.09531162291655657925, -1.030456265918283654 ) ) ;
#22281=DIRECTION ( 'NONE',  ( 1.000000000000000000, 0.000000000000000000, 0.000000000000000000 ) ) ;
#22283=DIRECTION ( 'NONE',  ( -1.000000000000000000, 0.000000000000000000, 0.000000000000000000 ) ) ;
#22284=EDGE_LOOP ( 'NONE', ( #6627, #27829, #14290, #30827, #15373 ) ) ;
#22288=ORIENTED_EDGE ( 'NONE', *, *, #23807, .T. ) ;
#22294=LINE ( 'NONE', #6589, #15569 ) ;
#22308=CARTESIAN_POINT ( 'NONE',  ( -56.34447759643617815, 0.004136860324227145148, -1.003319227365814470 ) ) ;
#22320=ADVANCED_FACE ( 'NONE', ( #28764 ), #3774, .F. ) ;
#22350=CARTESIAN_POINT ( 'NONE',  ( -38.14293509397970183, 21.49000000000000199, -1.050000000000000044 ) ) ;
#22357=VERTEX_POINT ( 'NONE', #8702 ) ;
#22364=DIRECTION ( 'NONE',  ( 0.000000000000000000, -0.000000000000000000, -1.000000000000000000 ) ) ;
#22372=EDGE_CURVE ( 'NONE', #17732, #10281, #18881, .T. ) ;
#22375=DIRECTION ( 'NONE',  ( -1.000000000000000000, 0.000000000000000000, 0.000000000000000000 ) ) ;
#22382=CARTESIAN_POINT ( 'NONE',  ( 107.5965811620429093, 18.76554845876667343, 5.148257179709845310 ) ) ;
#22385=CARTESIAN_POINT ( 'NONE',  ( 107.7536796087345294, 16.80655079293032017, -1.379243061950440108 ) ) ;
#22386=FACE_OUTER_BOUND ( 'NONE', #5066, .T. ) ;
#22394=CARTESIAN_POINT ( 'NONE',  ( -23.54713438637982748, 18.90773822806172433, 1.500000000000000000 ) ) ;
#22396=CYLINDRICAL_SURFACE ( 'NONE', #18255, 12.49867430706171767 ) ;
#22402=ORIENTED_EDGE ( 'NONE', *, *, #1597, .F. ) ;
#22422=CARTESIAN_POINT ( 'NONE',  ( 0.000000000000000000, 0.000000000000000000, -1.500000000000000000 ) ) ;
#22426=CARTESIAN_POINT ( 'NONE',  ( 8.870145747188287189, 0.000000000000000000, -1.000000000000001332 ) ) ;
#22432=EDGE_CURVE ( 'NONE', #8954, #1225, #20342, .T. ) ;
#22438=CARTESIAN_POINT ( 'NONE',  ( 107.4685836152551417, 18.03047445837466256, -4.889869265036825396 ) ) ;
#22457=AXIS2_PLACEMENT_3D ( 'NONE', #27999, #12751, #7587 ) ;
#22458=ORIENTED_EDGE ( 'NONE', *, *, #9139, .F. ) ;
#22477=CARTESIAN_POINT ( 'NONE',  ( 109.0524412912905774, 20.62920084672733267, -1.491740999229417941 ) ) ;
#22478=CARTESIAN_POINT ( 'NONE',  ( -56.27770248097862549, 0.4996615022747108448, 1.500000000000000000 ) ) ;
#22494=CARTESIAN_POINT ( 'NONE',  ( 56.97280603064898941, -277.2763395528616002, -1.500000000000000000 ) ) ;
#22524=CARTESIAN_POINT ( 'NONE',  ( -50.81000000000000227, -10.96999999999998643, 5.700000000000000178 ) ) ;
#22528=DIRECTION ( 'NONE',  ( 1.000000000000000000, -0.000000000000000000, -0.000000000000000000 ) ) ;
#22529=CARTESIAN_POINT ( 'NONE',  ( -56.32709181765920903, 0.0003929015865020345178, -1.038420530835418853 ) ) ;
#22544=LINE ( 'NONE', #25385, #4460 ) ;
#22545=VECTOR ( 'NONE', #12679, 1000.000000000000227 ) ;
#22566=CARTESIAN_POINT ( 'NONE',  ( 107.6996442589674103, 19.35565155597529596, 4.629213727441584325 ) ) ;
#22571=CARTESIAN_POINT ( 'NONE',  ( -50.81000000000000227, -10.96999999999998643, 1.500000000000000000 ) ) ;
#22577=CIRCLE ( 'NONE', #19912, 0.9999999999999991118 ) ;
#22580=CARTESIAN_POINT ( 'NONE',  ( -47.25352234179201361, 16.22999999999998266, 1.050000000000000044 ) ) ;
#22582=CARTESIAN_POINT ( 'NONE',  ( -22.65704777669159498, 18.60133783399176011, 1.500000000000506040 ) ) ;
#22595=CIRCLE ( 'NONE', #1237, 0.4499999999999997335 ) ;
#22600=CARTESIAN_POINT ( 'NONE',  ( 107.9956158609837047, 18.15374730895081257, -5.039121240573448013 ) ) ;
#22604=VERTEX_POINT ( 'NONE', #27175 ) ;
#22611=CARTESIAN_POINT ( 'NONE',  ( 21.09752163291441818, 16.24116299994017609, -1.050000000000000044 ) ) ;
#22626=CARTESIAN_POINT ( 'NONE',  ( 107.5416032035946898, 18.44933160811492101, -5.131841438779300546 ) ) ;
#22628=CARTESIAN_POINT ( 'NONE',  ( 8.930755659325139817, 0.4999999999999982792, -1.050000000000000044 ) ) ;
#22646=CARTESIAN_POINT ( 'NONE',  ( 5.865515302491369987, 15.00000000000000178, 1.508259000770582059 ) ) ;
#22647=ORIENTED_EDGE ( 'NONE', *, *, #11439, .T. ) ;
#22658=EDGE_LOOP ( 'NONE', ( #11649, #22989, #1350, #18625, #10537 ) ) ;
#22661=LINE ( 'NONE', #7103, #19744 ) ;
#22679=DIRECTION ( 'NONE',  ( 0.000000000000000000, 0.000000000000000000, -1.000000000000000000 ) ) ;
#22702=CARTESIAN_POINT ( 'NONE',  ( 107.3084118612033677, 16.37966538140715400, -1.491489915294727187 ) ) ;
#22707=DIRECTION ( 'NONE',  ( 1.000000000000000000, 0.000000000000000000, 0.000000000000000000 ) ) ;
#22709=CARTESIAN_POINT ( 'NONE',  ( -56.55463451115983986, 0.05299951999074122705, -1.274799463869835447 ) ) ;
#22739=CARTESIAN_POINT ( 'NONE',  ( -53.79666904180695042, 5.504338532704765363, 1.390325731058407399 ) ) ;
#22757=CARTESIAN_POINT ( 'NONE',  ( 107.5053003840741184, 18.24082670017404340, -5.040895989151252365 ) ) ;
#22759=CARTESIAN_POINT ( 'NONE',  ( -18.19731407151451918, 15.53049510967715463, 1.844195982360324226 ) ) ;
#22771=CARTESIAN_POINT ( 'NONE',  ( 22.66400097956248061, 17.80079245417792322, -1.500000000000000000 ) ) ;
#22785=CARTESIAN_POINT ( 'NONE',  ( 109.0524412912905774, 20.62920084672733267, 1.508259000770582059 ) ) ;
#22793=CARTESIAN_POINT ( 'NONE',  ( -2.506063600758156262, 0.4999999999999998890, 1.500000000000000000 ) ) ;
#22808=DIRECTION ( 'NONE',  ( 1.000000000000000000, 0.000000000000000000, 0.000000000000000000 ) ) ;
#22811=CARTESIAN_POINT ( 'NONE',  ( 78.40736801748178664, 24.56822898102832653, -4.612695725900422872 ) ) ;
#22816=CARTESIAN_POINT ( 'NONE',  ( -23.54713438637982748, 10.38166835460962645, 8.992620707982547756 ) ) ;
#22825=CARTESIAN_POINT ( 'NONE',  ( -41.09688370048776562, -10.96999999999998643, 8.628141679950115162 ) ) ;
#22827=EDGE_LOOP ( 'NONE', ( #20584, #16974, #31269, #21000 ) ) ;
#22840=DIRECTION ( 'NONE',  ( -0.8660254037844409281, 0.4999999999999960587, 0.000000000000000000 ) ) ;
#22844=LINE ( 'NONE', #2798, #15507 ) ;
#22851=CARTESIAN_POINT ( 'NONE',  ( -32.42885140446504977, -0.0003384977252881313063, 1.500000000000000000 ) ) ;
#22853=CARTESIAN_POINT ( 'NONE',  ( -50.81000000000000227, -10.96999999999998643, 5.700000000000000178 ) ) ;
#22858=ORIENTED_EDGE ( 'NONE', *, *, #13268, .F. ) ;
#22860=ORIENTED_EDGE ( 'NONE', *, *, #27574, .F. ) ;
#22863=CARTESIAN_POINT ( 'NONE',  ( 107.5518430304144886, 18.50822805398703252, 5.148363126710675530 ) ) ;
#22865=CARTESIAN_POINT ( 'NONE',  ( 107.9622325421415212, 20.81773585569407459, -1.491740999229417941 ) ) ;
#22866=VERTEX_POINT ( 'NONE', #8484 ) ;
#22872=EDGE_CURVE ( 'NONE', #4298, #14600, #245, .T. ) ;
#22897=CARTESIAN_POINT ( 'NONE',  ( 108.3696618535068126, 20.23658298680886958, 0.4463807625373348298 ) ) ;
#22910=CARTESIAN_POINT ( 'NONE',  ( -20.11703670643211339, 17.43879752748101808, 1.797616734936172023 ) ) ;
#22965=DIRECTION ( 'NONE',  ( -1.000000000000000000, 0.000000000000000000, 0.000000000000000000 ) ) ;
#22972=EDGE_CURVE ( 'NONE', #19201, #31304, #3706, .T. ) ;
#22983=VECTOR ( 'NONE', #25365, 1000.000000000000227 ) ;
#22989=ORIENTED_EDGE ( 'NONE', *, *, #29276, .F. ) ;
#22994=CARTESIAN_POINT ( 'NONE',  ( -54.05892116629462407, 5.342703470191877635, 1.499999999999898304 ) ) ;
#23005=AXIS2_PLACEMENT_3D ( 'NONE', #10696, #30454, #27760 ) ;
#23007=CARTESIAN_POINT ( 'NONE',  ( 107.6567584420023280, 16.56235156533065123, -1.437178912938893438 ) ) ;
#23015=LINE ( 'NONE', #27871, #31097 ) ;
#23021=AXIS2_PLACEMENT_3D ( 'NONE', #29037, #11127, #13780 ) ;
#23023=CARTESIAN_POINT ( 'NONE',  ( 108.0792187206003518, 18.61928101938756441, 5.148720508272580432 ) ) ;
#23041=DIRECTION ( 'NONE',  ( 1.000000000000000000, 5.361488761196502513E-16, -0.000000000000000000 ) ) ;
#23042=ORIENTED_EDGE ( 'NONE', *, *, #3269, .T. ) ;
#23049=VERTEX_POINT ( 'NONE', #7454 ) ;
#23051=CARTESIAN_POINT ( 'NONE',  ( 107.8715724909225173, 17.46302487926284996, -2.785784909554371858 ) ) ;
#23054=CARTESIAN_POINT ( 'NONE',  ( -37.80541082197543545, 3.520075575296775838, 1.500000000000000222 ) ) ;
#23056=ORIENTED_EDGE ( 'NONE', *, *, #19757, .F. ) ;
#23060=( BOUNDED_SURFACE ( )  B_SPLINE_SURFACE ( 3, 2, ( 
 ( #7142, #17338, #32396 ),
 ( #4629, #14805, #25002 ),
 ( #2116, #29551, #32731 ),
 ( #17484, #27682, #6637 ) ),
 .UNSPECIFIED., .F., .F., .F. ) 
 B_SPLINE_SURFACE_WITH_KNOTS ( ( 4, 4 ),
 ( 3, 3 ),
 ( 0.0001830234508717654455, 0.0002186438461075107423 ),
 ( 0.000000000000000000, 1.000000000000000000 ),
 .UNSPECIFIED. ) 
 GEOMETRIC_REPRESENTATION_ITEM ( )  RATIONAL_B_SPLINE_SURFACE ( (
 ( 1.000000000000000000, 0.7071067811865441310, 1.000000000000000000),
 ( 1.000000000000000000, 0.7464405371105022891, 1.000000000000000000),
 ( 1.000000000000000000, 0.7823978085798950488, 1.000000000000000000),
 ( 1.000000000000000000, 0.8123215895921556129, 1.000000000000000000) ) ) 
 REPRESENTATION_ITEM ( '' )  SURFACE ( )  );
#23063=CARTESIAN_POINT ( 'NONE',  ( 14.23800746264082839, 22.11259878822726321, -1.491740999229417941 ) ) ;
#23069=CARTESIAN_POINT ( 'NONE',  ( -28.84101375771544440, 6.775292334731556565, 2.070007460141180200 ) ) ;
#23082=VERTEX_POINT ( 'NONE', #15166 ) ;
#23084=EDGE_CURVE ( 'NONE', #25302, #29856, #31555, .T. ) ;
#23106=ADVANCED_FACE ( 'NONE', ( #12308 ), #32267, .T. ) ;
#23110=CARTESIAN_POINT ( 'NONE',  ( -28.64700708014754582, 15.87868365833990048, 1.835632814149771086 ) ) ;
#23114=EDGE_CURVE ( 'NONE', #9305, #7402, #10125, .T. ) ;
#23120=EDGE_LOOP ( 'NONE', ( #30178, #29422 ) ) ;
#23142=FACE_OUTER_BOUND ( 'NONE', #31472, .T. ) ;
#23145=AXIS2_PLACEMENT_3D ( 'NONE', #20408, #23244, #31273 ) ;
#23158=EDGE_CURVE ( 'NONE', #32925, #17962, #7536, .T. ) ;
#23165=CARTESIAN_POINT ( 'NONE',  ( -30.51827900900859802, 4.402097243136377180, 5.049999999999999822 ) ) ;
#23189=DIRECTION ( 'NONE',  ( -1.000000000000000000, 3.119226488900586565E-17, -7.720356475505610171E-17 ) ) ;
#23217=EDGE_LOOP ( 'NONE', ( #4744, #29051, #25952, #21963 ) ) ;
#23223=ADVANCED_FACE ( 'NONE', ( #15475 ), #3136, .T. ) ;
#23227=ORIENTED_EDGE ( 'NONE', *, *, #29793, .T. ) ;
#23237=CARTESIAN_POINT ( 'NONE',  ( -31.80940264096946635, 0.000000000000000000, 1.292893218813456535 ) ) ;
#23241=CARTESIAN_POINT ( 'NONE',  ( 107.7674015406661425, 19.73292211253945538, -3.806892900268363800 ) ) ;
#23244=DIRECTION ( 'NONE',  ( 8.326672684688674053E-17, 0.3746065934159164001, -0.9271838545667857590 ) ) ;
#23248=DIRECTION ( 'NONE',  ( 8.659560562355058583E-17, 0.3907311284892827086, 0.9205048534524364889 ) ) ;
#23249=B_SPLINE_CURVE_WITH_KNOTS ( 'NONE', 3,
 ( #6865, #11905, #22109, #32323 ),
 .UNSPECIFIED., .F., .F.,
 ( 4, 4 ),
 ( 9.757819552369539906E-19, 0.0003032258210394150151 ),
 .UNSPECIFIED. ) ;
#23256=CARTESIAN_POINT ( 'NONE',  ( -19.39001922729729088, 5.591785014860885639, 2.102227713797247155 ) ) ;
#23261=ADVANCED_FACE ( 'NONE', ( #1589 ), #11713, .T. ) ;
#23269=CARTESIAN_POINT ( 'NONE',  ( 7.577572045913208321, 15.00000000000002132, 4.629213727441584325 ) ) ;
#23276=DIRECTION ( 'NONE',  ( -0.006769954505784999722, -0.9999770835954140402, -0.000000000000000000 ) ) ;
#23278=CARTESIAN_POINT ( 'NONE',  ( -29.36843332409777574, 14.72720444484234115, 1.864077576974227934 ) ) ;
#23287=ORIENTED_EDGE ( 'NONE', *, *, #23640, .T. ) ;
#23298=ORIENTED_EDGE ( 'NONE', *, *, #12853, .T. ) ;
#23306=ORIENTED_EDGE ( 'NONE', *, *, #12949, .T. ) ;
#23309=DIRECTION ( 'NONE',  ( 0.4999999999999981681, 0.8660254037844395958, -0.000000000000000000 ) ) ;
#23339=CARTESIAN_POINT ( 'NONE',  ( 11.62091610453458301, 3.869040036316004016, 1.050000000000000044 ) ) ;
#23342=CARTESIAN_POINT ( 'NONE',  ( -41.54004718934325524, -10.96999999999998643, 8.549999999999998934 ) ) ;
#23347=CARTESIAN_POINT ( 'NONE',  ( 2.652619124157556740, 0.000000000000000000, -1.000000000000000000 ) ) ;
#23356=CARTESIAN_POINT ( 'NONE',  ( 108.0068349480237373, 18.21621961241920573, 4.414771370926587224 ) ) ;
#23373=CARTESIAN_POINT ( 'NONE',  ( 12.40148790557316616, 21.49000000000003041, -1.500000000000000000 ) ) ;
#23376=CARTESIAN_POINT ( 'NONE',  ( 9.297238421960550170, 0.2387279282522293267, -1.050000000000000044 ) ) ;
#23394=EDGE_CURVE ( 'NONE', #17959, #32155, #16620, .T. ) ;
#23400=ORIENTED_EDGE ( 'NONE', *, *, #18924, .F. ) ;
#23401=CARTESIAN_POINT ( 'NONE',  ( -23.54713438638086842, 3.998227953278294944, 2.146185852361370383 ) ) ;
#23412=CARTESIAN_POINT ( 'NONE',  ( 10.51841884045068731, 2.077444665426179782, 1.500000000000118572 ) ) ;
#23419=EDGE_CURVE ( 'NONE', #8954, #28455, #8090, .T. ) ;
#23420=CARTESIAN_POINT ( 'NONE',  ( -30.10261078476095520, 12.34770688644884906, 1.923950361969430922 ) ) ;
#23423=CARTESIAN_POINT ( 'NONE',  ( 109.7786606840771952, 18.61415246516070354, 5.412820279296878923 ) ) ;
#23447=DIRECTION ( 'NONE',  ( -0.000000000000000000, -0.000000000000000000, -1.000000000000000000 ) ) ;
#23452=LINE ( 'NONE', #15927, #25077 ) ;
#23465=( BOUNDED_CURVE ( )  B_SPLINE_CURVE ( 3, ( #30608, #23054, #10013, #20224 ),
 .UNSPECIFIED., .F., .F. ) 
 B_SPLINE_CURVE_WITH_KNOTS ( ( 4, 4 ),
 ( 3.141592653589793116, 6.283185307179586232 ),
 .UNSPECIFIED. ) 
 CURVE ( )  GEOMETRIC_REPRESENTATION_ITEM ( )  RATIONAL_B_SPLINE_CURVE ( ( 1.000000000000000000, 0.3333333333333333703, 0.3333333333333333703, 1.000000000000000000 ) ) 
 REPRESENTATION_ITEM ( '' )  );
#23469=CARTESIAN_POINT ( 'NONE',  ( 12.40148790557316616, 21.49000000000003041, -1.500000000000000000 ) ) ;
#23483=ORIENTED_EDGE ( 'NONE', *, *, #23847, .T. ) ;
#23491=EDGE_LOOP ( 'NONE', ( #7531, #32728, #13718, #32418 ) ) ;
#23492=CARTESIAN_POINT ( 'NONE',  ( 13.24811108103750712, 6.657149145102930987, 1.050000000000000266 ) ) ;
#23496=ORIENTED_EDGE ( 'NONE', *, *, #28790, .T. ) ;
#23511=AXIS2_PLACEMENT_3D ( 'NONE', #5296, #21177, #18829 ) ;
#23512=CARTESIAN_POINT ( 'NONE',  ( 9.331062908042598636, 15.00000000000002132, -4.612695725900422872 ) ) ;
#23529=VERTEX_POINT ( 'NONE', #8087 ) ;
#23534=CARTESIAN_POINT ( 'NONE',  ( 9.284228442262035585, 0.2197421434176238808, -1.042917449647795758 ) ) ;
#23553=ORIENTED_EDGE ( 'NONE', *, *, #10220, .F. ) ;
#23554=CARTESIAN_POINT ( 'NONE',  ( -57.39048296612208588, -3.170628888746132468, 5.871858320049880398 ) ) ;
#23572=CARTESIAN_POINT ( 'NONE',  ( 18.00993182317604990, 14.21018869494618819, -1.500000000000000000 ) ) ;
#23575=AXIS2_PLACEMENT_3D ( 'NONE', #13891, #29142, #6229 ) ;
#23576=CARTESIAN_POINT ( 'NONE',  ( 11.83510569430203319, 5.122261773727990075, 1.500000000000000000 ) ) ;
#23584=CARTESIAN_POINT ( 'NONE',  ( -23.54713438637982748, 5.934235225036485595, 7.654118351624816796 ) ) ;
#23588=CARTESIAN_POINT ( 'NONE',  ( -28.03779898944224058, 16.55826090817324925, 1.819008976926004717 ) ) ;
#23594=CARTESIAN_POINT ( 'NONE',  ( -53.35155202832373078, 4.402097243136373628, 5.049999999999999822 ) ) ;
#23610=ORIENTED_EDGE ( 'NONE', *, *, #12194, .T. ) ;
#23625=AXIS2_PLACEMENT_3D ( 'NONE', #10056, #30472, #15398 ) ;
#23629=VECTOR ( 'NONE', #20580, 1000.000000000000227 ) ;
#23638=EDGE_LOOP ( 'NONE', ( #20868, #23496, #17296, #7905, #7575 ) ) ;
#23640=EDGE_CURVE ( 'NONE', #21723, #6904, #5428, .T. ) ;
#23641=CARTESIAN_POINT ( 'NONE',  ( 107.3512941337518498, 17.37330583879708001, 3.589055591124487687 ) ) ;
#23645=AXIS2_PLACEMENT_3D ( 'NONE', #28351, #18643, #13456 ) ;
#23649=DIRECTION ( 'NONE',  ( -1.000000000000000000, 0.000000000000000000, 0.000000000000000000 ) ) ;
#23657=LINE ( 'NONE', #31211, #15056 ) ;
#23674=ORIENTED_EDGE ( 'NONE', *, *, #19757, .T. ) ;
#23675=( BOUNDED_SURFACE ( )  B_SPLINE_SURFACE ( 3, 2, ( 
 ( #21537, #31744, #8962 ),
 ( #16660, #9125, #32053 ),
 ( #4484, #21839, #19354 ),
 ( #29557, #16985, #13976 ),
 ( #32244, #26872, #6299 ),
 ( #9462, #27185, #6644 ) ),
 .UNSPECIFIED., .F., .F., .F. ) 
 B_SPLINE_SURFACE_WITH_KNOTS ( ( 4, 2, 4 ),
 ( 3, 3 ),
 ( 6.884163014324157004, 7.369072324149319897, 7.853981633974482790 ),
 ( 0.000000000000000000, 1.000000000000000000 ),
 .UNSPECIFIED. ) 
 GEOMETRIC_REPRESENTATION_ITEM ( )  RATIONAL_B_SPLINE_SURFACE ( (
 ( 1.000000000000000000, 0.8123215895924648100, 1.000000000000000000),
 ( 1.000000000000000000, 0.8591172521900213299, 1.000000000000000000),
 ( 1.000000000000000000, 0.9088222585364075234, 1.000000000000000000),
 ( 1.000000000000000000, 0.9794174349135026381, 1.000000000000000000),
 ( 1.000000000000000000, 1.000375673120273978, 1.000000000000000000),
 ( 1.000000000000000000, 1.000000000000000000, 1.000000000000000000) ) ) 
 REPRESENTATION_ITEM ( '' )  SURFACE ( )  );
#23677=FACE_OUTER_BOUND ( 'NONE', #3490, .T. ) ;
#23680=CARTESIAN_POINT ( 'NONE',  ( 2.514244811554134262, -8.107161948574434494E-17, -1.252246291852655125 ) ) ;
#23682=VECTOR ( 'NONE', #27794, 1000.000000000000000 ) ;
#23687=DIRECTION ( 'NONE',  ( -5.361488761196516318E-16, 1.000000000000000000, 0.000000000000000000 ) ) ;
#23689=CARTESIAN_POINT ( 'NONE',  ( -25.41317123495379704, 3.720325412122147846, 1.500000000000000000 ) ) ;
#23700=VECTOR ( 'NONE', #32735, 1000.000000000000000 ) ;
#23707=CARTESIAN_POINT ( 'NONE',  ( 9.288460890967574102, 0.2259157356912394610, 1.047117114142813499 ) ) ;
#23713=EDGE_CURVE ( 'NONE', #14512, #26215, #9051, .T. ) ;
#23716=CARTESIAN_POINT ( 'NONE',  ( 108.2737967297448307, 19.70276815113069091, -2.517673782553874862 ) ) ;
#23744=EDGE_LOOP ( 'NONE', ( #15759, #27189, #1539, #27529 ) ) ;
#23752=CARTESIAN_POINT ( 'NONE',  ( 1.787149210215136508, -1.031811077599730231, -1.500000000000000000 ) ) ;
#23755=CARTESIAN_POINT ( 'NONE',  ( 21.51801198755429922, 16.55905037279375591, 1.500000000000234257 ) ) ;
#23757=PLANE ( 'NONE',  #3338 ) ;
#23761=CARTESIAN_POINT ( 'NONE',  ( -25.76785678020393178, 4.411679249915887446, 2.134707912735335888 ) ) ;
#23764=CARTESIAN_POINT ( 'NONE',  ( -17.09300656982994937, 9.321674377477680906, 2.002134007589346343 ) ) ;
#23765=CARTESIAN_POINT ( 'NONE',  ( 46.69789307159569347, 25.15383447853596621, 4.629213727441585213 ) ) ;
#23780=VERTEX_POINT ( 'NONE', #27469 ) ;
#23784=ORIENTED_EDGE ( 'NONE', *, *, #18081, .F. ) ;
#23790=CARTESIAN_POINT ( 'NONE',  ( 14.71918161838887684, 9.125819088727514128, -1.050000000000000044 ) ) ;
#23796=CARTESIAN_POINT ( 'NONE',  ( -57.14353245301024486, 0.5000000000000000000, -1.500000000000000000 ) ) ;
#23807=EDGE_CURVE ( 'NONE', #30095, #24602, #1726, .T. ) ;
#23825=VERTEX_POINT ( 'NONE', #24789 ) ;
#23831=CARTESIAN_POINT ( 'NONE',  ( -53.98119003043982644, 5.049498764322128963, 2.713197721588770595 ) ) ;
#23847=EDGE_CURVE ( 'NONE', #21704, #8954, #25099, .T. ) ;
#23869=CARTESIAN_POINT ( 'NONE',  ( 108.1608272491863971, 19.07370950775312579, 3.877216635335003048 ) ) ;
#23872=ORIENTED_EDGE ( 'NONE', *, *, #30993, .F. ) ;
#23881=ADVANCED_FACE ( 'NONE', ( #7889 ), #15246, .T. ) ;
#23885=CARTESIAN_POINT ( 'NONE',  ( 17.41559371906258136, 18.02474698348859405, 1.508259000770581615 ) ) ;
#23899=EDGE_CURVE ( 'NONE', #11936, #9106, #5993, .T. ) ;
#23901=CARTESIAN_POINT ( 'NONE',  ( 11.15636752060594716, 3.970267605981960379, -1.500000000000000222 ) ) ;
#23902=ORIENTED_EDGE ( 'NONE', *, *, #26197, .T. ) ;
#23904=CARTESIAN_POINT ( 'NONE',  ( 12.93395381280125278, 7.012641540630032644, 1.500000000000000000 ) ) ;
#23910=CARTESIAN_POINT ( 'NONE',  ( -30.17898719005535213, 11.44152090502456787, 1.947135075133271220 ) ) ;
#23912=CARTESIAN_POINT ( 'NONE',  ( -23.54713438637982748, 3.520075575296777171, 1.500000000000000000 ) ) ;
#23914=CARTESIAN_POINT ( 'NONE',  ( 8.870145747188287189, 0.5000000000000001110, 0.000000000000000000 ) ) ;
#23920=( BOUNDED_SURFACE ( )  B_SPLINE_SURFACE ( 3, 2, ( 
 ( #19546, #32081, #6490 ),
 ( #4010, #14178, #24377 ),
 ( #29743, #1493, #11669 ),
 ( #9152, #24884, #29238 ) ),
 .UNSPECIFIED., .F., .F., .F. ) 
 B_SPLINE_SURFACE_WITH_KNOTS ( ( 4, 4 ),
 ( 3, 3 ),
 ( 0.000000000000000000, 0.003454001599076453322 ),
 ( 0.000000000000000000, 1.000000000000000000 ),
 .UNSPECIFIED. ) 
 GEOMETRIC_REPRESENTATION_ITEM ( )  RATIONAL_B_SPLINE_SURFACE ( (
 ( 1.000000000000000000, 0.7097644798780626818, 1.000000000000000000),
 ( 1.000000000000000000, 0.7097691176663378787, 1.000000000000000000),
 ( 1.000000000000000000, 0.7097737773069716649, 1.000000000000000000),
 ( 1.000000000000000000, 0.7097784590644244940, 1.000000000000000000) ) ) 
 REPRESENTATION_ITEM ( '' )  SURFACE ( )  );
#23923=CARTESIAN_POINT ( 'NONE',  ( 108.1033628964161295, 18.75372531717770386, -4.515627636720681792 ) ) ;
#23928=DIRECTION ( 'NONE',  ( 1.000000000000000000, 0.000000000000000000, 0.000000000000000000 ) ) ;
#23938=CARTESIAN_POINT ( 'NONE',  ( 9.302055952181039089, 0.2457637073014076745, -1.050000000000000044 ) ) ;
#23951=EDGE_CURVE ( 'NONE', #14212, #32393, #17201, .T. ) ;
#23955=CARTESIAN_POINT ( 'NONE',  ( -41.86373177837819526, -16.13513036599590222, 5.128141679950119602 ) ) ;
#23961=ORIENTED_EDGE ( 'NONE', *, *, #15680, .F. ) ;
#23970=PLANE ( 'NONE',  #11777 ) ;
#23974=CARTESIAN_POINT ( 'NONE',  ( 26.08945412691624099, 19.05746434167065928, -1.050000000000000044 ) ) ;
#23992=CARTESIAN_POINT ( 'NONE',  ( 10.47272779071480819, 17.64623289522323191, -5.396302277755719246 ) ) ;
#23995=ORIENTED_EDGE ( 'NONE', *, *, #11682, .F. ) ;
#24002=EDGE_CURVE ( 'NONE', #1418, #4740, #16237, .T. ) ;
#24005=CARTESIAN_POINT ( 'NONE',  ( 15.28872660057388799, 20.76088595412472060, 4.629213727441584325 ) ) ;
#24006=ORIENTED_EDGE ( 'NONE', *, *, #24585, .T. ) ;
#24027=CARTESIAN_POINT ( 'NONE',  ( -59.75626822162179508, -5.804869634004071521, 5.128141679950119602 ) ) ;
#24036=AXIS2_PLACEMENT_3D ( 'NONE', #5416, #7410, #28148 ) ;
#24056=CARTESIAN_POINT ( 'NONE',  ( 16.54275606342307725, 11.79585867019468992, 1.500000000000000000 ) ) ;
#24066=AXIS2_PLACEMENT_3D ( 'NONE', #4480, #7807, #788 ) ;
#24095=EDGE_CURVE ( 'NONE', #20953, #25225, #23015, .T. ) ;
#24101=CARTESIAN_POINT ( 'NONE',  ( 10.52016698309699372, 2.080188552104354383, -1.499999999999170441 ) ) ;
#24121=CARTESIAN_POINT ( 'NONE',  ( 8.870145747188287189, 0.000000000000000000, -1.000000000000000000 ) ) ;
#24125=EDGE_CURVE ( 'NONE', #17057, #27222, #4408, .T. ) ;
#24145=ORIENTED_EDGE ( 'NONE', *, *, #1799, .T. ) ;
#24162=VECTOR ( 'NONE', #31436, 1000.000000000000000 ) ;
#24170=CARTESIAN_POINT ( 'NONE',  ( 108.0068349480237515, 18.21621961241920573, 4.414771370926588112 ) ) ;
#24185=EDGE_CURVE ( 'NONE', #29127, #24602, #30078, .T. ) ;
#24193=AXIS2_PLACEMENT_3D ( 'NONE', #18021, #32760, #25027 ) ;
#24208=DIRECTION ( 'NONE',  ( -0.000000000000000000, -1.000000000000000000, -0.000000000000000000 ) ) ;
#24215=FACE_OUTER_BOUND ( 'NONE', #24440, .T. ) ;
#24220=VECTOR ( 'NONE', #7247, 1000.000000000000227 ) ;
#24224=CARTESIAN_POINT ( 'NONE',  ( -59.00528660915777124, -4.776024318451533190, 5.482724712897171671 ) ) ;
#24225=AXIS2_PLACEMENT_3D ( 'NONE', #10103, #28328, #17819 ) ;
#24226=ADVANCED_FACE ( 'NONE', ( #15673 ), #8620, .T. ) ;
#24232=ORIENTED_EDGE ( 'NONE', *, *, #28790, .F. ) ;
#24234=ORIENTED_EDGE ( 'NONE', *, *, #13653, .T. ) ;
#24244=DIRECTION ( 'NONE',  ( 1.000000000000000000, 0.000000000000000000, 0.000000000000000000 ) ) ;
#24246=CARTESIAN_POINT ( 'NONE',  ( -56.33578448492038859, 0.003046479527604620090, 1.500000000000000000 ) ) ;
#24254=CARTESIAN_POINT ( 'NONE',  ( -29.34923860676941842, 14.86020659576501224, 1.860696004608973109 ) ) ;
#24255=DIRECTION ( 'NONE',  ( 1.000000000000000000, 0.000000000000000000, 0.000000000000000000 ) ) ;
#24280=DIRECTION ( 'NONE',  ( -0.4999999999999978906, -0.8660254037844399289, 0.000000000000000000 ) ) ;
#24289=DIRECTION ( 'NONE',  ( -8.326672684688671588E-17, -0.3746065934159163446, 0.9271838545667856479 ) ) ;
#24296=CLOSED_SHELL ( 'NONE', ( #26993, #32514, #2481, #12005, #6851, #22320, #7117, #7304, #18149, #6729, #15290, #17532, #20200, #20343, #20085, #1233, #30511, #7217, #21210, #26472, #16149, #19620, #6647, #24226, #3597, #32702, #24888, #7826, #23261, #7776, #23106, #19374, #16098, #30873, #13317, #13075, #27957, #16525, #18471, #31279, #5497, #295, #7929, #31835, #3037, #30692, #29274, #32252, #20009, #29676, #25569, #18982, #3846, #4096, #13301, #1644, #26697, #18137, #24879, #7319, #17937, #1590, #67, #17585, #14225, #16938, #13669, #14042, #20801, #26829, #13255, #25878, #282, #3564, #4758, #13547, #25411, #5711, #31765, #25953, #31378, #23223, #25716, #3386, #12739, #4612, #3675, #15802, #2067, #28042, #20505, #28143, #123, #6476, #10553, #15982, #19228, #1053, #2279, #18130, #6325, #20556, #31474, #12606, #8513, #32681, #27895, #494, #29377, #26708, #18800, #19121, #18124, #7966, #23881 ) ) ;
#24302=CARTESIAN_POINT ( 'NONE',  ( 46.92593983402662872, 24.78664516185572708, -5.396302277755718357 ) ) ;
#24315=ORIENTED_EDGE ( 'NONE', *, *, #5697, .F. ) ;
#24316=CARTESIAN_POINT ( 'NONE',  ( 26.08945412691624099, 19.05746434167065928, 1.050000000000000044 ) ) ;
#24318=DIRECTION ( 'NONE',  ( -0.8476835837759374437, 0.5305021600302710638, 0.000000000000000000 ) ) ;
#24324=FACE_OUTER_BOUND ( 'NONE', #3788, .T. ) ;
#24328=CARTESIAN_POINT ( 'NONE',  ( 79.17573959169237696, 22.98125563777605151, 4.629213727441585213 ) ) ;
#24370=CYLINDRICAL_SURFACE ( 'NONE', #3365, 8.025310301077755781 ) ;
#24371=CARTESIAN_POINT ( 'NONE',  ( -58.44930958907092844, -3.890057978239433112, 5.414538096233303399 ) ) ;
#24376=ORIENTED_EDGE ( 'NONE', *, *, #5503, .F. ) ;
#24377=CARTESIAN_POINT ( 'NONE',  ( 107.3512941337730950, 17.37330583879339940, -3.572537589583222317 ) ) ;
#24398=VERTEX_POINT ( 'NONE', #11470 ) ;
#24404=FACE_OUTER_BOUND ( 'NONE', #18199, .T. ) ;
#24407=PRODUCT_DEFINITION_SHAPE ( 'NONE', 'NONE',  #2068 ) ;
#24410=VERTEX_POINT ( 'NONE', #32379 ) ;
#24411=PLANE ( 'NONE',  #31615 ) ;
#24424=CYLINDRICAL_SURFACE ( 'NONE', #7065, 5.100000000000000533 ) ;
#24425=DIRECTION ( 'NONE',  ( 0.000000000000000000, -0.9271838545667856479, -0.3746065934159162891 ) ) ;
#24428=CARTESIAN_POINT ( 'NONE',  ( 10.52016698344803558, 2.080188551888086934, -1.050000000000000044 ) ) ;
#24440=EDGE_LOOP ( 'NONE', ( #13243, #13397, #20323, #26998 ) ) ;
#24455=EDGE_LOOP ( 'NONE', ( #1832, #11595, #28751, #16026 ) ) ;
#24460=PLANE ( 'NONE',  #2200 ) ;
#24464=CARTESIAN_POINT ( 'NONE',  ( -56.40999100167014291, 0.01723988236541950519, -1.011943104398846049 ) ) ;
#24479=ORIENTED_EDGE ( 'NONE', *, *, #25085, .T. ) ;
#24484=EDGE_LOOP ( 'NONE', ( #3566, #6894, #5365, #12292 ) ) ;
#24499=EDGE_LOOP ( 'NONE', ( #17855, #32330, #21392, #4202 ) ) ;
#24514=CARTESIAN_POINT ( 'NONE',  ( -29.55113075415135881, 8.128449843281648768, 2.033773019847134655 ) ) ;
#24520=EDGE_CURVE ( 'NONE', #536, #32661, #169, .T. ) ;
#24521=CIRCLE ( 'NONE', #18665, 0.4499999999999999001 ) ;
#24526=CARTESIAN_POINT ( 'NONE',  ( 107.8775346209187234, 20.32496164342445510, 0.000000000000000000 ) ) ;
#24527=ORIENTED_EDGE ( 'NONE', *, *, #16142, .T. ) ;
#24536=AXIS2_PLACEMENT_3D ( 'NONE', #30688, #15266, #7256 ) ;
#24555=CARTESIAN_POINT ( 'NONE',  ( 13.56175523640557756, 21.92011675111214686, 1.183903575935491226 ) ) ;
#24578=FACE_OUTER_BOUND ( 'NONE', #3887, .T. ) ;
#24584=FACE_OUTER_BOUND ( 'NONE', #13195, .T. ) ;
#24585=EDGE_CURVE ( 'NONE', #536, #25915, #3256, .T. ) ;
#24590=CARTESIAN_POINT ( 'NONE',  ( 23.82349779659365652, 17.94250544621599630, -1.049999999999882361 ) ) ;
#24591=CARTESIAN_POINT ( 'NONE',  ( 9.282537329960035777, 0.2172754300400975558, -1.041239158277174948 ) ) ;
#24598=DIRECTION ( 'NONE',  ( -0.000000000000000000, -0.000000000000000000, -1.000000000000000000 ) ) ;
#24600=CARTESIAN_POINT ( 'NONE',  ( 15.28872660057388977, 20.76088595412472415, -4.612695725900422872 ) ) ;
#24601=CARTESIAN_POINT ( 'NONE',  ( -45.71000000000000085, -10.96999999999998643, 1.499999999999999556 ) ) ;
#24602=VERTEX_POINT ( 'NONE', #2768 ) ;
#24623=ORIENTED_EDGE ( 'NONE', *, *, #30900, .T. ) ;
#24627=B_SPLINE_CURVE_WITH_KNOTS ( 'NONE', 3,
 ( #31563, #646, #28720, #8647, #26404, #29067, #3161, #15993, #6154, #3505 ),
 .UNSPECIFIED., .F., .F.,
 ( 4, 2, 2, 2, 4 ),
 ( 4.336808689942017736E-18, 0.0001594250696560639969, 0.0003188501393121236571, 0.0006377002786242324606, 0.001275400557248461235 ),
 .UNSPECIFIED. ) ;
#24635=CARTESIAN_POINT ( 'NONE',  ( -56.69506688323772892, 0.2173071790064931286, 1.574469351512994386 ) ) ;
#24640=AXIS2_PLACEMENT_3D ( 'NONE', #28883, #26698, #1326 ) ;
#24685=DIRECTION ( 'NONE',  ( -1.000000000000000000, -5.361488761196502513E-16, 0.000000000000000000 ) ) ;
#24694=CARTESIAN_POINT ( 'NONE',  ( -23.54713438637982748, 8.275374457817616047, 8.599999999999999645 ) ) ;
#24708=CARTESIAN_POINT ( 'NONE',  ( 24.97738509828242925, 18.93945643846228677, -1.491740999229418829 ) ) ;
#24711=CARTESIAN_POINT ( 'NONE',  ( -0.2059365608663963898, 0.000000000000000000, 4.148259000770580407 ) ) ;
#24725=CARTESIAN_POINT ( 'NONE',  ( -50.81000000000000227, -10.96999999999998643, 9.000000000000000000 ) ) ;
#24740=VERTEX_POINT ( 'NONE', #32169 ) ;
#24746=CARTESIAN_POINT ( 'NONE',  ( 107.3709349538546007, 17.48268201568652813, 3.822938398868985566 ) ) ;
#24747=( BOUNDED_CURVE ( )  B_SPLINE_CURVE ( 3, ( #15825, #18501, #23680, #23347 ),
 .UNSPECIFIED., .F., .F. ) 
 B_SPLINE_CURVE_WITH_KNOTS ( ( 4, 4 ),
 ( 5.654238798699126711, 7.043025911564681607 ),
 .UNSPECIFIED. ) 
 CURVE ( )  GEOMETRIC_REPRESENTATION_ITEM ( )  RATIONAL_B_SPLINE_CURVE ( ( 1.000000000000000000, 0.8456279454424002751, 0.8456279454424002751, 1.000000000000000000 ) ) 
 REPRESENTATION_ITEM ( '' )  );
#24753=VECTOR ( 'NONE', #13331, 1000.000000000000000 ) ;
#24754=DIRECTION ( 'NONE',  ( -0.000000000000000000, -0.000000000000000000, -1.000000000000000000 ) ) ;
#24762=ORIENTED_EDGE ( 'NONE', *, *, #13166, .T. ) ;
#24769=AXIS2_PLACEMENT_3D ( 'NONE', #378, #12574, #7739 ) ;
#24780=CARTESIAN_POINT ( 'NONE',  ( 24.29583315733998816, 18.19363606257105914, -1.049999999999941425 ) ) ;
#24789=CARTESIAN_POINT ( 'NONE',  ( 107.4385791398478744, 17.85938043952733878, 4.629213727441584325 ) ) ;
#24790=CARTESIAN_POINT ( 'NONE',  ( -83.35439080561378944, -0.0003384977252891612984, 1.500000000000000000 ) ) ;
#24810=DIRECTION ( 'NONE',  ( 0.8660254037844409281, -0.4999999999999960587, 0.000000000000000000 ) ) ;
#24816=AXIS2_PLACEMENT_3D ( 'NONE', #26793, #24289, #16419 ) ;
#24819=CARTESIAN_POINT ( 'NONE',  ( -56.37268996909460128, 0.008707415260527892262, -1.007559461241812837 ) ) ;
#24837=CARTESIAN_POINT ( 'NONE',  ( -50.81000000000000227, 4.402097243136370963, 5.049999999999999822 ) ) ;
#24843=B_SPLINE_CURVE_WITH_KNOTS ( 'NONE', 3,
 ( #11078, #18602, #3574, #31476, #3239, #11234, #16262, #21442, #13734, #16409, #745, #28494, #1224 ),
 .UNSPECIFIED., .F., .F.,
 ( 4, 3, 3, 3, 4 ),
 ( 0.000000000000000000, 0.0008924174835303601240, 0.001784834967102757585, 0.002677252450717581070, 0.003341508248895443296 ),
 .UNSPECIFIED. ) ;
#24853=ORIENTED_EDGE ( 'NONE', *, *, #19417, .F. ) ;
#24863=CARTESIAN_POINT ( 'NONE',  ( 17.41559371906256004, 18.02474698348863669, -1.491740999229419273 ) ) ;
#24878=CARTESIAN_POINT ( 'NONE',  ( -29.02642725384296440, 4.820254766716771222, 1.500000000000000000 ) ) ;
#24879=ADVANCED_FACE ( 'NONE', ( #2410 ), #30316, .F. ) ;
#24884=CARTESIAN_POINT ( 'NONE',  ( 107.6659035224683407, 16.31777890981063805, -1.490131869724928615 ) ) ;
#24888=ADVANCED_FACE ( 'NONE', ( #12582 ), #7035, .T. ) ;
#24889=CARTESIAN_POINT ( 'NONE',  ( -56.28351068137280322, -9.529120656610874963E-19, -1.066050254142973275 ) ) ;
#24894=CARTESIAN_POINT ( 'NONE',  ( -23.54713438637982748, 18.46223496596754288, 1.773004750130224627 ) ) ;
#24901=DIRECTION ( 'NONE',  ( -0.000000000000000000, -0.000000000000000000, -1.000000000000000000 ) ) ;
#24910=CARTESIAN_POINT ( 'NONE',  ( -21.76268656866881557, 18.40448632064758527, 1.500000000000000222 ) ) ;
#24919=ORIENTED_EDGE ( 'NONE', *, *, #7450, .F. ) ;
#24935=CARTESIAN_POINT ( 'NONE',  ( 25.25352962647643906, 18.67320858041093956, -1.050000000000058886 ) ) ;
#24948=CYLINDRICAL_SURFACE ( 'NONE', #11894, 10.97000000000000064 ) ;
#24958=CARTESIAN_POINT ( 'NONE',  ( 108.2917183403153274, 19.80256275031683799, 2.320955343329570653 ) ) ;
#24978=DIRECTION ( 'NONE',  ( 1.000000000000000000, 0.000000000000000000, 0.000000000000000000 ) ) ;
#24981=DIRECTION ( 'NONE',  ( 5.361488761196516318E-16, -1.000000000000000000, 0.000000000000000000 ) ) ;
#24985=DIRECTION ( 'NONE',  ( -0.000000000000000000, 0.000000000000000000, 1.000000000000000000 ) ) ;
#24994=ORIENTED_EDGE ( 'NONE', *, *, #11569, .T. ) ;
#25002=CARTESIAN_POINT ( 'NONE',  ( 8.924027012814292448, 0.4017312525919723987, -1.500000000000001776 ) ) ;
#25007=CARTESIAN_POINT ( 'NONE',  ( -50.81000000000000227, -10.96999999999998643, 8.549999999999998934 ) ) ;
#25014=SPHERICAL_SURFACE ( 'NONE', #6983, 0.4500000000000000111 ) ;
#25019=CARTESIAN_POINT ( 'NONE',  ( -56.30671226373046778, 0.08474811141987699525, -1.285380615603192611 ) ) ;
#25023=ORIENTED_EDGE ( 'NONE', *, *, #12949, .F. ) ;
#25027=DIRECTION ( 'NONE',  ( 1.000000000000000000, 0.000000000000000000, 0.000000000000000000 ) ) ;
#25028=DIRECTION ( 'NONE',  ( -0.000000000000000000, -0.000000000000000000, -1.000000000000000000 ) ) ;
#25036=CARTESIAN_POINT ( 'NONE',  ( -56.30880873598355407, 0.09981903777915809850, -1.306826643672643673 ) ) ;
#25041=DIRECTION ( 'NONE',  ( 0.4999999999999978351, 0.8660254037844398178, 0.000000000000000000 ) ) ;
#25055=CARTESIAN_POINT ( 'NONE',  ( 107.8972572759871866, 20.45595522325154647, -2.263373122311984176 ) ) ;
#25060=CARTESIAN_POINT ( 'NONE',  ( -19.37241134977605128, 17.09829073722516668, 1.500000000000000000 ) ) ;
#25072=CARTESIAN_POINT ( 'NONE',  ( -39.83999999999998920, -10.96999999999998643, 1.500000000000000000 ) ) ;
#25077=VECTOR ( 'NONE', #23309, 1000.000000000000114 ) ;
#25078=CARTESIAN_POINT ( 'NONE',  ( 107.6765350359755615, 19.22395582067604991, -4.843906566570527872 ) ) ;
#25079=EDGE_LOOP ( 'NONE', ( #12902, #7223, #27698, #12491 ) ) ;
#25085=EDGE_CURVE ( 'NONE', #26215, #27222, #1783, .T. ) ;
#25090=CARTESIAN_POINT ( 'NONE',  ( 22.43659417803347722, 17.13630711828444575, -1.500000000000000000 ) ) ;
#25091=CARTESIAN_POINT ( 'NONE',  ( 22.41270750065876172, 17.13964222952529681, 1.050000000000000044 ) ) ;
#25092=CARTESIAN_POINT ( 'NONE',  ( 8.870145747188287189, 0.000000000000000000, 1.000000000000000000 ) ) ;
#25095=VERTEX_POINT ( 'NONE', #17939 ) ;
#25099=LINE ( 'NONE', #2216, #2791 ) ;
#25101=CARTESIAN_POINT ( 'NONE',  ( 107.8757006204448459, 20.33592830970491150, -2.519365258488940107 ) ) ;
#25102=EDGE_CURVE ( 'NONE', #4552, #32925, #534, .T. ) ;
#25105=VECTOR ( 'NONE', #15565, 1000.000000000000000 ) ;
#25120=CIRCLE ( 'NONE', #10713, 9.713116299512234875 ) ;
#25121=CARTESIAN_POINT ( 'NONE',  ( -40.71733131760397129, -12.43974741078717372, 5.871858320049880398 ) ) ;
#25124=CARTESIAN_POINT ( 'NONE',  ( 107.1772993348646281, 16.40207914262226296, 1.508259000770581615 ) ) ;
#25135=ORIENTED_EDGE ( 'NONE', *, *, #9159, .T. ) ;
#25139=AXIS2_PLACEMENT_3D ( 'NONE', #20152, #4111, #12760 ) ;
#25146=EDGE_CURVE ( 'NONE', #14230, #31255, #22595, .T. ) ;
#25147=PLANE ( 'NONE',  #25139 ) ;
#25159=FACE_OUTER_BOUND ( 'NONE', #3745, .T. ) ;
#25162=( LENGTH_UNIT ( ) NAMED_UNIT ( * ) SI_UNIT ( .MILLI., .METRE. ) );
#25165=ORIENTED_EDGE ( 'NONE', *, *, #18345, .T. ) ;
#25172=CIRCLE ( 'NONE', #15021, 0.5000000000000000000 ) ;
#25225=VERTEX_POINT ( 'NONE', #21593 ) ;
#25237=AXIS2_PLACEMENT_3D ( 'NONE', #30812, #10889, #30956 ) ;
#25245=CARTESIAN_POINT ( 'NONE',  ( 21.16269079926919972, 16.85597784695825752, 1.500000000000000222 ) ) ;
#25260=AXIS2_PLACEMENT_3D ( 'NONE', #23914, #13862, #11883 ) ;
#25263=DIRECTION ( 'NONE',  ( -1.000000000000000000, 0.000000000000000000, 0.000000000000000000 ) ) ;
#25264=EDGE_LOOP ( 'NONE', ( #3856, #19974 ) ) ;
#25265=CARTESIAN_POINT ( 'NONE',  ( 108.0492715581498118, 18.45252340228810795, -4.624728054639414943 ) ) ;
#25267=CARTESIAN_POINT ( 'NONE',  ( -17.73806761126738607, 14.75113368127120772, 1.863483178821739417 ) ) ;
#25275=CARTESIAN_POINT ( 'NONE',  ( 107.6996442589674103, 19.35565155597529596, 4.629213727441584325 ) ) ;
#25277=CARTESIAN_POINT ( 'NONE',  ( 25.73836023340068380, 18.89938647776750003, -1.050000000000000044 ) ) ;
#25285=EDGE_LOOP ( 'NONE', ( #16489, #9357, #17435, #6724 ) ) ;
#25290=DIRECTION ( 'NONE',  ( -0.4999999999999981126, -0.8660254037844395958, 0.000000000000000000 ) ) ;
#25293=PLANE ( 'NONE',  #23625 ) ;
#25298=EDGE_CURVE ( 'NONE', #12740, #32977, #2315, .T. ) ;
#25302=VERTEX_POINT ( 'NONE', #16243 ) ;
#25303=AXIS2_PLACEMENT_3D ( 'NONE', #29376, #19687, #4304 ) ;
#25304=TOROIDAL_SURFACE ( 'NONE', #28510, 9.269952810656748809, 0.4500000000000000111 ) ;
#25309=VERTEX_POINT ( 'NONE', #1373 ) ;
#25310=CARTESIAN_POINT ( 'NONE',  ( 108.0120102303167613, 18.24503762629559489, -4.459921598894291961 ) ) ;
#25315=DIRECTION ( 'NONE',  ( -0.000000000000000000, -0.000000000000000000, -1.000000000000000000 ) ) ;
#25322=EDGE_LOOP ( 'NONE', ( #17603, #1759, #3512, #8369, #21124, #24919, #2645, #26688, #26022, #20603 ) ) ;
#25329=AXIS2_PLACEMENT_3D ( 'NONE', #5610, #10596, #20800 ) ;
#25350=VECTOR ( 'NONE', #1910, 1000.000000000000000 ) ;
#25361=CARTESIAN_POINT ( 'NONE',  ( 24.89403984153603488, 18.93045399291958475, -1.497243178805399921 ) ) ;
#25365=DIRECTION ( 'NONE',  ( 0.4999999999999981126, 0.8660254037844395958, -0.000000000000000000 ) ) ;
#25371=CARTESIAN_POINT ( 'NONE',  ( 56.97280603064898941, -277.2763395528616002, -1.491740999229417941 ) ) ;
#25372=DIRECTION ( 'NONE',  ( -1.000000000000000000, 0.000000000000000000, 0.000000000000000000 ) ) ;
#25375=CARTESIAN_POINT ( 'NONE',  ( -56.60872035989488893, 0.09018158751379945492, -1.329259193462423827 ) ) ;
#25378=EDGE_CURVE ( 'NONE', #13143, #6245, #30101, .T. ) ;
#25383=CARTESIAN_POINT ( 'NONE',  ( 108.0255836577191246, 18.32061982589471327, 5.125284668028994517 ) ) ;
#25385=CARTESIAN_POINT ( 'NONE',  ( -23.54713438637982748, 8.763231220430828472, 1.786631099142472534 ) ) ;
#25405=CARTESIAN_POINT ( 'NONE',  ( 107.9842833020718444, 18.09064314930442308, -4.129529848691289473 ) ) ;
#25408=ORIENTED_EDGE ( 'NONE', *, *, #28300, .T. ) ;
#25411=ADVANCED_FACE ( 'NONE', ( #19576 ), #17272, .F. ) ;
#25427=ORIENTED_EDGE ( 'NONE', *, *, #27110, .F. ) ;
#25440=CARTESIAN_POINT ( 'NONE',  ( 15.28872660057388799, 20.76088595412472060, 4.629213727441584325 ) ) ;
#25467=ORIENTED_EDGE ( 'NONE', *, *, #30694, .F. ) ;
#25471=ORIENTED_EDGE ( 'NONE', *, *, #25708, .F. ) ;
#25472=DIRECTION ( 'NONE',  ( -0.4999999999999978906, -0.8660254037844399289, -0.000000000000000000 ) ) ;
#25483=CARTESIAN_POINT ( 'NONE',  ( -56.27770248097862549, 0.4996615022747108448, -1.050000000000000044 ) ) ;
#25523=CARTESIAN_POINT ( 'NONE',  ( -32.08053788975120568, -0.0003384977252905707612, 1.500000000000000000 ) ) ;
#25529=CARTESIAN_POINT ( 'NONE',  ( -56.33942387371224214, 0.003472127128727200539, -1.004056851832535235 ) ) ;
#25530=CARTESIAN_POINT ( 'NONE',  ( -56.27770248097862549, 0.4996615022747108448, -1.500000000000000000 ) ) ;
#25536=CARTESIAN_POINT ( 'NONE',  ( 108.0552541750404174, 18.48583697376223967, 4.648293729490854176 ) ) ;
#25545=EDGE_CURVE ( 'NONE', #14768, #9701, #4461, .T. ) ;
#25548=LINE ( 'NONE', #2655, #2243 ) ;
#25569=ADVANCED_FACE ( 'NONE', ( #15533 ), #21071, .T. ) ;
#25573=CARTESIAN_POINT ( 'NONE',  ( 8.886976913778033449, 2.271465516421269619E-16, 1.168311665897490581 ) ) ;
#25581=CARTESIAN_POINT ( 'NONE',  ( 108.0672442999933196, 18.55260272057762094, -4.631666742912559975 ) ) ;
#25583=CARTESIAN_POINT ( 'NONE',  ( -16.91631469035494462, 11.69557288659533434, 1.940592563500735501 ) ) ;
#25613=CARTESIAN_POINT ( 'NONE',  ( -40.16771308880407076, -10.96999999999998643, 5.949999999999999289 ) ) ;
#25627=EDGE_CURVE ( 'NONE', #16073, #4298, #10371, .T. ) ;
#25635=ORIENTED_EDGE ( 'NONE', *, *, #18364, .F. ) ;
#25644=CARTESIAN_POINT ( 'NONE',  ( 109.6329156864505165, 19.01855260168436246, -4.612695725900421984 ) ) ;
#25654=EDGE_LOOP ( 'NONE', ( #23902, #24527, #32945, #23056, #18445 ) ) ;
#25671=ORIENTED_EDGE ( 'NONE', *, *, #22087, .F. ) ;
#25674=EDGE_LOOP ( 'NONE', ( #27027, #288, #27065 ) ) ;
#25675=CARTESIAN_POINT ( 'NONE',  ( 9.302055952193859056, 0.2457637073201327793, 1.049999999999999822 ) ) ;
#25694=CARTESIAN_POINT ( 'NONE',  ( -56.65769528877406458, 0.1730602557903761496, -1.037707669418532319 ) ) ;
#25699=ORIENTED_EDGE ( 'NONE', *, *, #11089, .T. ) ;
#25702=CARTESIAN_POINT ( 'NONE',  ( 107.4616540840862768, 17.99089616900343813, 4.860603037907947233 ) ) ;
#25708=EDGE_CURVE ( 'NONE', #29447, #11755, #13823, .T. ) ;
#25711=ORIENTED_EDGE ( 'NONE', *, *, #16403, .F. ) ;
#25716=ADVANCED_FACE ( 'NONE', ( #28734 ), #16399, .F. ) ;
#25730=CARTESIAN_POINT ( 'NONE',  ( -40.49265397688009216, -13.13403825401228708, 5.499999999999999112 ) ) ;
#25738=CARTESIAN_POINT ( 'NONE',  ( 16.36487458112951643, 19.37645981759113312, -4.612695725900422872 ) ) ;
#25760=CARTESIAN_POINT ( 'NONE',  ( 108.0191616597610391, 18.28485960726052539, -4.516253988675255293 ) ) ;
#25761=VECTOR ( 'NONE', #30742, 1000.000000000000227 ) ;
#25763=CARTESIAN_POINT ( 'NONE',  ( -18.18687069758686903, 6.948720673121208335, 2.065371546005595693 ) ) ;
#25777=FACE_OUTER_BOUND ( 'NONE', #4134, .T. ) ;
#25778=CARTESIAN_POINT ( 'NONE',  ( 25.73747082621204640, 18.89898602765596536, 1.499999999998589573 ) ) ;
#25785=B_SPLINE_CURVE_WITH_KNOTS ( 'NONE', 3,
 ( #27429, #19913, #14536, #24746, #1870, #32451, #12045 ),
 .UNSPECIFIED., .F., .F.,
 ( 4, 3, 4 ),
 ( 5.449946885873038238E-17, 0.002561824599199770836, 0.003454325189396755934 ),
 .UNSPECIFIED. ) ;
#25788=CARTESIAN_POINT ( 'NONE',  ( -28.91036633256500465, 15.51073349983545313, 1.844682940529381199 ) ) ;
#25791=EDGE_CURVE ( 'NONE', #27055, #7787, #10469, .T. ) ;
#25796=DIRECTION ( 'NONE',  ( 0.000000000000000000, -0.000000000000000000, 1.000000000000000000 ) ) ;
#25797=VERTEX_POINT ( 'NONE', #24708 ) ;
#25810=CARTESIAN_POINT ( 'NONE',  ( -40.85893555729982296, -14.04586516063045210, 5.414538096233425968 ) ) ;
#25811=VERTEX_POINT ( 'NONE', #9646 ) ;
#25818=VECTOR ( 'NONE', #9059, 1000.000000000000000 ) ;
#25821=VECTOR ( 'NONE', #3072, 1000.000000000000227 ) ;
#25825=EDGE_LOOP ( 'NONE', ( #18791, #15772, #8322, #5983 ) ) ;
#25839=CIRCLE ( 'NONE', #20496, 0.4500000000000007327 ) ;
#25841=( BOUNDED_CURVE ( )  B_SPLINE_CURVE ( 3, ( #4396, #2210, #20112, #25092 ),
 .UNSPECIFIED., .F., .F. ) 
 B_SPLINE_CURVE_WITH_KNOTS ( ( 4, 4 ),
 ( 0.6009777071450068675, 1.570796326794896558 ),
 .UNSPECIFIED. ) 
 CURVE ( )  GEOMETRIC_REPRESENTATION_ITEM ( )  RATIONAL_B_SPLINE_CURVE ( ( 1.000000000000000000, 0.9231448173254028777, 0.9231448173254028777, 1.000000000000000000 ) ) 
 REPRESENTATION_ITEM ( '' )  );
#25843=CIRCLE ( 'NONE', #19446, 297.9387600756452343 ) ;
#25845=CARTESIAN_POINT ( 'NONE',  ( 13.44369214246638577, 21.88234542448674702, -1.272551993140566662 ) ) ;
#25853=CARTESIAN_POINT ( 'NONE',  ( 107.1769020805352142, 16.40214705320008903, -1.491740999229418829 ) ) ;
#25861=ORIENTED_EDGE ( 'NONE', *, *, #4723, .T. ) ;
#25878=ADVANCED_FACE ( 'NONE', ( #28616, #8374 ), #23757, .T. ) ;
#25905=CARTESIAN_POINT ( 'NONE',  ( -31.91713028529358098, -0.0003384977252905707612, 2.028141679950118625 ) ) ;
#25910=EDGE_LOOP ( 'NONE', ( #16570, #13059, #12422, #2567, #12869 ) ) ;
#25915=VERTEX_POINT ( 'NONE', #1185 ) ;
#25930=DIRECTION ( 'NONE',  ( 0.4999999999999967804, 0.8660254037844404840, 1.001543065824777131E-14 ) ) ;
#25935=CARTESIAN_POINT ( 'NONE',  ( -22.63686929475232645, 4.062439337332850897, 2.144399907006354855 ) ) ;
#25946=CARTESIAN_POINT ( 'NONE',  ( 8.930755659325141593, 0.5000000000000008882, 1.500000000000000000 ) ) ;
#25952=ORIENTED_EDGE ( 'NONE', *, *, #14642, .F. ) ;
#25953=ADVANCED_FACE ( 'NONE', ( #6342, #19566 ), #14704, .T. ) ;
#25956=CARTESIAN_POINT ( 'NONE',  ( -26.59846049200615781, 17.65632644948022190, 1.792369863739132985 ) ) ;
#25960=CARTESIAN_POINT ( 'NONE',  ( 109.6329156864505165, 19.01855260168436246, 4.629213727441584325 ) ) ;
#25962=ORIENTED_EDGE ( 'NONE', *, *, #16311, .T. ) ;
#25990=CARTESIAN_POINT ( 'NONE',  ( 0.2409471776115469921, 0.000000000000000000, -5.396302277755718357 ) ) ;
#25995=DIRECTION ( 'NONE',  ( -0.000000000000000000, -0.000000000000000000, -1.000000000000000000 ) ) ;
#26018=EDGE_CURVE ( 'NONE', #14768, #14212, #21889, .T. ) ;
#26020=DIRECTION ( 'NONE',  ( -0.000000000000000000, -0.000000000000000000, -1.000000000000000000 ) ) ;
#26022=ORIENTED_EDGE ( 'NONE', *, *, #14539, .T. ) ;
#26023=CARTESIAN_POINT ( 'NONE',  ( 9.910042481050302499, 1.133699783719172016, 1.049999999999999600 ) ) ;
#26030=DIRECTION ( 'NONE',  ( -0.8251117619019970872, 0.5649695393302031077, 0.000000000000000000 ) ) ;
#26043=CARTESIAN_POINT ( 'NONE',  ( 15.28872660057388799, 20.76088595412472060, -4.612695725900422872 ) ) ;
#26061=CARTESIAN_POINT ( 'NONE',  ( 108.3190036904951796, 19.95449834640353259, -1.980516148027076984 ) ) ;
#26064=CARTESIAN_POINT ( 'NONE',  ( 108.1382411484322290, 18.94794118670416694, 4.145841387855481841 ) ) ;
#26078=EDGE_CURVE ( 'NONE', #13143, #9106, #11691, .T. ) ;
#26083=CARTESIAN_POINT ( 'NONE',  ( 107.5147077154356623, 18.30459826903478771, -4.398253369385427547 ) ) ;
#26085=CYLINDRICAL_SURFACE ( 'NONE', #11902, 5.100000000000000533 ) ;
#26096=CARTESIAN_POINT ( 'NONE',  ( 11.04311965146451158, 15.00000000000000178, 1.508259000770581615 ) ) ;
#26097=CARTESIAN_POINT ( 'NONE',  ( 13.86820177083861871, 7.731989999893393417, 1.050000000000000044 ) ) ;
#26108=CARTESIAN_POINT ( 'NONE',  ( -20.31068713123109859, 5.033963319883215881, 1.500000000000000000 ) ) ;
#26119=CARTESIAN_POINT ( 'NONE',  ( 107.9618353151786181, 20.81780380167319677, 0.000000000000000000 ) ) ;
#26123=ORIENTED_EDGE ( 'NONE', *, *, #32089, .F. ) ;
#26133=DIRECTION ( 'NONE',  ( -0.000000000000000000, -0.000000000000000000, -1.000000000000000000 ) ) ;
#26135=ORIENTED_EDGE ( 'NONE', *, *, #21114, .T. ) ;
#26157=LINE ( 'NONE', #28520, #12488 ) ;
#26177=CARTESIAN_POINT ( 'NONE',  ( 16.42946203030704311, 11.64644840300599959, 1.049999999999999822 ) ) ;
#26194=CARTESIAN_POINT ( 'NONE',  ( -25.21220230200964352, 4.362210445733495590, 1.500000000000934142 ) ) ;
#26197=EDGE_CURVE ( 'NONE', #18045, #21273, #19422, .T. ) ;
#26200=CARTESIAN_POINT ( 'NONE',  ( 16.36487458112951643, 19.37645981759113312, -4.612695725900422872 ) ) ;
#26209=CIRCLE ( 'NONE', #11254, 297.9387600756452912 ) ;
#26212=CARTESIAN_POINT ( 'NONE',  ( 9.220089837531610044, 0.1261361023189421227, 1.391323255828233130 ) ) ;
#26215=VERTEX_POINT ( 'NONE', #3658 ) ;
#26220=CIRCLE ( 'NONE', #32623, 3.250000000000002665 ) ;
#26221=CARTESIAN_POINT ( 'NONE',  ( 9.292339479667081292, 0.2315767011690351151, -1.048511744989948813 ) ) ;
#26229=CARTESIAN_POINT ( 'NONE',  ( 56.97280603064898941, -277.2763395528616002, 4.629213727441584325 ) ) ;
#26231=CONICAL_SURFACE ( 'NONE', #12868, 2.099999999999997868, 1.029744258676653423 ) ;
#26232=EDGE_CURVE ( 'NONE', #14650, #6245, #31414, .T. ) ;
#26255=CARTESIAN_POINT ( 'NONE',  ( 9.331062908042635939, 15.00000000000000178, -4.612695725900422872 ) ) ;
#26265=CARTESIAN_POINT ( 'NONE',  ( 11.66870695089360588, 3.948484734291052067, 1.050000000000000044 ) ) ;
#26271=ORIENTED_EDGE ( 'NONE', *, *, #32581, .F. ) ;
#26277=CARTESIAN_POINT ( 'NONE',  ( -17.76073374637450542, 7.575402792874719182, 2.048453119712636550 ) ) ;
#26283=CIRCLE ( 'NONE', #11855, 0.4499999999999999001 ) ;
#26294=CARTESIAN_POINT ( 'NONE',  ( 108.0732140668137617, 18.58584473779162138, -4.631593095966008100 ) ) ;
#26322=LINE ( 'NONE', #23796, #3288 ) ;
#26374=AXIS2_PLACEMENT_3D ( 'NONE', #26229, #31268, #18690 ) ;
#26380=CARTESIAN_POINT ( 'NONE',  ( 108.1104766427000925, 18.79333746343691658, 4.476124295753212579 ) ) ;
#26394=ORIENTED_EDGE ( 'NONE', *, *, #15714, .T. ) ;
#26404=CARTESIAN_POINT ( 'NONE',  ( 25.93644697397389720, 19.04148194274331729, -1.255264836812425067 ) ) ;
#26407=EDGE_LOOP ( 'NONE', ( #15375, #5739, #21633 ) ) ;
#26409=CARTESIAN_POINT ( 'NONE',  ( 108.2737963169669655, 19.70276585262076452, 2.534196689747376663 ) ) ;
#26420=CARTESIAN_POINT ( 'NONE',  ( -58.12302020695992866, -3.824990096116924310, 5.760101628985031752 ) ) ;
#26437=DIRECTION ( 'NONE',  ( -8.326672684688674053E-17, -0.3746065934159164001, 0.9271838545667857590 ) ) ;
#26442=CARTESIAN_POINT ( 'NONE',  ( 12.71851269413118857, 6.640480776649662076, -1.500000000000000222 ) ) ;
#26445=CARTESIAN_POINT ( 'NONE',  ( 15.58693300141982441, 10.49296960241998100, 1.050000000000000044 ) ) ;
#26452=DIRECTION ( 'NONE',  ( 0.2951703194034056010, -0.3797261271633441404, 0.8767454310646958238 ) ) ;
#26453=CARTESIAN_POINT ( 'NONE',  ( -21.68109753780424143, 3.720325412122139408, 1.500000000000000000 ) ) ;
#26454=CARTESIAN_POINT ( 'NONE',  ( 110.0816933595962439, 17.77332459904788209, 5.412820279296879811 ) ) ;
#26457=CARTESIAN_POINT ( 'NONE',  ( 9.302055952193859056, 0.2457637073201327793, 1.049999999999999822 ) ) ;
#26460=CARTESIAN_POINT ( 'NONE',  ( 108.3696618535068126, 20.23658298680886958, 1.395260099363828665 ) ) ;
#26465=DIRECTION ( 'NONE',  ( -0.000000000000000000, 0.000000000000000000, 1.000000000000000000 ) ) ;
#26472=ADVANCED_FACE ( 'NONE', ( #15324 ), #15151, .T. ) ;
#26475=LINE ( 'NONE', #31655, #21902 ) ;
#26477=CARTESIAN_POINT ( 'NONE',  ( 19.01933586186248348, 14.56926017555086972, -1.500000000000000000 ) ) ;
#26489=CARTESIAN_POINT ( 'NONE',  ( -55.91000000000000369, -10.96999999999998643, 1.499999999999999556 ) ) ;
#26494=CARTESIAN_POINT ( 'NONE',  ( 15.55254023221931448, 20.42149909151575926, -5.396302277755718357 ) ) ;
#26496=PLANE ( 'NONE',  #20375 ) ;
#26502=CARTESIAN_POINT ( 'NONE',  ( 8.901201215455881055, 15.00000000000000000, 5.412820279296879811 ) ) ;
#26507=ORIENTED_EDGE ( 'NONE', *, *, #27217, .T. ) ;
#26513=EDGE_CURVE ( 'NONE', #11008, #13391, #13150, .T. ) ;
#26516=CARTESIAN_POINT ( 'NONE',  ( -50.81000000000000227, -10.96999999999998643, 5.949999999999999289 ) ) ;
#26526=CARTESIAN_POINT ( 'NONE',  ( -50.81000000000000227, -10.96999999999998643, 2.028141679950118625 ) ) ;
#26531=CARTESIAN_POINT ( 'NONE',  ( 108.1960732670209211, 19.26997324246898557, 4.630839363390588659 ) ) ;
#26533=ORIENTED_EDGE ( 'NONE', *, *, #774, .T. ) ;
#26535=EDGE_LOOP ( 'NONE', ( #29924, #2694, #18987, #21144, #32882 ) ) ;
#26562=ORIENTED_EDGE ( 'NONE', *, *, #32087, .F. ) ;
#26575=DIRECTION ( 'NONE',  ( 0.07581065956227768521, 0.4221436659004723091, -0.9033534575330096628 ) ) ;
#26591=ORIENTED_EDGE ( 'NONE', *, *, #1172, .T. ) ;
#26594=LINE ( 'NONE', #3696, #11477 ) ;
#26600=CARTESIAN_POINT ( 'NONE',  ( 9.288430967222316426, 0.2258737065014515821, 1.045938632499123999 ) ) ;
#26603=EDGE_CURVE ( 'NONE', #6904, #32600, #7899, .T. ) ;
#26607=DIRECTION ( 'NONE',  ( -0.4999999999999977240, -0.8660254037844398178, 0.000000000000000000 ) ) ;
#26619=CARTESIAN_POINT ( 'NONE',  ( 13.87075382900347975, 7.736340727340449419, -1.050000000000000044 ) ) ;
#26640=FACE_OUTER_BOUND ( 'NONE', #32192, .T. ) ;
#26644=CARTESIAN_POINT ( 'NONE',  ( -1.082681991931091270, 0.000000000000000000, 4.629213727441584325 ) ) ;
#26649=CARTESIAN_POINT ( 'NONE',  ( -56.71071518287084245, 0.7496615022747109558, 1.500000000000000000 ) ) ;
#26653=DIRECTION ( 'NONE',  ( 0.000000000000000000, -3.854941057726238689E-15, 1.000000000000000000 ) ) ;
#26655=DIRECTION ( 'NONE',  ( -0.000000000000000000, -0.000000000000000000, -1.000000000000000000 ) ) ;
#26661=CARTESIAN_POINT ( 'NONE',  ( 9.149098621172164769, 18.06225657836807841, -4.612695725900421984 ) ) ;
#26687=FACE_OUTER_BOUND ( 'NONE', #21195, .T. ) ;
#26688=ORIENTED_EDGE ( 'NONE', *, *, #244, .T. ) ;
#26690=CARTESIAN_POINT ( 'NONE',  ( 107.4454642110974447, 16.41225513980339912, 1.495340255777613869 ) ) ;
#26696=AXIS2_PLACEMENT_3D ( 'NONE', #10739, #31172, #15915 ) ;
#26697=ADVANCED_FACE ( 'NONE', ( #14590 ), #4728, .T. ) ;
#26698=DIRECTION ( 'NONE',  ( -0.000000000000000000, 0.000000000000000000, 1.000000000000000000 ) ) ;
#26708=ADVANCED_FACE ( 'NONE', ( #9401 ), #17307, .T. ) ;
#26712=CARTESIAN_POINT ( 'NONE',  ( -58.11719619654970614, -3.766776810957159771, 5.550376981476754068 ) ) ;
#26713=AXIS2_PLACEMENT_3D ( 'NONE', #17531, #9862, #33091 ) ;
#26717=DIRECTION ( 'NONE',  ( -1.000000000000000000, 0.000000000000000000, 0.000000000000000000 ) ) ;
#26719=FACE_OUTER_BOUND ( 'NONE', #3164, .T. ) ;
#26723=ORIENTED_EDGE ( 'NONE', *, *, #1409, .F. ) ;
#26738=EDGE_LOOP ( 'NONE', ( #1894, #6009, #11104, #24376 ) ) ;
#26746=AXIS2_PLACEMENT_3D ( 'NONE', #20304, #30857, #2089 ) ;
#26753=CARTESIAN_POINT ( 'NONE',  ( 17.32050807568873552, 10.00000000000002309, 0.000000000000000000 ) ) ;
#26755=VECTOR ( 'NONE', #20639, 1000.000000000000000 ) ;
#26765=CARTESIAN_POINT ( 'NONE',  ( 107.6996442589673819, 19.35565155597529596, -4.612695725900422872 ) ) ;
#26768=AXIS2_PLACEMENT_3D ( 'NONE', #22478, #14779, #6921 ) ;
#26778=AXIS2_PLACEMENT_3D ( 'NONE', #27998, #405, #5415 ) ;
#26783=CARTESIAN_POINT ( 'NONE',  ( 15.90893862193319386, 10.93205754319533263, -1.050000000000000044 ) ) ;
#26793=CARTESIAN_POINT ( 'NONE',  ( -4.058229847495222268E-16, -1.825746869171931852, 4.518882073553349699 ) ) ;
#26807=CARTESIAN_POINT ( 'NONE',  ( 110.0816933595962439, 17.77332459904788209, -5.396302277755718357 ) ) ;
#26808=ORIENTED_EDGE ( 'NONE', *, *, #13686, .F. ) ;
#26810=ORIENTED_EDGE ( 'NONE', *, *, #5540, .T. ) ;
#26821=CARTESIAN_POINT ( 'NONE',  ( 9.331062908042598636, 15.00000000000002132, 4.629213727441584325 ) ) ;
#26829=ADVANCED_FACE ( 'NONE', ( #5224 ), #25293, .T. ) ;
#26837=CARTESIAN_POINT ( 'NONE',  ( 47.62814091865205768, 23.65599663307499156, 4.629213727441585213 ) ) ;
#26872=CARTESIAN_POINT ( 'NONE',  ( 8.914564461877747092, -1.485421493711411364E-07, 1.044418714689500538 ) ) ;
#26875=LINE ( 'NONE', #21691, #31146 ) ;
#26884=CARTESIAN_POINT ( 'NONE',  ( 26.04364899819628576, 19.05268753777025026, 1.166395880049359457 ) ) ;
#26885=CARTESIAN_POINT ( 'NONE',  ( -56.27770248097862549, -0.0003384977252891612984, 0.000000000000000000 ) ) ;
#26887=LINE ( 'NONE', #21700, #28975 ) ;
#26904=CARTESIAN_POINT ( 'NONE',  ( -58.35662399578649939, -4.056783446705964025, 5.700525030782698011 ) ) ;
#26921=ORIENTED_EDGE ( 'NONE', *, *, #14666, .F. ) ;
#26922=AXIS2_PLACEMENT_3D ( 'NONE', #18156, #18343, #28361 ) ;
#26929=CARTESIAN_POINT ( 'NONE',  ( 12.84684103081497142, 21.67296960808364403, 1.472725903438507844 ) ) ;
#26935=CARTESIAN_POINT ( 'NONE',  ( -16.60354855507976524, 13.22775097665246946, 1.500000000000000000 ) ) ;
#26936=DIRECTION ( 'NONE',  ( -0.000000000000000000, 0.000000000000000000, 1.000000000000000000 ) ) ;
#26962=CARTESIAN_POINT ( 'NONE',  ( 15.60185111400613600, 10.48692277187139155, -1.050000000000000044 ) ) ;
#26969=DIRECTION ( 'NONE',  ( 0.000000000000000000, 0.000000000000000000, -1.000000000000000000 ) ) ;
#26983=CARTESIAN_POINT ( 'NONE',  ( 108.2036592059121887, 19.31221474348532396, 3.367636781498203558 ) ) ;
#26990=ORIENTED_EDGE ( 'NONE', *, *, #14539, .F. ) ;
#26991=ORIENTED_EDGE ( 'NONE', *, *, #24185, .F. ) ;
#26993=ADVANCED_FACE ( 'NONE', ( #28939 ), #20729, .F. ) ;
#26994=ORIENTED_EDGE ( 'NONE', *, *, #7935, .T. ) ;
#26998=ORIENTED_EDGE ( 'NONE', *, *, #229, .T. ) ;
#27027=ORIENTED_EDGE ( 'NONE', *, *, #18920, .F. ) ;
#27032=ORIENTED_EDGE ( 'NONE', *, *, #15867, .T. ) ;
#27034=CARTESIAN_POINT ( 'NONE',  ( 107.1772993348646281, 16.40207914262226296, 1.508259000770581615 ) ) ;
#27035=LINE ( 'NONE', #6155, #2304 ) ;
#27037=EDGE_LOOP ( 'NONE', ( #13583, #13270, #15545 ) ) ;
#27044=PLANE ( 'NONE',  #12377 ) ;
#27055=VERTEX_POINT ( 'NONE', #20084 ) ;
#27057=CARTESIAN_POINT ( 'NONE',  ( -58.79722610518447823, -4.531914678867814850, 5.561913525286415805 ) ) ;
#27065=ORIENTED_EDGE ( 'NONE', *, *, #14959, .T. ) ;
#27080=( BOUNDED_SURFACE ( )  B_SPLINE_SURFACE ( 3, 3, ( 
 ( #28771, #23765, #18435, #25960 ),
 ( #3214, #28627, #6049, #23423 ),
 ( #31454, #10904, #21109, #26454 ),
 ( #878, #5862, #8532, #13558 ) ),
 .UNSPECIFIED., .F., .F., .F. ) 
 B_SPLINE_SURFACE_WITH_KNOTS ( ( 4, 4 ),
 ( 4, 4 ),
 ( 0.000000000000000000, 1.000000000000000000 ),
 ( 0.000000000000000000, 1.000000000000000000 ),
 .UNSPECIFIED. ) 
 GEOMETRIC_REPRESENTATION_ITEM ( )  RATIONAL_B_SPLINE_SURFACE ( (
 ( 1.000000000000000000, 0.9917560313531952332, 0.9917560313531952332, 1.000000000000000000),
 ( 0.6539698177806696489, 0.6485785111069292119, 0.6485785111069292119, 0.6539698177806696489),
 ( 0.6539698177806696489, 0.6485785111069292119, 0.6485785111069292119, 0.6539698177806696489),
 ( 1.000000000000000000, 0.9917560313531952332, 0.9917560313531952332, 1.000000000000000000) ) ) 
 REPRESENTATION_ITEM ( '' )  SURFACE ( )  );
#27090=EDGE_LOOP ( 'NONE', ( #22132, #24994, #3111, #27596, #6714, #9359, #32133, #15042, #18283, #22402 ) ) ;
#27103=VERTEX_POINT ( 'NONE', #6000 ) ;
#27110=EDGE_CURVE ( 'NONE', #16163, #1782, #8171, .T. ) ;
#27132=CARTESIAN_POINT ( 'NONE',  ( 108.3798353887428192, 20.29323324528803596, 1.274429984091367318 ) ) ;
#27134=ORIENTED_EDGE ( 'NONE', *, *, #5321, .F. ) ;
#27154=CARTESIAN_POINT ( 'NONE',  ( 110.2274383572228942, 17.36892446252421962, 4.629213727441584325 ) ) ;
#27161=CARTESIAN_POINT ( 'NONE',  ( 5.865515302491369098, 15.00000000000000000, -1.500000000000000000 ) ) ;
#27166=DIRECTION ( 'NONE',  ( -0.2951703194034056565, 0.3797261271633441959, -0.8767454310646958238 ) ) ;
#27175=CARTESIAN_POINT ( 'NONE',  ( -56.77769102277633095, 0.5030464795276025081, -1.050000000000000044 ) ) ;
#27185=CARTESIAN_POINT ( 'NONE',  ( 8.870145747188287189, 0.000000000000000000, 1.000000000000000000 ) ) ;
#27189=ORIENTED_EDGE ( 'NONE', *, *, #26603, .F. ) ;
#27192=CARTESIAN_POINT ( 'NONE',  ( -31.52072750637464083, 0.5000000000000022204, 1.500000000000000000 ) ) ;
#27193=CARTESIAN_POINT ( 'NONE',  ( 17.41559371906258136, 18.02474698348859405, 1.508259000770581615 ) ) ;
#27195=VECTOR ( 'NONE', #27737, 1000.000000000000000 ) ;
#27217=EDGE_CURVE ( 'NONE', #14650, #9106, #22059, .T. ) ;
#27220=CIRCLE ( 'NONE', #12801, 0.4499999999999999001 ) ;
#27222=VERTEX_POINT ( 'NONE', #19538 ) ;
#27245=CARTESIAN_POINT ( 'NONE',  ( -24.48050464856572717, 18.90773822806010429, 1.500000000000000000 ) ) ;
#27248=AXIS2_PLACEMENT_3D ( 'NONE', #4063, #6373, #4561 ) ;
#27262=PLANE ( 'NONE',  #8669 ) ;
#27275=CARTESIAN_POINT ( 'NONE',  ( 24.08779030308693692, 18.59272488193695949, -1.500000000000000000 ) ) ;
#27283=CARTESIAN_POINT ( 'NONE',  ( 2.382865613620175349, 0.000000000000000000, 1.000000000000000222 ) ) ;
#27303=FACE_OUTER_BOUND ( 'NONE', #46, .T. ) ;
#27331=DIRECTION ( 'NONE',  ( 0.4999999999999978351, 0.8660254037844398178, 0.000000000000000000 ) ) ;
#27349=AXIS2_PLACEMENT_3D ( 'NONE', #22422, #7225, #32635 ) ;
#27351=SHAPE_REPRESENTATION ( 'Part2_handle2', ( #2865 ), #8690 ) ;
#27374=CARTESIAN_POINT ( 'NONE',  ( 108.1863125916463986, 19.21562195068647938, -4.729927366917035414 ) ) ;
#27378=DIRECTION ( 'NONE',  ( 0.000000000000000000, 1.000000000000000000, 0.000000000000000000 ) ) ;
#27386=CARTESIAN_POINT ( 'NONE',  ( -30.13808104058193749, 10.31370525110837200, 1.976276180383223391 ) ) ;
#27394=CARTESIAN_POINT ( 'NONE',  ( -28.83037791825872276, 5.159822176738817490, 1.500000000000000000 ) ) ;
#27404=B_SPLINE_CURVE_WITH_KNOTS ( 'NONE', 3,
 ( #3625, #26380, #11784, #21667, #21817, #5953, #3780, #952, #3963, #24170 ),
 .UNSPECIFIED., .F., .F.,
 ( 4, 2, 2, 2, 4 ),
 ( 0.000000000000000000, 0.0002027550720618977013, 0.0004055101441237954026, 0.0006082652161856931311, 0.0008110202882475908053 ),
 .UNSPECIFIED. ) ;
#27425=CARTESIAN_POINT ( 'NONE',  ( 13.58264871869483059, 21.92667377881535629, 1.161774810368582767 ) ) ;
#27427=B_SPLINE_CURVE_WITH_KNOTS ( 'NONE', 3,
 ( #17087, #16933, #29818, #14598 ),
 .UNSPECIFIED., .F., .F.,
 ( 4, 4 ),
 ( 1.640695603511827301E-18, 0.0002986946104689498695 ),
 .UNSPECIFIED. ) ;
#27429=CARTESIAN_POINT ( 'NONE',  ( 107.1769020805352142, 16.40214705320008903, 1.508259000770581615 ) ) ;
#27431=CIRCLE ( 'NONE', #19973, 10.43371088333262087 ) ;
#27432=VECTOR ( 'NONE', #20811, 1000.000000000000114 ) ;
#27433=CARTESIAN_POINT ( 'NONE',  ( -19.16594587638616076, 17.36640870223476085, 1.500000000000000000 ) ) ;
#27435=DIRECTION ( 'NONE',  ( 1.000000000000000000, 0.000000000000000000, 0.000000000000000000 ) ) ;
#27443=FACE_OUTER_BOUND ( 'NONE', #9156, .T. ) ;
#27446=CARTESIAN_POINT ( 'NONE',  ( 56.97280603064898941, -277.2763395528616002, 1.500000000000000000 ) ) ;
#27450=DIRECTION ( 'NONE',  ( -1.000000000000000000, 0.000000000000000000, 0.000000000000000000 ) ) ;
#27452=DIRECTION ( 'NONE',  ( 0.7822388118548813107, -0.4516257885949860884, -0.4291113938172939068 ) ) ;
#27453=EDGE_CURVE ( 'NONE', #29127, #2157, #19467, .T. ) ;
#27460=ORIENTED_EDGE ( 'NONE', *, *, #28151, .T. ) ;
#27461=CARTESIAN_POINT ( 'NONE',  ( 22.89387586481974424, 17.41384229090520464, -1.500000000000117906 ) ) ;
#27462=CARTESIAN_POINT ( 'NONE',  ( 8.886302293890576465, 0.01997115109545568104, -1.161565467022932729 ) ) ;
#27469=CARTESIAN_POINT ( 'NONE',  ( 8.870145747188287189, 0.000000000000000000, 1.000000000000000000 ) ) ;
#27474=CIRCLE ( 'NONE', #31754, 5.100000000000000533 ) ;
#27488=ORIENTED_EDGE ( 'NONE', *, *, #31040, .T. ) ;
#27491=ORIENTED_EDGE ( 'NONE', *, *, #22972, .F. ) ;
#27496=CONICAL_SURFACE ( 'NONE', #32313, 10.97000000000001485, 0.1745329251994333364 ) ;
#27507=DIRECTION ( 'NONE',  ( 0.000000000000000000, -0.9271838545667855369, -0.3746065934159163446 ) ) ;
#27517=CARTESIAN_POINT ( 'NONE',  ( 107.2807778896295616, 16.98061326146200045, -2.731285459285014205 ) ) ;
#27529=ORIENTED_EDGE ( 'NONE', *, *, #29562, .F. ) ;
#27536=CARTESIAN_POINT ( 'NONE',  ( -31.80940264096946635, 0.000000000000000000, 4.148259000770580407 ) ) ;
#27545=DIRECTION ( 'NONE',  ( 0.000000000000000000, 1.000000000000000000, 0.000000000000000000 ) ) ;
#27548=CARTESIAN_POINT ( 'NONE',  ( -56.72401055955798199, 0.2376380563149646796, -1.445333642338585634 ) ) ;
#27563=ORIENTED_EDGE ( 'NONE', *, *, #4347, .T. ) ;
#27574=EDGE_CURVE ( 'NONE', #25915, #12626, #31837, .T. ) ;
#27580=DIRECTION ( 'NONE',  ( -0.000000000000000000, -0.000000000000000000, -1.000000000000000000 ) ) ;
#27589=CARTESIAN_POINT ( 'NONE',  ( -16.91808550243790066, 10.26716432527312683, 1.977393880026240724 ) ) ;
#27590=CARTESIAN_POINT ( 'NONE',  ( -23.54713438637982748, 3.520075575296777171, 1.500000000000000000 ) ) ;
#27596=ORIENTED_EDGE ( 'NONE', *, *, #16403, .T. ) ;
#27597=CARTESIAN_POINT ( 'NONE',  ( 8.454317476977939450, 15.00000000000000178, 4.148259000770580407 ) ) ;
#27604=CARTESIAN_POINT ( 'NONE',  ( 108.0257329329460134, 18.32145104924472889, -5.109022856120751577 ) ) ;
#27606=DIRECTION ( 'NONE',  ( -1.000000000000000000, 1.321650053510178573E-16, -0.000000000000000000 ) ) ;
#27611=EDGE_CURVE ( 'NONE', #429, #28913, #4417, .T. ) ;
#27617=CARTESIAN_POINT ( 'NONE',  ( 8.950995676490915542, 0.000000000000000000, -1.008084992930270651 ) ) ;
#27638=ORIENTED_EDGE ( 'NONE', *, *, #28956, .T. ) ;
#27639=CARTESIAN_POINT ( 'NONE',  ( 107.7876430001691404, 19.84562591319662417, 3.582469705350817435 ) ) ;
#27644=EDGE_LOOP ( 'NONE', ( #6178, #6671, #31926, #29407 ) ) ;
#27681=CARTESIAN_POINT ( 'NONE',  ( -59.84585868070823267, -5.753144558333703529, 1.500000000000000000 ) ) ;
#27682=CARTESIAN_POINT ( 'NONE',  ( 9.192617927958346868, 0.08611596088357059697, -1.322472180771091077 ) ) ;
#27690=LINE ( 'NONE', #2308, #21908 ) ;
#27692=CARTESIAN_POINT ( 'NONE',  ( 79.17573959169237696, 22.98125563777605151, -4.612695725900423760 ) ) ;
#27696=CARTESIAN_POINT ( 'NONE',  ( -56.77817977891114509, 0.4289077168656530992, -1.500224696652619372 ) ) ;
#27698=ORIENTED_EDGE ( 'NONE', *, *, #1597, .T. ) ;
#27717=ORIENTED_EDGE ( 'NONE', *, *, #12396, .F. ) ;
#27725=CARTESIAN_POINT ( 'NONE',  ( -41.54914239086199501, -15.55749394147906806, 5.221013518636386408 ) ) ;
#27736=CARTESIAN_POINT ( 'NONE',  ( 12.72110778810032805, 6.644964735738586370, 1.500000000000000222 ) ) ;
#27737=DIRECTION ( 'NONE',  ( -1.000000000000000000, -1.369475477426763776E-16, 0.000000000000000000 ) ) ;
#27740=CARTESIAN_POINT ( 'NONE',  ( -27.51259159022300693, 5.525525355233276592, 1.500000000001506795 ) ) ;
#27743=CARTESIAN_POINT ( 'NONE',  ( 8.870145747188287189, 0.000000000000000000, 1.000000000000000000 ) ) ;
#27755=CARTESIAN_POINT ( 'NONE',  ( -23.31977477728428028, 3.998227953278257640, 2.146185852361371715 ) ) ;
#27760=DIRECTION ( 'NONE',  ( -0.1327696077594705815, 0.9911469271785068313, 0.000000000000000000 ) ) ;
#27779=CARTESIAN_POINT ( 'NONE',  ( 107.4505076186455312, 17.92734628881788694, -4.758038775231021589 ) ) ;
#27781=DIRECTION ( 'NONE',  ( -0.8251117619019981975, 0.5649695393302014423, 0.000000000000000000 ) ) ;
#27792=LINE ( 'NONE', #2233, #24220 ) ;
#27794=DIRECTION ( 'NONE',  ( 0.09975574163943223827, -0.1727820128662104771, 0.9798954883250904357 ) ) ;
#27809=FACE_OUTER_BOUND ( 'NONE', #4052, .T. ) ;
#27810=DIRECTION ( 'NONE',  ( -0.000000000000000000, -0.000000000000000000, -1.000000000000000000 ) ) ;
#27820=VECTOR ( 'NONE', #6414, 1000.000000000000000 ) ;
#27829=ORIENTED_EDGE ( 'NONE', *, *, #15714, .F. ) ;
#27850=CARTESIAN_POINT ( 'NONE',  ( 24.72695737054825926, 18.91229966141139229, -1.500000000000000000 ) ) ;
#27860=CIRCLE ( 'NONE', #20404, 12.49867430706171767 ) ;
#27864=DIRECTION ( 'NONE',  ( -1.000000000000000000, 0.000000000000000000, 0.000000000000000000 ) ) ;
#27867=FACE_OUTER_BOUND ( 'NONE', #31547, .T. ) ;
#27870=CARTESIAN_POINT ( 'NONE',  ( -56.33578448538598593, 0.003046479576510432215, -1.000000000003751888 ) ) ;
#27871=CARTESIAN_POINT ( 'NONE',  ( 1.787149210215136508, -1.031811077599730231, 1.500000000000000000 ) ) ;
#27873=VECTOR ( 'NONE', #17766, 1000.000000000000114 ) ;
#27878=AXIS2_PLACEMENT_3D ( 'NONE', #25530, #7820, #14821 ) ;
#27895=ADVANCED_FACE ( 'NONE', ( #10141 ), #2766, .T. ) ;
#27903=FACE_OUTER_BOUND ( 'NONE', #18056, .T. ) ;
#27913=CARTESIAN_POINT ( 'NONE',  ( -53.85782592458283347, 5.498961903950442931, 1.337771607534410601 ) ) ;
#27920=CARTESIAN_POINT ( 'NONE',  ( 14.89337309020629085, 18.05463290658611442, -1.491740999229419273 ) ) ;
#27923=CARTESIAN_POINT ( 'NONE',  ( -30.17618327032176140, 10.26716432527324407, 1.977393880026174333 ) ) ;
#27927=B_SPLINE_CURVE_WITH_KNOTS ( 'NONE', 3,
 ( #16819, #3787, #1301, #8948, #11137, #21338, #29347, #9105, #19333, #15137 ),
 .UNSPECIFIED., .F., .F.,
 ( 4, 2, 2, 2, 4 ),
 ( -2.048411440084507189E-05, 0.0009701475628287921241, 0.001960779240058429466, 0.002951410917288066482, 0.003942042594517703932 ),
 .UNSPECIFIED. ) ;
#27942=CARTESIAN_POINT ( 'NONE',  ( -21.98045600181102088, 18.26191254974343536, 1.777803877838809221 ) ) ;
#27957=ADVANCED_FACE ( 'NONE', ( #13788 ), #14063, .T. ) ;
#27976=ORIENTED_EDGE ( 'NONE', *, *, #7221, .T. ) ;
#27977=CIRCLE ( 'NONE', #24769, 0.5000000000000006661 ) ;
#27997=EDGE_LOOP ( 'NONE', ( #16659, #18752, #28370, #28832, #2213 ) ) ;
#27998=CARTESIAN_POINT ( 'NONE',  ( -0.2059365608663963898, 0.5000000000000000000, -1.000000000000000000 ) ) ;
#27999=CARTESIAN_POINT ( 'NONE',  ( 17.32050807568873552, 10.00000000000002309, -1.500000000000000000 ) ) ;
#28042=ADVANCED_FACE ( 'NONE', ( #1788 ), #3968, .T. ) ;
#28051=CARTESIAN_POINT ( 'NONE',  ( -56.30973635671871591, -3.699839913606783250E-14, -1.000000000020692115 ) ) ;
#28053=ORIENTED_EDGE ( 'NONE', *, *, #8449, .F. ) ;
#28059=EDGE_CURVE ( 'NONE', #32600, #29167, #16621, .T. ) ;
#28060=CARTESIAN_POINT ( 'NONE',  ( 107.9510396086168811, 17.90552914680446506, 4.858489096870307833 ) ) ;
#28062=FACE_OUTER_BOUND ( 'NONE', #4173, .T. ) ;
#28066=DIRECTION ( 'NONE',  ( -1.000000000000000000, -1.369475477426764022E-16, 0.000000000000000000 ) ) ;
#28076=CARTESIAN_POINT ( 'NONE',  ( -41.39035047991316674, -16.40843718609402302, 2.028141679950118625 ) ) ;
#28077=CARTESIAN_POINT ( 'NONE',  ( 107.4385791398478744, 17.85938043952733878, 4.629213727441584325 ) ) ;
#28088=EDGE_CURVE ( 'NONE', #15521, #29681, #4456, .T. ) ;
#28091=CARTESIAN_POINT ( 'NONE',  ( -24.48050464856543584, 3.520075575297991755, 1.500000000000000000 ) ) ;
#28095=DIRECTION ( 'NONE',  ( 0.000000000000000000, 0.000000000000000000, 1.000000000000000000 ) ) ;
#28100=VERTEX_POINT ( 'NONE', #6779 ) ;
#28103=CARTESIAN_POINT ( 'NONE',  ( -16.95333583173749759, 10.33954000514843585, 1.975604575489919412 ) ) ;
#28127=CARTESIAN_POINT ( 'NONE',  ( -38.14293509397969473, 10.97000000000000419, 1.500000000000000000 ) ) ;
#28143=ADVANCED_FACE ( 'NONE', ( #21822 ), #1601, .T. ) ;
#28148=DIRECTION ( 'NONE',  ( -0.8660254037844409281, 0.4999999999999960587, 0.000000000000000000 ) ) ;
#28151=EDGE_CURVE ( 'NONE', #11370, #21301, #7126, .T. ) ;
#28155=DIRECTION ( 'NONE',  ( 1.000000000000000000, 0.000000000000000000, 7.709882115452493155E-15 ) ) ;
#28164=( BOUNDED_SURFACE ( )  B_SPLINE_SURFACE ( 1, 3, ( 
 ( #29521, #26661, #31867, #11776 ),
 ( #21660, #21980, #1772, #3771 ) ),
 .UNSPECIFIED., .F., .F., .F. ) 
 B_SPLINE_SURFACE_WITH_KNOTS ( ( 2, 2 ),
 ( 4, 4 ),
 ( 0.000000000000000000, 1.000000000000000000 ),
 ( 0.000000000000000000, 1.000000000000000000 ),
 .UNSPECIFIED. ) 
 GEOMETRIC_REPRESENTATION_ITEM ( )  RATIONAL_B_SPLINE_SURFACE ( (
 ( 1.000000000000000000, 0.9321687722090974404, 0.9321687722090974404, 1.000000000000000000),
 ( 1.000000000000000000, 0.9321687722090974404, 0.9321687722090974404, 1.000000000000000000) ) ) 
 REPRESENTATION_ITEM ( '' )  SURFACE ( )  );
#28172=VERTEX_POINT ( 'NONE', #22825 ) ;
#28193=CYLINDRICAL_SURFACE ( 'NONE', #23511, 3.250000000000002665 ) ;
#28201=CARTESIAN_POINT ( 'NONE',  ( -56.35610254884790038, 0.001801644430070462348, -1.071919094844493214 ) ) ;
#28210=ORIENTED_EDGE ( 'NONE', *, *, #5684, .F. ) ;
#28218=CARTESIAN_POINT ( 'NONE',  ( -56.28351068136514357, 0.000000000000000000, -1.000000000000000000 ) ) ;
#28245=EDGE_CURVE ( 'NONE', #24410, #11079, #25843, .T. ) ;
#28249=CARTESIAN_POINT ( 'NONE',  ( 107.6454888467326469, 19.04626834818095915, -4.993545475007672430 ) ) ;
#28251=CARTESIAN_POINT ( 'NONE',  ( -17.23523782256200576, 9.003349235486576063, 2.010613759594101602 ) ) ;
#28254=ORIENTED_EDGE ( 'NONE', *, *, #15706, .F. ) ;
#28255=EDGE_CURVE ( 'NONE', #22155, #18469, #13008, .T. ) ;
#28264=DIRECTION ( 'NONE',  ( 0.000000000000000000, 0.000000000000000000, -1.000000000000000000 ) ) ;
#28272=CARTESIAN_POINT ( 'NONE',  ( -25.35132950642825733, 18.20714672489456731, 1.779116719942482883 ) ) ;
#28278=ORIENTED_EDGE ( 'NONE', *, *, #14056, .F. ) ;
#28296=VERTEX_POINT ( 'NONE', #20665 ) ;
#28300=EDGE_CURVE ( 'NONE', #17857, #17891, #26157, .T. ) ;
#28305=EDGE_LOOP ( 'NONE', ( #20104, #15777, #760, #12468, #26990 ) ) ;
#28312=CIRCLE ( 'NONE', #17106, 0.4499999999999983458 ) ;
#28324=CIRCLE ( 'NONE', #13344, 10.95101833074431852 ) ;
#28328=DIRECTION ( 'NONE',  ( 1.000000000000000000, 0.000000000000000000, 0.000000000000000000 ) ) ;
#28345=VERTEX_POINT ( 'NONE', #23955 ) ;
#28351=CARTESIAN_POINT ( 'NONE',  ( 17.32050807568873552, 10.00000000000002309, 1.500000000000000000 ) ) ;
#28354=ORIENTED_EDGE ( 'NONE', *, *, #24095, .T. ) ;
#28357=DIRECTION ( 'NONE',  ( 1.000000000000000000, 0.000000000000000000, 0.000000000000000000 ) ) ;
#28361=DIRECTION ( 'NONE',  ( 0.000000000000000000, 0.000000000000000000, 1.000000000000000000 ) ) ;
#28370=ORIENTED_EDGE ( 'NONE', *, *, #9278, .F. ) ;
#28373=AXIS2_PLACEMENT_3D ( 'NONE', #1405, #1243, #8274 ) ;
#28374=CARTESIAN_POINT ( 'NONE',  ( 107.4385791398478744, 17.85938043952739918, 4.629213727441584325 ) ) ;
#28377=ORIENTED_EDGE ( 'NONE', *, *, #25708, .T. ) ;
#28396=CARTESIAN_POINT ( 'NONE',  ( -50.81000000000000227, -10.96999999999998643, 5.500000000000000000 ) ) ;
#28399=DIRECTION ( 'NONE',  ( 0.4999999999999918954, 0.8660254037844433705, -0.000000000000000000 ) ) ;
#28403=AXIS2_PLACEMENT_3D ( 'NONE', #26526, #19003, #29189 ) ;
#28410=EDGE_CURVE ( 'NONE', #2361, #12070, #27427, .T. ) ;
#28420=CARTESIAN_POINT ( 'NONE',  ( -2.794738735352966685, 0.000000000000000000, 1.508259000770582059 ) ) ;
#28436=CARTESIAN_POINT ( 'NONE',  ( -17.23085155655856582, 13.48267608780297167, 1.895199557107909438 ) ) ;
#28439=ORIENTED_EDGE ( 'NONE', *, *, #6176, .F. ) ;
#28447=CARTESIAN_POINT ( 'NONE',  ( 22.89656613554824105, 17.95482223816882339, -1.500000000000000222 ) ) ;
#28450=CARTESIAN_POINT ( 'NONE',  ( 22.41270750095310049, 17.13964222901159573, 1.499999999999170441 ) ) ;
#28455=VERTEX_POINT ( 'NONE', #4229 ) ;
#28457=EDGE_CURVE ( 'NONE', #13484, #9295, #27431, .T. ) ;
#28461=DIRECTION ( 'NONE',  ( 1.000000000000000000, 6.288372600415920195E-15, 0.000000000000000000 ) ) ;
#28482=CARTESIAN_POINT ( 'NONE',  ( -41.86373177837820236, -16.13513036599589867, 5.128141679950118714 ) ) ;
#28494=CARTESIAN_POINT ( 'NONE',  ( 107.7704433617907398, 16.89989798460841541, 1.595839734757286577 ) ) ;
#28497=CARTESIAN_POINT ( 'NONE',  ( -56.34260592272676149, 0.003888339313515875358, -1.002939418600732768 ) ) ;
#28503=CARTESIAN_POINT ( 'NONE',  ( -83.35439080561378944, -0.0003384977252891612984, 0.000000000000000000 ) ) ;
#28509=ORIENTED_EDGE ( 'NONE', *, *, #28088, .F. ) ;
#28510=AXIS2_PLACEMENT_3D ( 'NONE', #25007, #7958, #2800 ) ;
#28520=CARTESIAN_POINT ( 'NONE',  ( 2.382865613620175349, 0.000000000000000000, 1.508259000770581615 ) ) ;
#28527=LINE ( 'NONE', #10958, #29488 ) ;
#28535=CIRCLE ( 'NONE', #16226, 5.587650971692158741 ) ;
#28543=DIRECTION ( 'NONE',  ( 0.5649695393302035518, 0.8251117619019968652, -0.000000000000000000 ) ) ;
#28545=DIRECTION ( 'NONE',  ( 0.9842544651762054064, -0.1767573132311699713, 0.000000000000000000 ) ) ;
#28564=DIRECTION ( 'NONE',  ( 0.8247831655431905329, -0.5654491399202531410, 0.000000000000000000 ) ) ;
#28566=EDGE_CURVE ( 'NONE', #15394, #15974, #27792, .T. ) ;
#28569=CARTESIAN_POINT ( 'NONE',  ( 10.90258948330155953, 17.51112508050605854, 4.629213727441584325 ) ) ;
#28576=CARTESIAN_POINT ( 'NONE',  ( 108.2286012845016074, 19.45110207874543917, -3.054862429917418520 ) ) ;
#28579=EDGE_CURVE ( 'NONE', #9295, #1225, #7700, .T. ) ;
#28596=ORIENTED_EDGE ( 'NONE', *, *, #28579, .F. ) ;
#28611=DIRECTION ( 'NONE',  ( -0.000000000000000000, -0.3746065934159164001, 0.9271838545667856479 ) ) ;
#28613=CARTESIAN_POINT ( 'NONE',  ( -55.91000000000000369, -10.96999999999998643, 5.700000000000000178 ) ) ;
#28614=CARTESIAN_POINT ( 'NONE',  ( 17.92222975120050776, 13.44085466220149172, 1.050000000000000044 ) ) ;
#28616=FACE_OUTER_BOUND ( 'NONE', #29363, .T. ) ;
#28626=CARTESIAN_POINT ( 'NONE',  ( -22.70948346437429066, 4.195786794270493836, 1.500000000001212808 ) ) ;
#28627=CARTESIAN_POINT ( 'NONE',  ( 46.92593983402662872, 24.78664516185572353, 5.412820279296878923 ) ) ;
#28629=DIRECTION ( 'NONE',  ( 0.8660254037844424824, -0.4999999999999933942, 0.000000000000000000 ) ) ;
#28637=ORIENTED_EDGE ( 'NONE', *, *, #15867, .F. ) ;
#28643=DIRECTION ( 'NONE',  ( -1.000000000000000000, 0.000000000000000000, 0.000000000000000000 ) ) ;
#28662=EDGE_LOOP ( 'NONE', ( #26808, #32723, #27976, #30402 ) ) ;
#28685=CARTESIAN_POINT ( 'NONE',  ( 10.49279877231860425, 2.037595134782375084, 1.050000000000000266 ) ) ;
#28697=CARTESIAN_POINT ( 'NONE',  ( 13.62547635268498780, 21.94000000000002970, -1.500000000000000000 ) ) ;
#28720=CARTESIAN_POINT ( 'NONE',  ( 26.05758037654617354, 19.05414323982526525, -1.152255141331423705 ) ) ;
#28734=FACE_OUTER_BOUND ( 'NONE', #19771, .T. ) ;
#28746=DIRECTION ( 'NONE',  ( -0.8660254037844418162, 0.4999999999999946154, 0.000000000000000000 ) ) ;
#28750=ORIENTED_EDGE ( 'NONE', *, *, #21609, .T. ) ;
#28751=ORIENTED_EDGE ( 'NONE', *, *, #9523, .T. ) ;
#28753=DIRECTION ( 'NONE',  ( 0.000000000000000000, -0.9271838545667856479, -0.3746065934159163446 ) ) ;
#28760=CARTESIAN_POINT ( 'NONE',  ( 14.61912536820988784, 9.825622711161967615, 1.500000000000000000 ) ) ;
#28764=FACE_OUTER_BOUND ( 'NONE', #17514, .T. ) ;
#28765=ORIENTED_EDGE ( 'NONE', *, *, #20628, .F. ) ;
#28769=CARTESIAN_POINT ( 'NONE',  ( -19.16594587638449099, 5.061405101124994310, 1.500000000000000000 ) ) ;
#28771=CARTESIAN_POINT ( 'NONE',  ( 15.28872660057386845, 20.76088595412476678, 4.629213727441584325 ) ) ;
#28779=DIRECTION ( 'NONE',  ( -0.7822388118548813107, 0.4516257885949860884, 0.4291113938172937958 ) ) ;
#28784=FACE_OUTER_BOUND ( 'NONE', #28662, .T. ) ;
#28785=FACE_OUTER_BOUND ( 'NONE', #8645, .T. ) ;
#28790=EDGE_CURVE ( 'NONE', #18979, #6904, #30577, .T. ) ;
#28791=CARTESIAN_POINT ( 'NONE',  ( -2.541067152580809729, 0.4393720697977929746, -1.497239384009418250 ) ) ;
#28812=CARTESIAN_POINT ( 'NONE',  ( 107.1769020805352142, 16.40214705320006061, 1.508259000770582725 ) ) ;
#28823=VECTOR ( 'NONE', #3085, 1000.000000000000000 ) ;
#28832=ORIENTED_EDGE ( 'NONE', *, *, #15446, .T. ) ;
#28836=EDGE_LOOP ( 'NONE', ( #1311, #31471, #13536, #23784, #10363 ) ) ;
#28858=VECTOR ( 'NONE', #29879, 1000.000000000000000 ) ;
#28864=EDGE_CURVE ( 'NONE', #27055, #19054, #8008, .T. ) ;
#28865=VERTEX_POINT ( 'NONE', #20400 ) ;
#28871=AXIS2_PLACEMENT_3D ( 'NONE', #19105, #3247, #11425 ) ;
#28872=CARTESIAN_POINT ( 'NONE',  ( 8.911384905465473238, 0.2172754300402683358, 1.412391582771866716 ) ) ;
#28874=CARTESIAN_POINT ( 'NONE',  ( 13.04731869766886554, 19.33256796700939262, 5.412820279296879811 ) ) ;
#28883=CARTESIAN_POINT ( 'NONE',  ( -56.27770248097862549, 0.4996615022747108448, -1.050000000000000044 ) ) ;
#28897=CARTESIAN_POINT ( 'NONE',  ( -57.12917293608614955, -2.964366234459023808, 5.871858320049880398 ) ) ;
#28898=AXIS2_PLACEMENT_3D ( 'NONE', #11494, #21690, #22808 ) ;
#28905=CARTESIAN_POINT ( 'NONE',  ( -23.54713438637982748, 8.443947424854778561, 8.182767265444946148 ) ) ;
#28906=EDGE_CURVE ( 'NONE', #7656, #25302, #12690, .T. ) ;
#28908=VECTOR ( 'NONE', #25472, 1000.000000000000227 ) ;
#28913=VERTEX_POINT ( 'NONE', #30783 ) ;
#28939=FACE_OUTER_BOUND ( 'NONE', #16965, .T. ) ;
#28946=CIRCLE ( 'NONE', #32159, 10.97000000000000064 ) ;
#28954=TOROIDAL_SURFACE ( 'NONE', #9654, 0.05000000000000002359, 0.4500000000000000111 ) ;
#28956=EDGE_CURVE ( 'NONE', #28865, #28455, #12130, .T. ) ;
#28958=AXIS2_PLACEMENT_3D ( 'NONE', #9335, #12022, #22216 ) ;
#28963=CARTESIAN_POINT ( 'NONE',  ( -31.80959807272228090, -0.0003384977252905707612, 0.000000000000000000 ) ) ;
#28975=VECTOR ( 'NONE', #8973, 1000.000000000000114 ) ;
#28976=CARTESIAN_POINT ( 'NONE',  ( 12.22604216760896989, 4.899348760700370065, -1.050000000000000044 ) ) ;
#29005=DIRECTION ( 'NONE',  ( 0.4999999999999977796, 0.8660254037844399289, 0.000000000000000000 ) ) ;
#29017=EDGE_CURVE ( 'NONE', #25797, #29167, #1599, .T. ) ;
#29037=CARTESIAN_POINT ( 'NONE',  ( -23.54713438637982748, 8.275374457817619600, 8.600000000000003197 ) ) ;
#29051=ORIENTED_EDGE ( 'NONE', *, *, #16475, .T. ) ;
#29054=AXIS2_PLACEMENT_3D ( 'NONE', #28396, #5666, #18675 ) ;
#29067=CARTESIAN_POINT ( 'NONE',  ( 25.79765260763087298, 19.02692269782062340, -1.329833256668973229 ) ) ;
#29072=CARTESIAN_POINT ( 'NONE',  ( 17.32050807568873552, 10.00000000000002309, -1.500000000000000000 ) ) ;
#29084=CARTESIAN_POINT ( 'NONE',  ( -57.62025439570817298, -2.863290445579637300, 5.500000000000000000 ) ) ;
#29086=LINE ( 'NONE', #13825, #4949 ) ;
#29088=ORIENTED_EDGE ( 'NONE', *, *, #4642, .T. ) ;
#29092=CARTESIAN_POINT ( 'NONE',  ( 9.331062908042635939, 15.00000000000000178, -4.612695725900422872 ) ) ;
#29108=DIRECTION ( 'NONE',  ( 1.000000000000000000, 0.000000000000000000, -0.000000000000000000 ) ) ;
#29119=DIRECTION ( 'NONE',  ( -0.1327696077594705815, 0.9911469271785068313, 0.000000000000000000 ) ) ;
#29120=CARTESIAN_POINT ( 'NONE',  ( 9.300322098500100054, 0.2432316347765305364, 1.049936813265543556 ) ) ;
#29125=FACE_OUTER_BOUND ( 'NONE', #19024, .T. ) ;
#29127=VERTEX_POINT ( 'NONE', #5120 ) ;
#29140=CARTESIAN_POINT ( 'NONE',  ( 9.302055952181039089, 0.2457637073014076190, -1.500000000000000000 ) ) ;
#29142=DIRECTION ( 'NONE',  ( -0.000000000000000000, -0.3746065934159164001, 0.9271838545667856479 ) ) ;
#29166=ORIENTED_EDGE ( 'NONE', *, *, #23084, .F. ) ;
#29167=VERTEX_POINT ( 'NONE', #25853 ) ;
#29177=CARTESIAN_POINT ( 'NONE',  ( -56.61259478326383743, 0.1231456938264295642, 1.516656275171373469 ) ) ;
#29187=CARTESIAN_POINT ( 'NONE',  ( 0.000000000000000000, 0.000000000000000000, 1.500000000000000000 ) ) ;
#29189=DIRECTION ( 'NONE',  ( -1.000000000000000000, 0.000000000000000000, 0.000000000000000000 ) ) ;
#29221=DIRECTION ( 'NONE',  ( 0.8660254037844409281, -0.4999999999999960587, 0.000000000000000000 ) ) ;
#29238=CARTESIAN_POINT ( 'NONE',  ( 107.1769020805352142, 16.40214705320006061, -1.491740999229420161 ) ) ;
#29246=DIRECTION ( 'NONE',  ( 0.000000000000000000, 0.000000000000000000, 1.000000000000000000 ) ) ;
#29256=CARTESIAN_POINT ( 'NONE',  ( 19.82965097529934084, 15.28209255204611594, 1.049999999999883027 ) ) ;
#29258=DIRECTION ( 'NONE',  ( 0.000000000000000000, 0.000000000000000000, -1.000000000000000000 ) ) ;
#29274=ADVANCED_FACE ( 'NONE', ( #26640 ), #26496, .T. ) ;
#29276=EDGE_CURVE ( 'NONE', #8881, #22866, #13426, .T. ) ;
#29289=CARTESIAN_POINT ( 'NONE',  ( 17.54326037877522637, 13.05023557613625584, -1.050000000000000044 ) ) ;
#29300=CARTESIAN_POINT ( 'NONE',  ( 2.382865613620175349, 0.000000000000000000, 1.508259000770581615 ) ) ;
#29309=DIRECTION ( 'NONE',  ( -0.9164966213036979115, 0.4000424266736042900, 0.000000000000000000 ) ) ;
#29310=EDGE_CURVE ( 'NONE', #22866, #25302, #27860, .T. ) ;
#29322=CARTESIAN_POINT ( 'NONE',  ( 13.62547635268498780, 21.94000000000002970, 1.500000000000000000 ) ) ;
#29345=CARTESIAN_POINT ( 'NONE',  ( -29.34654203815345141, 5.078599898679035718, 1.213362788697829542 ) ) ;
#29347=CARTESIAN_POINT ( 'NONE',  ( -40.96618937992463572, -13.73263466181244041, 5.759795317147328397 ) ) ;
#29350=EDGE_CURVE ( 'NONE', #2361, #4711, #22294, .T. ) ;
#29362=CARTESIAN_POINT ( 'NONE',  ( 10.90258948330155953, 17.51112508050605854, 4.629213727441584325 ) ) ;
#29363=EDGE_LOOP ( 'NONE', ( #12911, #5495 ) ) ;
#29366=DIRECTION ( 'NONE',  ( -0.000000000000000000, -0.000000000000000000, -1.000000000000000000 ) ) ;
#29372=TOROIDAL_SURFACE ( 'NONE', #3218, 10.43371088333261731, 0.4500000000000000111 ) ;
#29374=DIRECTION ( 'NONE',  ( 0.000000000000000000, 0.000000000000000000, 1.000000000000000000 ) ) ;
#29376=CARTESIAN_POINT ( 'NONE',  ( 107.2615523761464260, 16.89492944954590214, 0.000000000000000000 ) ) ;
#29377=ADVANCED_FACE ( 'NONE', ( #27303 ), #10059, .T. ) ;
#29407=ORIENTED_EDGE ( 'NONE', *, *, #4642, .F. ) ;
#29422=ORIENTED_EDGE ( 'NONE', *, *, #3986, .F. ) ;
#29433=CARTESIAN_POINT ( 'NONE',  ( -24.43722099606875275, 18.60133783399176011, 1.500000000000506040 ) ) ;
#29435=CONICAL_SURFACE ( 'NONE', #15002, 5.999999999999999112, 0.08726646259971666819 ) ;
#29443=AXIS2_PLACEMENT_3D ( 'NONE', #17935, #383, #13081 ) ;
#29447=VERTEX_POINT ( 'NONE', #22793 ) ;
#29459=EDGE_CURVE ( 'NONE', #30955, #30284, #17773, .T. ) ;
#29464=ORIENTED_EDGE ( 'NONE', *, *, #31481, .T. ) ;
#29478=VECTOR ( 'NONE', #2133, 1000.000000000000000 ) ;
#29488=VECTOR ( 'NONE', #15455, 999.9999999999998863 ) ;
#29489=DIRECTION ( 'NONE',  ( 0.000000000000000000, 0.000000000000000000, -1.000000000000000000 ) ) ;
#29521=CARTESIAN_POINT ( 'NONE',  ( 7.577572045913206544, 15.00000000000002132, -4.612695725900421984 ) ) ;
#29529=CIRCLE ( 'NONE', #30624, 302.4235430809786749 ) ;
#29551=CARTESIAN_POINT ( 'NONE',  ( 9.220104123695119114, 0.1261569107277066837, -1.391360883757695399 ) ) ;
#29552=AXIS2_PLACEMENT_3D ( 'NONE', #7185, #10160, #32776 ) ;
#29557=CARTESIAN_POINT ( 'NONE',  ( 8.886302293890576465, 0.01997115109545394632, 1.161565467022927622 ) ) ;
#29560=DIRECTION ( 'NONE',  ( 1.000000000000000000, -0.000000000000000000, -0.000000000000000000 ) ) ;
#29562=EDGE_CURVE ( 'NONE', #28100, #21723, #19656, .T. ) ;
#29565=CARTESIAN_POINT ( 'NONE',  ( 108.1105523077318651, 18.79375879618914169, -4.458706230583343810 ) ) ;
#29566=FACE_OUTER_BOUND ( 'NONE', #17223, .T. ) ;
#29574=ORIENTED_EDGE ( 'NONE', *, *, #13539, .F. ) ;
#29577=CARTESIAN_POINT ( 'NONE',  ( 17.32050807568873552, 10.00000000000002309, 0.000000000000000000 ) ) ;
#29587=CARTESIAN_POINT ( 'NONE',  ( -40.16771308880407076, -10.96999999999998643, 5.500000000000000000 ) ) ;
#29604=AXIS2_PLACEMENT_3D ( 'NONE', #30744, #27545, #128 ) ;
#29613=CARTESIAN_POINT ( 'NONE',  ( 16.02642041956679719, 11.88017725832204974, 1.500000000000000222 ) ) ;
#29616=CARTESIAN_POINT ( 'NONE',  ( -16.41799616858202171, 12.22102706438217368, 1.500000000000000000 ) ) ;
#29617=CARTESIAN_POINT ( 'NONE',  ( -24.41756317296288969, 18.46223496596762459, 1.773004750130063867 ) ) ;
#29626=VECTOR ( 'NONE', #32161, 1000.000000000000000 ) ;
#29627=CARTESIAN_POINT ( 'NONE',  ( 9.302055952181039089, 0.2457637073014079521, -1.050000000000000044 ) ) ;
#29644=CARTESIAN_POINT ( 'NONE',  ( 13.32584843873297409, 6.791410140412673435, -1.500000000000237366 ) ) ;
#29668=VERTEX_POINT ( 'NONE', #5731 ) ;
#29676=ADVANCED_FACE ( 'NONE', ( #29125 ), #6211, .T. ) ;
#29679=CARTESIAN_POINT ( 'NONE',  ( 1.787149210215136508, -1.031811077599730231, 1.500000000000000000 ) ) ;
#29681=VERTEX_POINT ( 'NONE', #3709 ) ;
#29683=CARTESIAN_POINT ( 'NONE',  ( -56.36516744639037313, 0.007311977099128529056, -1.006610376653334971 ) ) ;
#29687=CARTESIAN_POINT ( 'NONE',  ( 15.28872660057386845, 20.76088595412476678, -4.612695725900421984 ) ) ;
#29713=CARTESIAN_POINT ( 'NONE',  ( 14.89840567085375866, 9.424658325534814196, -1.050000000000000044 ) ) ;
#29725=CARTESIAN_POINT ( 'NONE',  ( -57.12917293608614955, -2.964366234459024696, 5.871858320049880398 ) ) ;
#29728=CARTESIAN_POINT ( 'NONE',  ( 25.59657441296793934, 19.00570861426560043, 1.395765800962750713 ) ) ;
#29743=CARTESIAN_POINT ( 'NONE',  ( 107.8323272165538640, 17.24449170613245030, -2.317971953726807754 ) ) ;
#29770=CARTESIAN_POINT ( 'NONE',  ( -26.89442091290521830, 17.54567542505808575, 1.795026885182104071 ) ) ;
#29786=EDGE_LOOP ( 'NONE', ( #11111, #16160 ) ) ;
#29788=CARTESIAN_POINT ( 'NONE',  ( -53.72801162551947840, 5.497307881342318403, 1.430198536305348656 ) ) ;
#29790=CARTESIAN_POINT ( 'NONE',  ( 0.6708088701982984903, 0.000000000000000000, -4.612695725900422872 ) ) ;
#29793=EDGE_CURVE ( 'NONE', #1782, #1418, #7670, .T. ) ;
#29796=FACE_OUTER_BOUND ( 'NONE', #25285, .T. ) ;
#29818=CARTESIAN_POINT ( 'NONE',  ( 8.917086725895012833, 0.3004441037763295186, -1.469409787067161410 ) ) ;
#29832=EDGE_CURVE ( 'NONE', #14230, #16163, #2648, .T. ) ;
#29837=EDGE_LOOP ( 'NONE', ( #11348, #30874, #22209, #20749, #18714 ) ) ;
#29844=DIRECTION ( 'NONE',  ( 0.000000000000000000, 0.000000000000000000, 1.000000000000000000 ) ) ;
#29856=VERTEX_POINT ( 'NONE', #20711 ) ;
#29857=DIRECTION ( 'NONE',  ( -0.1736481776669307198, -2.126576849575776229E-17, -0.9848077530122080203 ) ) ;
#29860=CARTESIAN_POINT ( 'NONE',  ( 17.32050807568873552, 10.00000000000002309, -1.500000000000000000 ) ) ;
#29873=CARTESIAN_POINT ( 'NONE',  ( 107.3084207622235482, 16.37966385977266270, 1.508007899815985153 ) ) ;
#29874=DIRECTION ( 'NONE',  ( -0.000000000000000000, -0.000000000000000000, -1.000000000000000000 ) ) ;
#29879=DIRECTION ( 'NONE',  ( -0.000000000000000000, -0.000000000000000000, -1.000000000000000000 ) ) ;
#29897=EDGE_CURVE ( 'NONE', #22155, #12070, #14474, .T. ) ;
#29924=ORIENTED_EDGE ( 'NONE', *, *, #2889, .F. ) ;
#29925=CARTESIAN_POINT ( 'NONE',  ( 11.68225172329192496, 4.861379696014986429, 1.500000000000000222 ) ) ;
#29926=CARTESIAN_POINT ( 'NONE',  ( -50.81000000000000227, -10.96999999999998643, 1.500000000000000000 ) ) ;
#29932=CARTESIAN_POINT ( 'NONE',  ( -50.81000000000000227, -10.96999999999998643, 5.500000000000000000 ) ) ;
#29935=AXIS2_PLACEMENT_3D ( 'NONE', #5209, #12878, #17920 ) ;
#29954=EDGE_CURVE ( 'NONE', #2157, #8276, #18246, .T. ) ;
#29958=FACE_OUTER_BOUND ( 'NONE', #26535, .T. ) ;
#29961=CARTESIAN_POINT ( 'NONE',  ( 24.29583315745070848, 18.19363606234995245, -1.499999999999882316 ) ) ;
#29971=LINE ( 'NONE', #24790, #25350 ) ;
#29985=VECTOR ( 'NONE', #5747, 1000.000000000000114 ) ;
#29991=CARTESIAN_POINT ( 'NONE',  ( 107.9638161812118256, 20.82655351785575348, 1.489452138568093664 ) ) ;
#29997=CARTESIAN_POINT ( 'NONE',  ( 56.97280603064898941, -277.2763395528616002, -1.491740999229418829 ) ) ;
#30009=AXIS2_PLACEMENT_3D ( 'NONE', #29932, #24754, #27435 ) ;
#30018=PLANE ( 'NONE',  #18409 ) ;
#30021=EDGE_CURVE ( 'NONE', #29668, #12740, #28527, .T. ) ;
#30023=FACE_OUTER_BOUND ( 'NONE', #25674, .T. ) ;
#30045=AXIS2_PLACEMENT_3D ( 'NONE', #16264, #16411, #24280 ) ;
#30047=ORIENTED_EDGE ( 'NONE', *, *, #28410, .T. ) ;
#30058=CARTESIAN_POINT ( 'NONE',  ( -55.91000000000000369, -10.96999999999998643, 5.700000000000000178 ) ) ;
#30067=DIRECTION ( 'NONE',  ( 1.000000000000000000, 0.000000000000000000, 0.000000000000000000 ) ) ;
#30076=DIRECTION ( 'NONE',  ( 0.000000000000000000, 0.000000000000000000, -1.000000000000000000 ) ) ;
#30077=CARTESIAN_POINT ( 'NONE',  ( -56.32443066862174419, 0.3152581172270095267, -1.465964887886411550 ) ) ;
#30078=LINE ( 'NONE', #15325, #29478 ) ;
#30084=AXIS2_PLACEMENT_3D ( 'NONE', #1935, #4438, #4245 ) ;
#30086=CARTESIAN_POINT ( 'NONE',  ( -29.01811942205308270, 5.485000000000015419, 1.500000000000000000 ) ) ;
#30089=PLANE ( 'NONE',  #712 ) ;
#30094=CIRCLE ( 'NONE', #6561, 0.9999999999999991118 ) ;
#30095=VERTEX_POINT ( 'NONE', #20818 ) ;
#30100=VECTOR ( 'NONE', #25028, 1000.000000000000000 ) ;
#30101=CIRCLE ( 'NONE', #7123, 0.4499999999999990119 ) ;
#30109=PLANE ( 'NONE',  #14439 ) ;
#30110=EDGE_CURVE ( 'NONE', #6161, #14600, #23657, .T. ) ;
#30116=CARTESIAN_POINT ( 'NONE',  ( 107.9617355966649654, 17.96508862869939094, -3.860795742263698482 ) ) ;
#30127=CARTESIAN_POINT ( 'NONE',  ( -16.85110191150524273, 12.14507408406953637, 1.499999999999892975 ) ) ;
#30128=CARTESIAN_POINT ( 'NONE',  ( -25.41317123495344177, 18.70748839123610452, 1.500000000000000000 ) ) ;
#30142=CARTESIAN_POINT ( 'NONE',  ( 108.0843732272301736, 18.64798334617831799, -4.598824503537998432 ) ) ;
#30151=DIRECTION ( 'NONE',  ( -0.7822388118548815328, 0.4516257885949861439, -0.4291113938172932962 ) ) ;
#30155=CARTESIAN_POINT ( 'NONE',  ( 8.870145747188287189, 0.000000000000000000, -1.000000000000002220 ) ) ;
#30165=CARTESIAN_POINT ( 'NONE',  ( 108.4602224094683010, 20.74085989589152845, -1.474553323550922723 ) ) ;
#30178=ORIENTED_EDGE ( 'NONE', *, *, #12098, .F. ) ;
#30189=PLANE ( 'NONE',  #10683 ) ;
#30221=FACE_OUTER_BOUND ( 'NONE', #14925, .T. ) ;
#30232=CARTESIAN_POINT ( 'NONE',  ( -31.91713028529358098, -0.0003384977252905707612, 2.028141679950118625 ) ) ;
#30233=CARTESIAN_POINT ( 'NONE',  ( 47.62814091865205768, 23.65599663307499512, -4.612695725900423760 ) ) ;
#30238=CARTESIAN_POINT ( 'NONE',  ( -56.28386703554979675, 2.926702260634249026E-12, -1.039475297285789024 ) ) ;
#30269=CARTESIAN_POINT ( 'NONE',  ( 107.9166481000539193, 17.71402365689241520, -3.323306282662723543 ) ) ;
#30276=CARTESIAN_POINT ( 'NONE',  ( 9.513773624275961183, 1.351470648933397412, 1.500000000000000222 ) ) ;
#30284=VERTEX_POINT ( 'NONE', #25124 ) ;
#30294=ORIENTED_EDGE ( 'NONE', *, *, #22432, .T. ) ;
#30302=CARTESIAN_POINT ( 'NONE',  ( -50.81000000000000227, -10.96999999999998643, 1.499999999999999556 ) ) ;
#30306=CARTESIAN_POINT ( 'NONE',  ( 5.865515302491369987, 15.00000000000000178, 1.508259000770582059 ) ) ;
#30316=CYLINDRICAL_SURFACE ( 'NONE', #21514, 12.49867430706168570 ) ;
#30337=DIRECTION ( 'NONE',  ( 0.000000000000000000, -0.9271838545667856479, -0.3746065934159164001 ) ) ;
#30340=CARTESIAN_POINT ( 'NONE',  ( 17.32050807568873552, 10.00000000000002309, 4.629213727441584325 ) ) ;
#30354=EDGE_CURVE ( 'NONE', #22866, #12952, #4916, .T. ) ;
#30362=CARTESIAN_POINT ( 'NONE',  ( 56.97280603064898941, -277.2763395528616002, -1.491740999229418829 ) ) ;
#30388=CARTESIAN_POINT ( 'NONE',  ( -56.29416256380356032, 0.02368334168385285987, -1.154763663137946761 ) ) ;
#30392=ORIENTED_EDGE ( 'NONE', *, *, #23394, .F. ) ;
#30398=CARTESIAN_POINT ( 'NONE',  ( 108.3696618535068126, 20.23658298680886958, 1.395260099363828665 ) ) ;
#30402=ORIENTED_EDGE ( 'NONE', *, *, #9562, .F. ) ;
#30425=ORIENTED_EDGE ( 'NONE', *, *, #12206, .T. ) ;
#30447=CARTESIAN_POINT ( 'NONE',  ( 107.4480564796146780, 17.91338030753361465, -4.728172914300420970 ) ) ;
#30454=DIRECTION ( 'NONE',  ( -0.000000000000000000, -0.000000000000000000, -1.000000000000000000 ) ) ;
#30472=DIRECTION ( 'NONE',  ( -0.8528685319524442754, 0.4924038765061022893, 0.1736481776669307198 ) ) ;
#30480=VERTEX_POINT ( 'NONE', #3410 ) ;
#30489=ORIENTED_EDGE ( 'NONE', *, *, #25545, .T. ) ;
#30493=CARTESIAN_POINT ( 'NONE',  ( -40.96572980946567100, -13.73075632567362980, 5.760101628985244915 ) ) ;
#30504=B_SPLINE_CURVE_WITH_KNOTS ( 'NONE', 3,
 ( #32201, #8786, #31707, #16449, #6419, #19309, #32014, #18990, #24635, #29177, #9270, #16804 ),
 .UNSPECIFIED., .F., .F.,
 ( 4, 2, 2, 2, 2, 4 ),
 ( 2.983873419563917522E-05, 0.0001332968301352377373, 0.0002367549260748362994, 0.0004436711179540329085, 0.0006505873098332294905, 0.0008575035017124260726 ),
 .UNSPECIFIED. ) ;
#30507=CARTESIAN_POINT ( 'NONE',  ( -56.33578448492038859, 0.003046479527603615251, -1.001959257668779690 ) ) ;
#30511=ADVANCED_FACE ( 'NONE', ( #28784 ), #16136, .T. ) ;
#30516=FACE_OUTER_BOUND ( 'NONE', #7999, .T. ) ;
#30524=( BOUNDED_SURFACE ( )  B_SPLINE_SURFACE ( 3, 2, ( 
 ( #9365, #19917, #1522 ),
 ( #29617, #29433, #27245 ),
 ( #16887, #19574, #30128 ),
 ( #29770, #6849, #14047 ),
 ( #17036, #6527, #14540 ),
 ( #12050, #22246, #16542 ),
 ( #24254, #19730, #1370 ),
 ( #4539, #11547, #21743 ),
 ( #11698, #31951, #19235 ),
 ( #27923, #7702, #4691 ),
 ( #17714, #20405, #17396 ),
 ( #32799, #2178, #5188 ),
 ( #23069, #7352, #30785 ),
 ( #15972, #27740, #17543 ),
 ( #20086, #17897, #10984 ),
 ( #5036, #26194, #23689 ),
 ( #15215, #4847, #28091 ),
 ( #2679, #7203, #27590 ) ),
 .UNSPECIFIED., .F., .F., .F. ) 
 B_SPLINE_SURFACE_WITH_KNOTS ( ( 4, 2, 2, 2, 2, 2, 2, 2, 4 ),
 ( 3, 3 ),
 ( 0.000000000000000000, 0.3926990816987241395, 0.7853981633974482790, 1.178097245096172418, 1.570796326794896558, 1.963495408493620697, 2.356194490192344837, 2.748893571891068976, 3.141592653589793116 ),
 ( 0.000000000000000000, 1.000000000000000000 ),
 .UNSPECIFIED. ) 
 GEOMETRIC_REPRESENTATION_ITEM ( )  RATIONAL_B_SPLINE_SURFACE ( (
 ( 1.000000000000000000, 0.8526401643540935105, 1.000000000000000000),
 ( 1.000000000000000000, 0.8526458704374199060, 1.000000000000000000),
 ( 1.000000000000000000, 0.8500048284159407164, 1.000000000000000000),
 ( 1.000000000000000000, 0.8396427561410217955, 1.000000000000000000),
 ( 1.000000000000000000, 0.8319131657169130944, 1.000000000000000000),
 ( 1.000000000000000000, 0.8119378018741435499, 1.000000000000000000),
 ( 1.000000000000000000, 0.7996867613998320801, 1.000000000000000000),
 ( 1.000000000000000000, 0.7717639430037522841, 1.000000000000000000),
 ( 1.000000000000000000, 0.7560862040295790454, 1.000000000000000000),
 ( 1.000000000000000000, 0.7231030986475501798, 1.000000000000000000),
 ( 1.000000000000000000, 0.7057963334870693828, 1.000000000000000000),
 ( 1.000000000000000000, 0.6721825289763700972, 1.000000000000000000),
 ( 1.000000000000000000, 0.6558905360689835096, 1.000000000000000000),
 ( 1.000000000000000000, 0.6276164863454245513, 1.000000000000000000),
 ( 1.000000000000000000, 0.6156781713470711459, 1.000000000000000000),
 ( 1.000000000000000000, 0.5992555908992014402, 1.000000000000000000),
 ( 1.000000000000000000, 0.5947841457457127001, 1.000000000000000000),
 ( 1.000000000000000000, 0.5948227867513392608, 1.000000000000000000) ) ) 
 REPRESENTATION_ITEM ( '' )  SURFACE ( )  );
#30527=ORIENTED_EDGE ( 'NONE', *, *, #8102, .T. ) ;
#30530=DIRECTION ( 'NONE',  ( 1.000000000000000000, 0.000000000000000000, 0.000000000000000000 ) ) ;
#30540=ORIENTED_EDGE ( 'NONE', *, *, #29897, .T. ) ;
#30542=FACE_OUTER_BOUND ( 'NONE', #12347, .T. ) ;
#30561=LINE ( 'NONE', #10478, #25761 ) ;
#30567=CARTESIAN_POINT ( 'NONE',  ( -56.71489992210280207, 0.2545037525615557183, -1.043529352691957124 ) ) ;
#30577=B_SPLINE_CURVE_WITH_KNOTS ( 'NONE', 3,
 ( #7699, #25055, #20230, #23241, #10176, #186, #30931 ),
 .UNSPECIFIED., .F., .F.,
 ( 4, 3, 4 ),
 ( 2.602085213965210256E-18, 0.002564119400760675634, 0.003456443488766134785 ),
 .UNSPECIFIED. ) ;
#30598=CYLINDRICAL_SURFACE ( 'NONE', #29552, 0.4500000000000025646 ) ;
#30600=AXIS2_PLACEMENT_3D ( 'NONE', #11209, #9366, #4188 ) ;
#30608=CARTESIAN_POINT ( 'NONE',  ( -23.54713438637982748, 3.520075575296777171, 1.500000000000000000 ) ) ;
#30624=AXIS2_PLACEMENT_3D ( 'NONE', #15863, #11173, #8197 ) ;
#30627=LINE ( 'NONE', #20738, #11362 ) ;
#30638=CARTESIAN_POINT ( 'NONE',  ( -23.54713438637982748, 8.763231220430828472, 1.786631099142472534 ) ) ;
#30640=CARTESIAN_POINT ( 'NONE',  ( -18.90002009650197934, 6.067137108840462645, 2.089261350533889061 ) ) ;
#30645=EDGE_CURVE ( 'NONE', #7325, #20999, #23249, .T. ) ;
#30652=VECTOR ( 'NONE', #12081, 1000.000000000000000 ) ;
#30658=VECTOR ( 'NONE', #4081, 1000.000000000000114 ) ;
#30666=CARTESIAN_POINT ( 'NONE',  ( -24.00476095649313635, 18.44930403746426961, 1.773314187735097747 ) ) ;
#30684=ORIENTED_EDGE ( 'NONE', *, *, #995, .F. ) ;
#30686=ORIENTED_EDGE ( 'NONE', *, *, #12845, .F. ) ;
#30688=CARTESIAN_POINT ( 'NONE',  ( 17.32050807568873552, 10.00000000000002309, 1.500000000000000000 ) ) ;
#30692=ADVANCED_FACE ( 'NONE', ( #24578 ), #27262, .T. ) ;
#30694=EDGE_CURVE ( 'NONE', #32393, #25811, #17224, .T. ) ;
#30702=DIRECTION ( 'NONE',  ( -4.458171167563057872E-29, 1.000000000000000000, 5.782411586589359611E-15 ) ) ;
#30703=CIRCLE ( 'NONE', #18933, 2.524999999999999911 ) ;
#30706=CARTESIAN_POINT ( 'NONE',  ( 7.577572045913243848, 15.00000000000000178, -4.612695725900422872 ) ) ;
#30723=VECTOR ( 'NONE', #15932, 1000.000000000000000 ) ;
#30742=DIRECTION ( 'NONE',  ( 0.4809547266710044178, 0.000000000000000000, 0.8767454310646958238 ) ) ;
#30744=CARTESIAN_POINT ( 'NONE',  ( -0.2059365608663963898, 0.000000000000000000, -4.131740999229418954 ) ) ;
#30748=CARTESIAN_POINT ( 'NONE',  ( -56.74498568481996585, 0.3183045829754697076, -1.046596361453495216 ) ) ;
#30754=CARTESIAN_POINT ( 'NONE',  ( 107.6037974194920679, 18.80702961649189575, 5.126032704575725241 ) ) ;
#30774=CARTESIAN_POINT ( 'NONE',  ( 107.4505081161385363, 17.92734912429073191, 4.774562840296773025 ) ) ;
#30781=ORIENTED_EDGE ( 'NONE', *, *, #6221, .T. ) ;
#30782=CARTESIAN_POINT ( 'NONE',  ( 10.90258948330155953, 17.51112508050605854, -4.612695725900421984 ) ) ;
#30783=CARTESIAN_POINT ( 'NONE',  ( 0.6708088701982989344, 0.000000000000000000, -4.612695725900422872 ) ) ;
#30785=CARTESIAN_POINT ( 'NONE',  ( -29.24806983202650557, 6.485688093852433944, 1.500000000000000000 ) ) ;
#30795=EDGE_CURVE ( 'NONE', #32393, #14212, #9663, .T. ) ;
#30800=CARTESIAN_POINT ( 'NONE',  ( 107.5519901325125716, 18.50907416150531049, -5.131959998105128484 ) ) ;
#30802=CARTESIAN_POINT ( 'NONE',  ( -21.11158745431430361, 4.499601903092431243, 2.132273290772896512 ) ) ;
#30812=CARTESIAN_POINT ( 'NONE',  ( -23.54713438637982748, 13.62472719076215988, 10.27593816114768011 ) ) ;
#30813=CARTESIAN_POINT ( 'NONE',  ( 25.25107927547938758, 18.67207037180926221, 1.049999999999822853 ) ) ;
#30819=DIRECTION ( 'NONE',  ( 0.9999770835954139292, -0.006769954505784861812, 0.000000000000000000 ) ) ;
#30827=ORIENTED_EDGE ( 'NONE', *, *, #29276, .T. ) ;
#30842=CARTESIAN_POINT ( 'NONE',  ( -50.81000000000000227, -10.96999999999998643, 1.949999999999999956 ) ) ;
#30845=CARTESIAN_POINT ( 'NONE',  ( -57.40374817251313999, -2.616512360834426953, 5.500000000000000000 ) ) ;
#30848=CARTESIAN_POINT ( 'NONE',  ( 2.619288827430985567, 0.4094970184090461762, -1.491740999229418829 ) ) ;
#30857=DIRECTION ( 'NONE',  ( 0.000000000000000000, 0.000000000000000000, 1.000000000000000000 ) ) ;
#30859=LINE ( 'NONE', #7779, #30723 ) ;
#30869=CARTESIAN_POINT ( 'NONE',  ( 9.187365643239736812, 0.07845480144325966965, -1.031721989605145051 ) ) ;
#30873=ADVANCED_FACE ( 'NONE', ( #3678 ), #26085, .F. ) ;
#30874=ORIENTED_EDGE ( 'NONE', *, *, #20462, .T. ) ;
#30882=ORIENTED_EDGE ( 'NONE', *, *, #8073, .T. ) ;
#30885=EDGE_LOOP ( 'NONE', ( #31226, #16246, #13130, #20036 ) ) ;
#30886=CARTESIAN_POINT ( 'NONE',  ( 18.91213585445015610, 14.46970239064985719, 1.050000000000000044 ) ) ;
#30887=FACE_OUTER_BOUND ( 'NONE', #22081, .T. ) ;
#30900=EDGE_CURVE ( 'NONE', #4370, #13391, #22577, .T. ) ;
#30904=CARTESIAN_POINT ( 'NONE',  ( 108.0895235638783163, 18.67666245286735105, 4.597069131703993783 ) ) ;
#30914=CARTESIAN_POINT ( 'NONE',  ( 9.295257658903679499, 0.2358351158402515468, 1.049999985396302904 ) ) ;
#30921=CARTESIAN_POINT ( 'NONE',  ( -30.51827900900860158, 4.402097243136374516, 5.049999999999999822 ) ) ;
#30931=CARTESIAN_POINT ( 'NONE',  ( 107.6996442589673819, 19.35565155597529596, -4.612695725900422872 ) ) ;
#30944=ORIENTED_EDGE ( 'NONE', *, *, #21404, .T. ) ;
#30955=VERTEX_POINT ( 'NONE', #19710 ) ;
#30956=DIRECTION ( 'NONE',  ( 0.000000000000000000, 1.000000000000000000, 0.000000000000000000 ) ) ;
#30957=CARTESIAN_POINT ( 'NONE',  ( 22.17513219109303080, 17.52220421518676829, 1.500000000000000000 ) ) ;
#30960=DIRECTION ( 'NONE',  ( 0.000000000000000000, 0.000000000000000000, 1.000000000000000000 ) ) ;
#30963=ORIENTED_EDGE ( 'NONE', *, *, #13539, .T. ) ;
#30966=CARTESIAN_POINT ( 'NONE',  ( -29.87068905793955409, 13.45819068726228984, 1.895815882016619991 ) ) ;
#30988=ORIENTED_EDGE ( 'NONE', *, *, #3048, .F. ) ;
#30993=EDGE_CURVE ( 'NONE', #21159, #32554, #32092, .T. ) ;
#31009=CARTESIAN_POINT ( 'NONE',  ( -30.13448816962999643, 4.180515498708627931, 5.128141679950118714 ) ) ;
#31016=CARTESIAN_POINT ( 'NONE',  ( 13.56178860298438593, 21.92012725262058481, -1.183869197697829279 ) ) ;
#31032=CARTESIAN_POINT ( 'NONE',  ( -2.794738735352966685, 0.000000000000000000, 1.508259000770582059 ) ) ;
#31037=CARTESIAN_POINT ( 'NONE',  ( 26.08945412691624099, 19.05746434167065928, 1.050000000000000044 ) ) ;
#31040=EDGE_CURVE ( 'NONE', #10337, #20196, #10301, .T. ) ;
#31051=CARTESIAN_POINT ( 'NONE',  ( 108.2850536699472883, 19.76545123595448672, 0.4463807625373348298 ) ) ;
#31097=VECTOR ( 'NONE', #7163, 1000.000000000000000 ) ;
#31110=EDGE_LOOP ( 'NONE', ( #16951, #22232, #14570, #13283 ) ) ;
#31112=TOROIDAL_SURFACE ( 'NONE', #3359, 9.269952810656748809, 0.4500000000000000111 ) ;
#31126=VECTOR ( 'NONE', #7730, 1000.000000000000227 ) ;
#31127=ORIENTED_EDGE ( 'NONE', *, *, #18107, .T. ) ;
#31135=CARTESIAN_POINT ( 'NONE',  ( 20.31145943757101335, 16.24075847989571386, -1.499999999999999556 ) ) ;
#31137=CARTESIAN_POINT ( 'NONE',  ( 5.865515302491333571, 15.00000000000002132, 1.508259000770582059 ) ) ;
#31146=VECTOR ( 'NONE', #29560, 1000.000000000000000 ) ;
#31152=AXIS2_PLACEMENT_3D ( 'NONE', #22628, #17578, #27781 ) ;
#31162=CARTESIAN_POINT ( 'NONE',  ( 108.1104793158158230, 18.79335234840002400, -4.459574495179032816 ) ) ;
#31167=CARTESIAN_POINT ( 'NONE',  ( 9.282537329959740902, 0.2172754300396697036, 1.050000000000000044 ) ) ;
#31172=DIRECTION ( 'NONE',  ( -4.458171167563057872E-29, 1.000000000000000000, 5.782411586589359611E-15 ) ) ;
#31180=DIRECTION ( 'NONE',  ( -0.000000000000000000, -0.000000000000000000, -1.000000000000000000 ) ) ;
#31205=DIRECTION ( 'NONE',  ( 0.000000000000000000, 0.000000000000000000, -1.000000000000000000 ) ) ;
#31208=ORIENTED_EDGE ( 'NONE', *, *, #618, .F. ) ;
#31211=CARTESIAN_POINT ( 'NONE',  ( -41.30970132048468457, -16.45499999999997343, 1.500000000000000000 ) ) ;
#31213=FACE_OUTER_BOUND ( 'NONE', #19126, .T. ) ;
#31226=ORIENTED_EDGE ( 'NONE', *, *, #22071, .F. ) ;
#31227=CYLINDRICAL_SURFACE ( 'NONE', #14418, 0.4499999999999990119 ) ;
#31255=VERTEX_POINT ( 'NONE', #6258 ) ;
#31268=DIRECTION ( 'NONE',  ( -0.000000000000000000, -0.000000000000000000, -1.000000000000000000 ) ) ;
#31269=ORIENTED_EDGE ( 'NONE', *, *, #18345, .F. ) ;
#31273=DIRECTION ( 'NONE',  ( 0.000000000000000000, -0.9271838545667856479, -0.3746065934159163446 ) ) ;
#31277=ORIENTED_EDGE ( 'NONE', *, *, #32437, .T. ) ;
#31279=ADVANCED_FACE ( 'NONE', ( #8923 ), #11340, .T. ) ;
#31282=CARTESIAN_POINT ( 'NONE',  ( -53.35155202832373078, 4.402097243136376292, 5.050000000000000711 ) ) ;
#31284=ORIENTED_EDGE ( 'NONE', *, *, #9278, .T. ) ;
#31287=DIRECTION ( 'NONE',  ( 0.000000000000000000, 1.000000000000000000, 0.000000000000000000 ) ) ;
#31299=CARTESIAN_POINT ( 'NONE',  ( 17.56297300373453041, 13.04222886866727826, 1.499999999999999112 ) ) ;
#31304=VERTEX_POINT ( 'NONE', #24316 ) ;
#31305=CARTESIAN_POINT ( 'NONE',  ( -59.37247738224319704, -6.026451378431818107, 5.049999999999999822 ) ) ;
#31311=DIRECTION ( 'NONE',  ( 0.000000000000000000, -0.9848077530122079093, -0.1736481776669314414 ) ) ;
#31318=CARTESIAN_POINT ( 'NONE',  ( 108.0375581208015205, 18.38729836123134831, -4.602450496903218280 ) ) ;
#31347=CARTESIAN_POINT ( 'NONE',  ( 107.7530755790422319, 16.80318731729154891, 2.547137921104602132 ) ) ;
#31362=ORIENTED_EDGE ( 'NONE', *, *, #8704, .F. ) ;
#31378=ADVANCED_FACE ( 'NONE', ( #27809 ), #4924, .F. ) ;
#31382=DIRECTION ( 'NONE',  ( 0.4999999999999977796, 0.8660254037844398178, 0.000000000000000000 ) ) ;
#31386=ORIENTED_EDGE ( 'NONE', *, *, #14721, .T. ) ;
#31388=CARTESIAN_POINT ( 'NONE',  ( 108.1863001008973555, 19.21555239728606779, 4.746593323837460687 ) ) ;
#31398=CARTESIAN_POINT ( 'NONE',  ( 11.90652295052632503, 20.12228623747235901, 4.629213727441584325 ) ) ;
#31399=ORIENTED_EDGE ( 'NONE', *, *, #11569, .F. ) ;
#31407=CARTESIAN_POINT ( 'NONE',  ( 108.3696618535068126, 20.23658298680886958, 1.395260099363828665 ) ) ;
#31410=ORIENTED_EDGE ( 'NONE', *, *, #8473, .T. ) ;
#31414=LINE ( 'NONE', #13814, #24753 ) ;
#31436=DIRECTION ( 'NONE',  ( -0.4809547266710045288, -0.000000000000000000, -0.8767454310646958238 ) ) ;
#31440=CARTESIAN_POINT ( 'NONE',  ( 13.23256811278013778, 7.534661545873150068, -1.499999999999999778 ) ) ;
#31443=CARTESIAN_POINT ( 'NONE',  ( 9.302055952181040865, 0.2457637073014104223, 1.500000000000000000 ) ) ;
#31450=CARTESIAN_POINT ( 'NONE',  ( -27.70354918513814368, 5.575484043998305772, 2.102665754804134313 ) ) ;
#31454=CARTESIAN_POINT ( 'NONE',  ( 16.10106094948405797, 19.71584668020019038, 5.412820279296879811 ) ) ;
#31457=CARTESIAN_POINT ( 'NONE',  ( -60.22964952008683781, -5.531562813905958720, 2.028141679950118625 ) ) ;
#31463=CYLINDRICAL_SURFACE ( 'NONE', #12259, 0.4500000000000025646 ) ;
#31470=CARTESIAN_POINT ( 'NONE',  ( -50.81000000000000227, -10.96999999999998643, 1.949999999999999956 ) ) ;
#31471=ORIENTED_EDGE ( 'NONE', *, *, #20462, .F. ) ;
#31472=EDGE_LOOP ( 'NONE', ( #13921, #30489, #9725, #3001 ) ) ;
#31474=ADVANCED_FACE ( 'NONE', ( #13400 ), #5247, .T. ) ;
#31476=CARTESIAN_POINT ( 'NONE',  ( 107.9391920281211839, 17.83955714378018342, 3.608571156949641257 ) ) ;
#31477=ORIENTED_EDGE ( 'NONE', *, *, #8102, .F. ) ;
#31478=CARTESIAN_POINT ( 'NONE',  ( 16.86324541463584481, 12.23239806835116816, -1.499999999999407585 ) ) ;
#31481=EDGE_CURVE ( 'NONE', #4711, #18415, #9174, .T. ) ;
#31492=AXIS2_PLACEMENT_3D ( 'NONE', #10931, #1048, #10749 ) ;
#31496=CARTESIAN_POINT ( 'NONE',  ( 12.84707270680543267, 21.67305773080836673, -1.472686733844490004 ) ) ;
#31526=CARTESIAN_POINT ( 'NONE',  ( -31.80940264096945924, 1.734723475976807094E-15, 0.000000000000000000 ) ) ;
#31527=CARTESIAN_POINT ( 'NONE',  ( 79.92595492699416582, 21.43178168691304819, 1.508259000770581393 ) ) ;
#31541=VECTOR ( 'NONE', #26465, 1000.000000000000000 ) ;
#31542=CARTESIAN_POINT ( 'NONE',  ( 9.578960313758919654, 17.92714876365089793, -5.396302277755719246 ) ) ;
#31547=EDGE_LOOP ( 'NONE', ( #21208, #23995, #20612, #26921 ) ) ;
#31555=CIRCLE ( 'NONE', #5404, 302.4235430809786749 ) ;
#31563=CARTESIAN_POINT ( 'NONE',  ( 26.08945412691624099, 19.05746434167065928, -1.050000000000000044 ) ) ;
#31580=AXIS2_PLACEMENT_3D ( 'NONE', #17167, #27378, #20837 ) ;
#31582=CARTESIAN_POINT ( 'NONE',  ( -58.35512979123338084, -4.055258467324091676, 5.700934511681459149 ) ) ;
#31609=ORIENTED_EDGE ( 'NONE', *, *, #28300, .F. ) ;
#31612=CARTESIAN_POINT ( 'NONE',  ( 16.87315779114032566, 12.21951710881648090, 1.499999999999999112 ) ) ;
#31615=AXIS2_PLACEMENT_3D ( 'NONE', #9700, #11552, #9201 ) ;
#31635=TOROIDAL_SURFACE ( 'NONE', #8064, 5.587650971692158741, 0.4500000000000000111 ) ;
#31655=CARTESIAN_POINT ( 'NONE',  ( -45.71000000000000085, -10.96999999999998643, 5.700000000000000178 ) ) ;
#31658=PLANE ( 'NONE',  #30045 ) ;
#31688=CARTESIAN_POINT ( 'NONE',  ( 17.32050807568873552, 10.00000000000002309, -1.491740999229417941 ) ) ;
#31707=CARTESIAN_POINT ( 'NONE',  ( -56.77654246901312263, 0.4654628299899072896, 1.959872961020660664 ) ) ;
#31716=AXIS2_PLACEMENT_3D ( 'NONE', #7079, #2069, #17438 ) ;
#31720=CARTESIAN_POINT ( 'NONE',  ( 107.6996442589673819, 19.35565155597529596, -4.612695725900422872 ) ) ;
#31728=CARTESIAN_POINT ( 'NONE',  ( 13.41780342409107973, 19.07609913100965571, -4.612695725900421984 ) ) ;
#31739=CARTESIAN_POINT ( 'NONE',  ( 11.61992484759235644, 3.867395925924771660, -1.050000000000000044 ) ) ;
#31744=CARTESIAN_POINT ( 'NONE',  ( 9.192617927958339763, 0.08611596088385452263, 1.322472180770052352 ) ) ;
#31754=AXIS2_PLACEMENT_3D ( 'NONE', #22853, #1981, #25372 ) ;
#31765=ADVANCED_FACE ( 'NONE', ( #11417 ), #13942, .F. ) ;
#31789=CARTESIAN_POINT ( 'NONE',  ( 0.000000000000000000, 0.000000000000000000, 1.500000000000000000 ) ) ;
#31792=( BOUNDED_SURFACE ( )  B_SPLINE_SURFACE ( 3, 1, ( 
 ( #5749, #21282 ),
 ( #25990, #11083 ),
 ( #2755, #20795 ),
 ( #8082, #7923 ) ),
 .UNSPECIFIED., .F., .F., .F. ) 
 B_SPLINE_SURFACE_WITH_KNOTS ( ( 4, 4 ),
 ( 2, 2 ),
 ( 0.000000000000000000, 1.000000000000000000 ),
 ( 0.000000000000000000, 1.000000000000000000 ),
 .UNSPECIFIED. ) 
 GEOMETRIC_REPRESENTATION_ITEM ( )  RATIONAL_B_SPLINE_SURFACE ( (
 ( 1.000000000000000000, 1.000000000000000000),
 ( 0.6539698177806696489, 0.6539698177806696489),
 ( 0.6539698177806696489, 0.6539698177806696489),
 ( 1.000000000000000000, 1.000000000000000000) ) ) 
 REPRESENTATION_ITEM ( '' )  SURFACE ( )  );
#31809=CARTESIAN_POINT ( 'NONE',  ( 15.84732276226623604, 14.44600775457921493, -1.050000000000000044 ) ) ;
#31815=CARTESIAN_POINT ( 'NONE',  ( 108.0068349480237515, 18.21621961241920573, 4.414771370926588112 ) ) ;
#31819=CARTESIAN_POINT ( 'NONE',  ( 16.86324541396879795, 12.23239806884165581, -1.050000000000000044 ) ) ;
#31820=CARTESIAN_POINT ( 'NONE',  ( -2.726590971468680458, 0.1614173311939631483, -1.446082916213561553 ) ) ;
#31832=CARTESIAN_POINT ( 'NONE',  ( -23.54713438637983103, 11.18299864920563103, 1.403377589220444088 ) ) ;
#31835=ADVANCED_FACE ( 'NONE', ( #29958 ), #16912, .T. ) ;
#31837=LINE ( 'NONE', #14397, #30658 ) ;
#31842=ORIENTED_EDGE ( 'NONE', *, *, #16142, .F. ) ;
#31856=CARTESIAN_POINT ( 'NONE',  ( -42.85764933975779201, 24.74387538314362800, 1.500000000000000000 ) ) ;
#31867=CARTESIAN_POINT ( 'NONE',  ( 11.90652295052632503, 20.12228623747236256, -4.612695725900421984 ) ) ;
#31885=ORIENTED_EDGE ( 'NONE', *, *, #10481, .F. ) ;
#31892=CARTESIAN_POINT ( 'NONE',  ( 9.331062908042598636, 15.00000000000002132, 4.629213727441584325 ) ) ;
#31903=CARTESIAN_POINT ( 'NONE',  ( -50.81000000000000227, -10.96999999999998643, 5.949999999999999289 ) ) ;
#31916=CARTESIAN_POINT ( 'NONE',  ( -47.25352234179201361, 16.22999999999998266, -1.500000000000000000 ) ) ;
#31926=ORIENTED_EDGE ( 'NONE', *, *, #15755, .T. ) ;
#31951=CARTESIAN_POINT ( 'NONE',  ( -30.24316686125445131, 12.14507408406858779, 1.500000000000003109 ) ) ;
#31974=CARTESIAN_POINT ( 'NONE',  ( 8.930755659325139817, 0.4999999999999980571, -1.500000000000000000 ) ) ;
#32014=CARTESIAN_POINT ( 'NONE',  ( -56.76080480439498643, 0.3612510994447631907, 1.709681292476414649 ) ) ;
#32047=CARTESIAN_POINT ( 'NONE',  ( 25.10659403416954660, 18.61493763628891784, -1.050000000000000266 ) ) ;
#32053=CARTESIAN_POINT ( 'NONE',  ( 9.236821176939054467, 0.1505923090604429360, 1.036667534179766648 ) ) ;
#32059=FACE_OUTER_BOUND ( 'NONE', #23744, .T. ) ;
#32060=CIRCLE ( 'NONE', #18704, 8.025310301077755781 ) ;
#32075=AXIS2_PLACEMENT_3D ( 'NONE', #19223, #6840, #24244 ) ;
#32081=CARTESIAN_POINT ( 'NONE',  ( 107.9275968081481238, 17.77499038371485440, -4.611092782519711442 ) ) ;
#32087=EDGE_CURVE ( 'NONE', #28296, #2170, #32938, .T. ) ;
#32089=EDGE_CURVE ( 'NONE', #1782, #17721, #8127, .T. ) ;
#32090=AXIS2_PLACEMENT_3D ( 'NONE', #6863, #17052, #4378 ) ;
#32092=LINE ( 'NONE', #16705, #22045 ) ;
#32105=DIRECTION ( 'NONE',  ( 0.000000000000000000, -0.000000000000000000, 1.000000000000000000 ) ) ;
#32117=DIRECTION ( 'NONE',  ( 1.000000000000000000, 0.000000000000000000, 0.000000000000000000 ) ) ;
#32118=FACE_OUTER_BOUND ( 'NONE', #9797, .T. ) ;
#32128=CIRCLE ( 'NONE', #30009, 10.64228691119593151 ) ;
#32133=ORIENTED_EDGE ( 'NONE', *, *, #30354, .T. ) ;
#32137=CIRCLE ( 'NONE', #28898, 9.269952810656748809 ) ;
#32147=VECTOR ( 'NONE', #12298, 1000.000000000000000 ) ;
#32155=VERTEX_POINT ( 'NONE', #16549 ) ;
#32159=AXIS2_PLACEMENT_3D ( 'NONE', #2096, #24985, #14633 ) ;
#32161=DIRECTION ( 'NONE',  ( 1.000000000000000000, 0.000000000000000000, 0.000000000000000000 ) ) ;
#32169=CARTESIAN_POINT ( 'NONE',  ( -54.06000000000000227, -10.96999999999998643, 5.700000000000000178 ) ) ;
#32180=ORIENTED_EDGE ( 'NONE', *, *, #8308, .T. ) ;
#32183=ORIENTED_EDGE ( 'NONE', *, *, #19034, .F. ) ;
#32192=EDGE_LOOP ( 'NONE', ( #25408, #12167, #28354, #934, #13614 ) ) ;
#32201=CARTESIAN_POINT ( 'NONE',  ( -56.77537022611499395, 0.4514244267945254907, 2.028141679927229379 ) ) ;
#32219=AXIS2_PLACEMENT_3D ( 'NONE', #17717, #17232, #14356 ) ;
#32228=CARTESIAN_POINT ( 'NONE',  ( 107.1769020805352142, 16.40214705320008903, 1.508259000770581615 ) ) ;
#32240=DIRECTION ( 'NONE',  ( 0.000000000000000000, -0.9271838545667856479, -0.3746065934159163446 ) ) ;
#32244=CARTESIAN_POINT ( 'NONE',  ( 8.878230740118540965, 0.000000000000000000, 1.080849929302613033 ) ) ;
#32252=ADVANCED_FACE ( 'NONE', ( #27443 ), #24411, .T. ) ;
#32261=CARTESIAN_POINT ( 'NONE',  ( -28.03476286530682771, 5.886549661986336446, 2.094166778015133623 ) ) ;
#32267=( BOUNDED_SURFACE ( )  B_SPLINE_SURFACE ( 1, 3, ( 
 ( #24863, #2478, #9821, #32563 ),
 ( #20039, #30233, #27692, #12647 ) ),
 .UNSPECIFIED., .F., .F., .F. ) 
 B_SPLINE_SURFACE_WITH_KNOTS ( ( 2, 2 ),
 ( 4, 4 ),
 ( 0.000000000000000000, 1.000000000000000000 ),
 ( 0.000000000000000000, 1.000000000000000000 ),
 .UNSPECIFIED. ) 
 GEOMETRIC_REPRESENTATION_ITEM ( )  RATIONAL_B_SPLINE_SURFACE ( (
 ( 1.000000000000000000, 0.9917560313531952332, 0.9917560313531952332, 1.000000000000000000),
 ( 1.000000000000000000, 0.9917560313531952332, 0.9917560313531952332, 1.000000000000000000) ) ) 
 REPRESENTATION_ITEM ( '' )  SURFACE ( )  );
#32274=CYLINDRICAL_SURFACE ( 'NONE', #28958, 302.4235430809786180 ) ;
#32300=DIRECTION ( 'NONE',  ( -0.4999999999999960032, -0.8660254037844409281, 0.000000000000000000 ) ) ;
#32307=DIRECTION ( 'NONE',  ( 1.000000000000000000, 0.000000000000000000, 0.000000000000000000 ) ) ;
#32313=AXIS2_PLACEMENT_3D ( 'NONE', #29926, #17226, #2175 ) ;
#32314=CARTESIAN_POINT ( 'NONE',  ( 5.865515302491369098, 15.00000000000000000, 1.500000000000000000 ) ) ;
#32323=CARTESIAN_POINT ( 'NONE',  ( 8.911384905465473238, 0.2172754300402719996, 1.412391582771868492 ) ) ;
#32325=EDGE_LOOP ( 'NONE', ( #8861, #16018, #22117, #11600, #19700, #9568, #30392, #13786, #10957 ) ) ;
#32330=ORIENTED_EDGE ( 'NONE', *, *, #10311, .T. ) ;
#32331=CARTESIAN_POINT ( 'NONE',  ( 26.04661131027748056, 19.53168319095744465, -1.500000000000000000 ) ) ;
#32348=CARTESIAN_POINT ( 'NONE',  ( -50.81000000000000227, -10.96999999999998643, 1.500000000000000000 ) ) ;
#32350=ORIENTED_EDGE ( 'NONE', *, *, #7994, .F. ) ;
#32358=ORIENTED_EDGE ( 'NONE', *, *, #16629, .F. ) ;
#32377=CARTESIAN_POINT ( 'NONE',  ( -38.14293509397970183, 21.49000000000000199, 1.050000000000000044 ) ) ;
#32379=CARTESIAN_POINT ( 'NONE',  ( 24.72695737054825926, 18.91229966141139229, -1.500000000000000000 ) ) ;
#32382=ORIENTED_EDGE ( 'NONE', *, *, #11145, .F. ) ;
#32386=EDGE_LOOP ( 'NONE', ( #24145, #12839 ) ) ;
#32393=VERTEX_POINT ( 'NONE', #18057 ) ;
#32395=CARTESIAN_POINT ( 'NONE',  ( 13.24625820531402631, 6.653948736490935545, -1.050000000000000044 ) ) ;
#32396=CARTESIAN_POINT ( 'NONE',  ( 8.930755659325141593, 0.5000000000000086597, -1.500000000000000000 ) ) ;
#32402=CARTESIAN_POINT ( 'NONE',  ( 56.97280603064898941, -277.2763395528616002, 4.629213727441584325 ) ) ;
#32411=FACE_OUTER_BOUND ( 'NONE', #509, .T. ) ;
#32418=ORIENTED_EDGE ( 'NONE', *, *, #20622, .F. ) ;
#32423=DIRECTION ( 'NONE',  ( 0.000000000000000000, -1.000000000000000000, 0.000000000000000000 ) ) ;
#32425=CARTESIAN_POINT ( 'NONE',  ( -59.58387603396901966, -5.539140460716925674, 5.221328934740562033 ) ) ;
#32431=DIRECTION ( 'NONE',  ( 0.4999999999999977796, 0.8660254037844398178, 0.000000000000000000 ) ) ;
#32437=EDGE_CURVE ( 'NONE', #17424, #8184, #10029, .T. ) ;
#32442=EDGE_LOOP ( 'NONE', ( #25471, #12103, #20755, #26533, #1529 ) ) ;
#32448=CARTESIAN_POINT ( 'NONE',  ( 13.28821369005689945, 21.83086517065485666, 1.350282695622831319 ) ) ;
#32451=CARTESIAN_POINT ( 'NONE',  ( 107.4160271293911251, 17.73379232341987333, 4.360465883803716913 ) ) ;
#32455=FACE_OUTER_BOUND ( 'NONE', #27090, .T. ) ;
#32458=EDGE_CURVE ( 'NONE', #23049, #9305, #9741, .T. ) ;
#32471=CARTESIAN_POINT ( 'NONE',  ( -23.54713438637982748, 3.520075575296777171, 2.000000000000000000 ) ) ;
#32487=ORIENTED_EDGE ( 'NONE', *, *, #15727, .F. ) ;
#32494=CARTESIAN_POINT ( 'NONE',  ( 0.6708088701982989344, 0.000000000000000000, 4.629213727441584325 ) ) ;
#32514=ADVANCED_FACE ( 'NONE', ( #18401 ), #17220, .T. ) ;
#32515=VERTEX_POINT ( 'NONE', #10865 ) ;
#32518=ORIENTED_EDGE ( 'NONE', *, *, #25791, .F. ) ;
#32526=EDGE_CURVE ( 'NONE', #12740, #2610, #20893, .T. ) ;
#32536=DIRECTION ( 'NONE',  ( -1.000000000000000000, -1.369475477426764022E-16, 0.000000000000000000 ) ) ;
#32554=VERTEX_POINT ( 'NONE', #11356 ) ;
#32563=CARTESIAN_POINT ( 'NONE',  ( 110.8079127523828618, 15.75827621748124940, -1.491740999229419273 ) ) ;
#32581=EDGE_CURVE ( 'NONE', #436, #21704, #9595, .T. ) ;
#32600=VERTEX_POINT ( 'NONE', #1344 ) ;
#32607=EDGE_LOOP ( 'NONE', ( #9123, #19743, #11740 ) ) ;
#32612=CIRCLE ( 'NONE', #28871, 10.19912342234043834 ) ;
#32620=ORIENTED_EDGE ( 'NONE', *, *, #3629, .F. ) ;
#32623=AXIS2_PLACEMENT_3D ( 'NONE', #1535, #17248, #27450 ) ;
#32631=ORIENTED_EDGE ( 'NONE', *, *, #28245, .F. ) ;
#32635=DIRECTION ( 'NONE',  ( 1.000000000000000000, 0.000000000000000000, 0.000000000000000000 ) ) ;
#32636=CIRCLE ( 'NONE', #26746, 9.269952810656748809 ) ;
#32642=CARTESIAN_POINT ( 'NONE',  ( 8.900602013106571064, 0.09531162291654594887, -1.304562659182835871 ) ) ;
#32661=VERTEX_POINT ( 'NONE', #17189 ) ;
#32679=ORIENTED_EDGE ( 'NONE', *, *, #15821, .F. ) ;
#32681=ADVANCED_FACE ( 'NONE', ( #26719 ), #23920, .T. ) ;
#32685=VERTEX_POINT ( 'NONE', #29587 ) ;
#32686=CARTESIAN_POINT ( 'NONE',  ( -56.77769102277633095, 0.5030464795276025081, -1.050000000000000044 ) ) ;
#32693=CARTESIAN_POINT ( 'NONE',  ( 107.7673897845259461, 19.73285661471971508, 3.823381474136016145 ) ) ;
#32702=ADVANCED_FACE ( 'NONE', ( #22053 ), #32274, .T. ) ;
#32714=DIRECTION ( 'NONE',  ( -0.000000000000000000, -0.000000000000000000, -1.000000000000000000 ) ) ;
#32723=ORIENTED_EDGE ( 'NONE', *, *, #7935, .F. ) ;
#32725=VECTOR ( 'NONE', #23248, 1000.000000000000227 ) ;
#32728=ORIENTED_EDGE ( 'NONE', *, *, #346, .T. ) ;
#32731=CARTESIAN_POINT ( 'NONE',  ( 8.917264641016661386, 0.3030370628138376321, -1.471187449996646190 ) ) ;
#32733=CARTESIAN_POINT ( 'NONE',  ( -54.06000000000000227, -10.96999999999998643, 9.000000000000000000 ) ) ;
#32735=DIRECTION ( 'NONE',  ( 0.000000000000000000, 0.000000000000000000, 1.000000000000000000 ) ) ;
#32741=PRODUCT ( 'Part2_handle2', 'Part2_handle2', '', ( #14647 ) ) ;
#32742=DIRECTION ( 'NONE',  ( -0.2880220749472530706, -0.1662896225033516362, 0.9430753128943475394 ) ) ;
#32747=VECTOR ( 'NONE', #384, 1000.000000000000000 ) ;
#32751=CARTESIAN_POINT ( 'NONE',  ( -56.75720195825324765, 0.3530522875096756552, -1.047845628850368582 ) ) ;
#32760=DIRECTION ( 'NONE',  ( 0.000000000000000000, -0.000000000000000000, -1.000000000000000000 ) ) ;
#32765=ORIENTED_EDGE ( 'NONE', *, *, #2417, .F. ) ;
#32776=DIRECTION ( 'NONE',  ( -0.8660254037844409281, 0.4999999999999960587, 0.000000000000000000 ) ) ;
#32783=CYLINDRICAL_SURFACE ( 'NONE', #26713, 3.250000000000002665 ) ;
#32792=CARTESIAN_POINT ( 'NONE',  ( 23.80188655377674323, 18.45496240403558019, 1.500000000000000222 ) ) ;
#32799=CARTESIAN_POINT ( 'NONE',  ( -29.33353502638487953, 7.575402792874002422, 2.048453119712660087 ) ) ;
#32812=CARTESIAN_POINT ( 'NONE',  ( 107.9511351265079782, 17.90606102802182420, -4.842550456795976288 ) ) ;
#32822=CARTESIAN_POINT ( 'NONE',  ( 23.82349779645404553, 17.94250544646148882, -1.499999999999882316 ) ) ;
#32839=CARTESIAN_POINT ( 'NONE',  ( 14.23800746264080885, 22.11259878822730229, 1.508259000770582059 ) ) ;
#32851=ORIENTED_EDGE ( 'NONE', *, *, #1409, .T. ) ;
#32864=DIRECTION ( 'NONE',  ( -0.4809547266710039182, 0.000000000000000000, 0.8767454310646960458 ) ) ;
#32868=DIRECTION ( 'NONE',  ( -1.000000000000000000, -5.263081354843156381E-15, 0.000000000000000000 ) ) ;
#32874=( BOUNDED_SURFACE ( )  B_SPLINE_SURFACE ( 3, 2, ( 
 ( #29, #10214, #7731 ),
 ( #12393, #25778, #20436 ),
 ( #17923, #2905, #30813 ),
 ( #20757, #18073, #5373 ),
 ( #13068, #371, #10546 ),
 ( #30957, #28450, #25091 ),
 ( #9897, #23755, #3544 ),
 ( #13850, #21582, #29256 ),
 ( #13702, #11381, #3202 ),
 ( #21097, #18424, #28614 ),
 ( #21402, #31299, #10702 ),
 ( #8371, #31612, #15888 ),
 ( #8521, #24056, #13363 ),
 ( #18568, #5708, #26445 ),
 ( #28760, #13546, #1182 ),
 ( #3380, #868, #26097 ),
 ( #23904, #11196, #15743 ),
 ( #23576, #10890, #5850 ),
 ( #3691, #16034, #26265 ),
 ( #699, #23412, #11047 ),
 ( #1012, #21245, #8699 ),
 ( #25946, #31443, #18722 ) ),
 .UNSPECIFIED., .F., .F., .F. ) 
 B_SPLINE_SURFACE_WITH_KNOTS ( ( 4, 2, 2, 2, 2, 2, 2, 2, 2, 2, 4 ),
 ( 3, 3 ),
 ( 0.004062408222415266751, 0.005697251201790947198, 0.007332094181166628512, 0.01060178013991799027, 0.01387146609866935290, 0.01550630907804503335, 0.01714115205742071379, 0.02041083801617207816, 0.02368052397492343905, 0.02695020993367479994, 0.03021989589242616431 ),
 ( 0.000000000000000000, 1.000000000000000000 ),
 .UNSPECIFIED. ) 
 GEOMETRIC_REPRESENTATION_ITEM ( )  RATIONAL_B_SPLINE_SURFACE ( (
 ( 1.000000000000000000, 0.7071067811865475727, 1.000000000000000000),
 ( 1.000000000000000000, 0.7071067811865475727, 1.000000000000000000),
 ( 1.000000000000000000, 0.7071067811865475727, 1.000000000000000000),
 ( 1.000000000000000000, 0.7071067811865475727, 1.000000000000000000),
 ( 1.000000000000000000, 0.7071067811865475727, 1.000000000000000000),
 ( 1.000000000000000000, 0.7071067811865475727, 1.000000000000000000),
 ( 1.000000000000000000, 0.7071067811865475727, 1.000000000000000000),
 ( 1.000000000000000000, 0.7071067811865475727, 1.000000000000000000),
 ( 1.000000000000000000, 0.7071067811865475727, 1.000000000000000000),
 ( 1.000000000000000000, 0.7071067811865475727, 1.000000000000000000),
 ( 1.000000000000000000, 0.7071067811865483499, 1.000000000000000000),
 ( 1.000000000000000000, 0.7071067811865483499, 1.000000000000000000),
 ( 1.000000000000000000, 0.7071067811865475727, 1.000000000000000000),
 ( 1.000000000000000000, 0.7071067811865475727, 1.000000000000000000),
 ( 1.000000000000000000, 0.7071067811865475727, 1.000000000000000000),
 ( 1.000000000000000000, 0.7071067811865475727, 1.000000000000000000),
 ( 1.000000000000000000, 0.7071067811865475727, 1.000000000000000000),
 ( 1.000000000000000000, 0.7071067811865475727, 1.000000000000000000),
 ( 1.000000000000000000, 0.7071067811865475727, 1.000000000000000000),
 ( 1.000000000000000000, 0.7071067811865475727, 1.000000000000000000),
 ( 1.000000000000000000, 0.7071067811865475727, 1.000000000000000000),
 ( 1.000000000000000000, 0.7071067811865475727, 1.000000000000000000) ) ) 
 REPRESENTATION_ITEM ( '' )  SURFACE ( )  );
#32882=ORIENTED_EDGE ( 'NONE', *, *, #822, .T. ) ;
#32893=DIRECTION ( 'NONE',  ( -0.09975574163943223827, 0.1727820128662104493, -0.9798954883250904357 ) ) ;
#32896=CARTESIAN_POINT ( 'NONE',  ( -23.54713438637982748, 3.263167658947396799, 6.089596369742212190 ) ) ;
#32908=CARTESIAN_POINT ( 'NONE',  ( -23.54713438637982748, 8.275374457817619600, 8.600000000000004974 ) ) ;
#32911=CARTESIAN_POINT ( 'NONE',  ( -56.52933573942885204, 0.04063196321577920711, -1.249307687641485476 ) ) ;
#32921=DIRECTION ( 'NONE',  ( 0.000000000000000000, -0.9876883405951383255, 0.1564344650402271775 ) ) ;
#32925=VERTEX_POINT ( 'NONE', #20708 ) ;
#32938=LINE ( 'NONE', #28076, #22545 ) ;
#32945=ORIENTED_EDGE ( 'NONE', *, *, #6395, .F. ) ;
#32949=CARTESIAN_POINT ( 'NONE',  ( 9.331062908042598636, 15.00000000000002132, -4.612695725900422872 ) ) ;
#32952=EDGE_CURVE ( 'NONE', #1225, #17959, #628, .T. ) ;
#32965=CARTESIAN_POINT ( 'NONE',  ( 107.6039373603924645, 18.80783371073036037, -5.109269587507049515 ) ) ;
#32967=CARTESIAN_POINT ( 'NONE',  ( -19.40370476787681042, 16.88291497481784020, 1.811101872898883469 ) ) ;
#32977=VERTEX_POINT ( 'NONE', #32228 ) ;
#32978=CARTESIAN_POINT ( 'NONE',  ( 25.05859343314882537, 19.07886064307538021, -1.500000000000000000 ) ) ;
#32997=CARTESIAN_POINT ( 'NONE',  ( 107.1772993348646139, 16.40207914262226296, 0.000000000000000000 ) ) ;
#33001=CARTESIAN_POINT ( 'NONE',  ( -40.76519394227695159, -12.76841724022742852, 5.871858310191298003 ) ) ;
#33007=CARTESIAN_POINT ( 'NONE',  ( -0.2059365608663963898, 0.000000000000000000, 0.000000000000000000 ) ) ;
#33014=CARTESIAN_POINT ( 'NONE',  ( -47.64323377349501243, 16.45499999999998408, 1.050000000000000044 ) ) ;
#33028=B_SPLINE_CURVE_WITH_KNOTS ( 'NONE', 3,
 ( #20223, #25730, #12531, #5177, #27725, #2860 ),
 .UNSPECIFIED., .F., .F.,
 ( 4, 2, 4 ),
 ( 0.000000000000000000, 0.001992811738820069942, 0.003985623477640139883 ),
 .UNSPECIFIED. ) ;
#33041=CARTESIAN_POINT ( 'NONE',  ( 56.97280603064898941, -277.2763395528616002, -1.491740999229418829 ) ) ;
#33042=CARTESIAN_POINT ( 'NONE',  ( -53.95513674679793326, 5.522463357794191730, 1.050000000000049116 ) ) ;
#33051=CARTESIAN_POINT ( 'NONE',  ( 107.4454455519092164, 16.41225027714849816, -1.478824073157309016 ) ) ;
#33091=DIRECTION ( 'NONE',  ( -1.000000000000000000, 0.000000000000000000, 0.000000000000000000 ) ) ;
#33141=COLOUR_RGB('Black', 0.09019608, 0.27058824, 0.51372549);
#33142=FILL_AREA_STYLE_COLOUR('',#33141);
#33143=FILL_AREA_STYLE('',(#33142));
#33144=SURFACE_STYLE_FILL_AREA(#33143);
#33145=SURFACE_SIDE_STYLE('',(#33144));
#33146=SURFACE_STYLE_USAGE(.BOTH.,#33145);
#33147=PRESENTATION_STYLE_ASSIGNMENT((#33146));
#33150=STYLED_ITEM('',(#33147),#21573);
#33151=MECHANICAL_DESIGN_GEOMETRIC_PRESENTATION_REPRESENTATION('',(#33150),#8690);
ENDSEC;
END-ISO-10303-21;
